ISO-10303-21;
HEADER;
/* Generated by software containing ST-Developer
 * from STEP Tools, Inc. (www.steptools.com) 
 */

FILE_DESCRIPTION(
/* description */ (''),
/* implementation_level */ '2;1');

FILE_NAME(
/* name */ '19_Casing_Screw_ISO_4762_M10x35.step',
/* time_stamp */ '2026-10-26T03:50:32-07:00',
/* author */ (''),
/* organization */ (''),
/* preprocessor_version */ 'ST-DEVELOPER v20.2',
/* originating_system */ 'Autodesk Translation Framework v15.15.0.0',
/* authorisation */ '');

FILE_SCHEMA (('AUTOMOTIVE_DESIGN { 1 0 10303 214 3 1 1 }'));
ENDSEC;

DATA;
#10=MECHANICAL_DESIGN_GEOMETRIC_PRESENTATION_REPRESENTATION('',(#1057),#76660);
#170=B_SPLINE_SURFACE_WITH_KNOTS('',3,3,((#70882,#70883,#70884,#70885,#70886,
#70887,#70888,#70889,#70890,#70891,#70892,#70893,#70894,#70895,#70896,#70897,
#70898,#70899,#70900,#70901,#70902,#70903,#70904,#70905,#70906,#70907,#70908,
#70909,#70910,#70911,#70912,#70913,#70914,#70915,#70916,#70917,#70918,#70919,
#70920,#70921,#70922,#70923,#70924,#70925,#70926,#70927,#70928,#70929,#70930,
#70931,#70932,#70933,#70934,#70935,#70936,#70937,#70938,#70939,#70940,#70941,
#70942,#70943,#70944,#70945,#70946,#70947,#70948,#70949,#70950,#70951,#70952,
#70953,#70954,#70955,#70956,#70957,#70958,#70959,#70960,#70961,#70962,#70963,
#70964,#70965,#70966,#70967,#70968,#70969,#70970,#70971,#70972,#70973,#70974,
#70975,#70976,#70977,#70978,#70979,#70980,#70981,#70982,#70983,#70984,#70985,
#70986,#70987,#70988,#70989,#70990,#70991,#70992,#70993,#70994,#70995,#70996,
#70997,#70998,#70999,#71000,#71001,#71002,#71003,#71004,#71005,#71006,#71007,
#71008,#71009,#71010,#71011,#71012,#71013,#71014,#71015,#71016,#71017,#71018,
#71019,#71020,#71021,#71022,#71023,#71024,#71025,#71026,#71027,#71028,#71029,
#71030,#71031,#71032),(#71033,#71034,#71035,#71036,#71037,#71038,#71039,
#71040,#71041,#71042,#71043,#71044,#71045,#71046,#71047,#71048,#71049,#71050,
#71051,#71052,#71053,#71054,#71055,#71056,#71057,#71058,#71059,#71060,#71061,
#71062,#71063,#71064,#71065,#71066,#71067,#71068,#71069,#71070,#71071,#71072,
#71073,#71074,#71075,#71076,#71077,#71078,#71079,#71080,#71081,#71082,#71083,
#71084,#71085,#71086,#71087,#71088,#71089,#71090,#71091,#71092,#71093,#71094,
#71095,#71096,#71097,#71098,#71099,#71100,#71101,#71102,#71103,#71104,#71105,
#71106,#71107,#71108,#71109,#71110,#71111,#71112,#71113,#71114,#71115,#71116,
#71117,#71118,#71119,#71120,#71121,#71122,#71123,#71124,#71125,#71126,#71127,
#71128,#71129,#71130,#71131,#71132,#71133,#71134,#71135,#71136,#71137,#71138,
#71139,#71140,#71141,#71142,#71143,#71144,#71145,#71146,#71147,#71148,#71149,
#71150,#71151,#71152,#71153,#71154,#71155,#71156,#71157,#71158,#71159,#71160,
#71161,#71162,#71163,#71164,#71165,#71166,#71167,#71168,#71169,#71170,#71171,
#71172,#71173,#71174,#71175,#71176,#71177,#71178,#71179,#71180,#71181,#71182,
#71183),(#71184,#71185,#71186,#71187,#71188,#71189,#71190,#71191,#71192,
#71193,#71194,#71195,#71196,#71197,#71198,#71199,#71200,#71201,#71202,#71203,
#71204,#71205,#71206,#71207,#71208,#71209,#71210,#71211,#71212,#71213,#71214,
#71215,#71216,#71217,#71218,#71219,#71220,#71221,#71222,#71223,#71224,#71225,
#71226,#71227,#71228,#71229,#71230,#71231,#71232,#71233,#71234,#71235,#71236,
#71237,#71238,#71239,#71240,#71241,#71242,#71243,#71244,#71245,#71246,#71247,
#71248,#71249,#71250,#71251,#71252,#71253,#71254,#71255,#71256,#71257,#71258,
#71259,#71260,#71261,#71262,#71263,#71264,#71265,#71266,#71267,#71268,#71269,
#71270,#71271,#71272,#71273,#71274,#71275,#71276,#71277,#71278,#71279,#71280,
#71281,#71282,#71283,#71284,#71285,#71286,#71287,#71288,#71289,#71290,#71291,
#71292,#71293,#71294,#71295,#71296,#71297,#71298,#71299,#71300,#71301,#71302,
#71303,#71304,#71305,#71306,#71307,#71308,#71309,#71310,#71311,#71312,#71313,
#71314,#71315,#71316,#71317,#71318,#71319,#71320,#71321,#71322,#71323,#71324,
#71325,#71326,#71327,#71328,#71329,#71330,#71331,#71332,#71333,#71334),
(#71335,#71336,#71337,#71338,#71339,#71340,#71341,#71342,#71343,#71344,
#71345,#71346,#71347,#71348,#71349,#71350,#71351,#71352,#71353,#71354,#71355,
#71356,#71357,#71358,#71359,#71360,#71361,#71362,#71363,#71364,#71365,#71366,
#71367,#71368,#71369,#71370,#71371,#71372,#71373,#71374,#71375,#71376,#71377,
#71378,#71379,#71380,#71381,#71382,#71383,#71384,#71385,#71386,#71387,#71388,
#71389,#71390,#71391,#71392,#71393,#71394,#71395,#71396,#71397,#71398,#71399,
#71400,#71401,#71402,#71403,#71404,#71405,#71406,#71407,#71408,#71409,#71410,
#71411,#71412,#71413,#71414,#71415,#71416,#71417,#71418,#71419,#71420,#71421,
#71422,#71423,#71424,#71425,#71426,#71427,#71428,#71429,#71430,#71431,#71432,
#71433,#71434,#71435,#71436,#71437,#71438,#71439,#71440,#71441,#71442,#71443,
#71444,#71445,#71446,#71447,#71448,#71449,#71450,#71451,#71452,#71453,#71454,
#71455,#71456,#71457,#71458,#71459,#71460,#71461,#71462,#71463,#71464,#71465,
#71466,#71467,#71468,#71469,#71470,#71471,#71472,#71473,#71474,#71475,#71476,
#71477,#71478,#71479,#71480,#71481,#71482,#71483,#71484,#71485)),
 .UNSPECIFIED.,.F.,.F.,.F.,(4,4),(4,1,1,1,1,1,1,1,1,1,1,1,1,1,1,1,1,1,1,
1,1,1,1,1,1,1,1,1,1,1,1,1,1,1,1,1,1,1,1,1,1,1,1,1,1,1,1,1,1,1,1,1,1,1,1,
1,1,1,1,1,1,1,1,1,1,1,1,1,1,1,1,1,1,1,1,1,1,1,1,1,1,1,1,1,1,1,1,1,1,1,1,
1,1,1,1,1,1,1,1,1,1,1,1,1,1,1,1,1,1,1,1,1,1,1,1,1,1,1,1,1,1,1,1,1,1,1,1,
1,1,1,1,1,1,1,1,1,1,1,1,1,1,1,1,1,1,1,1,1,4),(0.,0.0986691610045069),(8.3098959515534,
8.80937110859088,9.30884626562835,10.3077965797033,11.3067468937783,12.3056972078532,
13.3046475219282,14.3035978360031,15.3025481500781,16.3014984641531,17.300448778228,
18.299399092303,19.2983494063779,20.2972997204529,21.2962500345278,22.2952003486028,
23.2941506626778,24.2931009767527,25.2920512908277,26.2910016049026,27.2899519189776,
28.2889022330525,29.2878525471275,30.2868028612024,31.2857531752774,32.2847034893524,
33.2836538034273,34.2826041175023,35.2815544315772,36.2805047456522,37.2794550597271,
38.2784053738021,39.2773556878771,40.276306001952,41.275256316027,42.2742066301019,
43.2731569441769,44.2721072582518,45.2710575723268,46.2700078864018,47.2689582004767,
48.2679085145517,49.2668588286266,50.2658091427016,51.2647594567765,52.2637097708515,
53.2626600849265,54.2616103990014,55.2605607130764,56.2595110271513,57.2584613412263,
58.2574116553012,59.2563619693762,60.2553122834511,61.2542625975261,62.2532129116011,
63.252163225676,64.251113539751,65.2500638538259,66.2490141679009,67.2479644819759,
68.2469147960508,69.2458651101258,70.2448154242007,71.2437657382757,72.2427160523506,
73.2416663664256,74.2406166805006,75.2395669945755,76.2385173086505,77.2374676227254,
78.2364179368004,79.2353682508753,80.2343185649503,81.2332688790252,82.2322191931002,
83.2311695071752,84.2301198212501,85.2290701353251,86.2280204494,87.226970763475,
88.2259210775499,89.2248713916249,90.2238217056999,91.2227720197748,92.2217223338498,
93.2206726479247,94.2196229619997,95.2185732760747,96.2175235901496,97.2164739042246,
98.2154242182995,99.2143745323745,100.213324846449,101.212275160524,102.211225474599,
103.210175788674,104.209126102749,105.208076416824,106.207026730899,107.205977044974,
108.204927359049,109.203877673124,110.202827987199,111.201778301274,112.200728615349,
113.199678929424,114.198629243499,115.197579557574,116.196529871649,117.195480185724,
118.194430499799,119.193380813874,120.192331127949,121.191281442024,122.190231756098,
123.189182070173,124.188132384248,125.187082698323,126.186033012398,127.184983326473,
128.183933640548,129.182883954623,130.181834268698,131.180784582773,132.179734896848,
133.178685210923,134.177635524998,135.176585839073,136.175536153148,137.174486467223,
138.173436781298,139.172387095373,140.171337409448,141.170287723523,142.169238037598,
143.168188351673,144.167138665748,145.166088979822,146.165039293897,147.163989607972,
148.162939922047,149.161890236122,150.160840550197,151.159790864272,152.158741178347,
153.157691492422,153.65716664946,154.156641806497),.UNSPECIFIED.);
#171=B_SPLINE_SURFACE_WITH_KNOTS('',3,3,((#71662,#71663,#71664,#71665,#71666,
#71667,#71668,#71669,#71670,#71671,#71672,#71673,#71674,#71675,#71676,#71677,
#71678,#71679,#71680,#71681,#71682,#71683,#71684,#71685,#71686,#71687,#71688,
#71689,#71690,#71691,#71692,#71693,#71694,#71695,#71696,#71697,#71698,#71699,
#71700,#71701,#71702,#71703,#71704,#71705,#71706,#71707,#71708,#71709,#71710,
#71711,#71712,#71713,#71714,#71715,#71716,#71717,#71718,#71719,#71720,#71721,
#71722,#71723,#71724,#71725,#71726,#71727,#71728,#71729,#71730,#71731,#71732,
#71733,#71734,#71735,#71736,#71737,#71738,#71739,#71740,#71741,#71742,#71743,
#71744,#71745,#71746,#71747,#71748,#71749,#71750,#71751,#71752,#71753,#71754,
#71755,#71756,#71757,#71758,#71759,#71760,#71761,#71762,#71763,#71764,#71765,
#71766,#71767,#71768,#71769,#71770,#71771,#71772,#71773,#71774,#71775,#71776,
#71777,#71778,#71779,#71780,#71781,#71782,#71783,#71784,#71785,#71786,#71787,
#71788,#71789,#71790,#71791,#71792,#71793,#71794,#71795,#71796,#71797,#71798,
#71799,#71800,#71801,#71802,#71803,#71804,#71805,#71806,#71807,#71808,#71809,
#71810,#71811,#71812),(#71813,#71814,#71815,#71816,#71817,#71818,#71819,
#71820,#71821,#71822,#71823,#71824,#71825,#71826,#71827,#71828,#71829,#71830,
#71831,#71832,#71833,#71834,#71835,#71836,#71837,#71838,#71839,#71840,#71841,
#71842,#71843,#71844,#71845,#71846,#71847,#71848,#71849,#71850,#71851,#71852,
#71853,#71854,#71855,#71856,#71857,#71858,#71859,#71860,#71861,#71862,#71863,
#71864,#71865,#71866,#71867,#71868,#71869,#71870,#71871,#71872,#71873,#71874,
#71875,#71876,#71877,#71878,#71879,#71880,#71881,#71882,#71883,#71884,#71885,
#71886,#71887,#71888,#71889,#71890,#71891,#71892,#71893,#71894,#71895,#71896,
#71897,#71898,#71899,#71900,#71901,#71902,#71903,#71904,#71905,#71906,#71907,
#71908,#71909,#71910,#71911,#71912,#71913,#71914,#71915,#71916,#71917,#71918,
#71919,#71920,#71921,#71922,#71923,#71924,#71925,#71926,#71927,#71928,#71929,
#71930,#71931,#71932,#71933,#71934,#71935,#71936,#71937,#71938,#71939,#71940,
#71941,#71942,#71943,#71944,#71945,#71946,#71947,#71948,#71949,#71950,#71951,
#71952,#71953,#71954,#71955,#71956,#71957,#71958,#71959,#71960,#71961,#71962,
#71963),(#71964,#71965,#71966,#71967,#71968,#71969,#71970,#71971,#71972,
#71973,#71974,#71975,#71976,#71977,#71978,#71979,#71980,#71981,#71982,#71983,
#71984,#71985,#71986,#71987,#71988,#71989,#71990,#71991,#71992,#71993,#71994,
#71995,#71996,#71997,#71998,#71999,#72000,#72001,#72002,#72003,#72004,#72005,
#72006,#72007,#72008,#72009,#72010,#72011,#72012,#72013,#72014,#72015,#72016,
#72017,#72018,#72019,#72020,#72021,#72022,#72023,#72024,#72025,#72026,#72027,
#72028,#72029,#72030,#72031,#72032,#72033,#72034,#72035,#72036,#72037,#72038,
#72039,#72040,#72041,#72042,#72043,#72044,#72045,#72046,#72047,#72048,#72049,
#72050,#72051,#72052,#72053,#72054,#72055,#72056,#72057,#72058,#72059,#72060,
#72061,#72062,#72063,#72064,#72065,#72066,#72067,#72068,#72069,#72070,#72071,
#72072,#72073,#72074,#72075,#72076,#72077,#72078,#72079,#72080,#72081,#72082,
#72083,#72084,#72085,#72086,#72087,#72088,#72089,#72090,#72091,#72092,#72093,
#72094,#72095,#72096,#72097,#72098,#72099,#72100,#72101,#72102,#72103,#72104,
#72105,#72106,#72107,#72108,#72109,#72110,#72111,#72112,#72113,#72114),
(#72115,#72116,#72117,#72118,#72119,#72120,#72121,#72122,#72123,#72124,
#72125,#72126,#72127,#72128,#72129,#72130,#72131,#72132,#72133,#72134,#72135,
#72136,#72137,#72138,#72139,#72140,#72141,#72142,#72143,#72144,#72145,#72146,
#72147,#72148,#72149,#72150,#72151,#72152,#72153,#72154,#72155,#72156,#72157,
#72158,#72159,#72160,#72161,#72162,#72163,#72164,#72165,#72166,#72167,#72168,
#72169,#72170,#72171,#72172,#72173,#72174,#72175,#72176,#72177,#72178,#72179,
#72180,#72181,#72182,#72183,#72184,#72185,#72186,#72187,#72188,#72189,#72190,
#72191,#72192,#72193,#72194,#72195,#72196,#72197,#72198,#72199,#72200,#72201,
#72202,#72203,#72204,#72205,#72206,#72207,#72208,#72209,#72210,#72211,#72212,
#72213,#72214,#72215,#72216,#72217,#72218,#72219,#72220,#72221,#72222,#72223,
#72224,#72225,#72226,#72227,#72228,#72229,#72230,#72231,#72232,#72233,#72234,
#72235,#72236,#72237,#72238,#72239,#72240,#72241,#72242,#72243,#72244,#72245,
#72246,#72247,#72248,#72249,#72250,#72251,#72252,#72253,#72254,#72255,#72256,
#72257,#72258,#72259,#72260,#72261,#72262,#72263,#72264,#72265)),
 .UNSPECIFIED.,.F.,.F.,.F.,(4,4),(4,1,1,1,1,1,1,1,1,1,1,1,1,1,1,1,1,1,1,
1,1,1,1,1,1,1,1,1,1,1,1,1,1,1,1,1,1,1,1,1,1,1,1,1,1,1,1,1,1,1,1,1,1,1,1,
1,1,1,1,1,1,1,1,1,1,1,1,1,1,1,1,1,1,1,1,1,1,1,1,1,1,1,1,1,1,1,1,1,1,1,1,
1,1,1,1,1,1,1,1,1,1,1,1,1,1,1,1,1,1,1,1,1,1,1,1,1,1,1,1,1,1,1,1,1,1,1,1,
1,1,1,1,1,1,1,1,1,1,1,1,1,1,1,1,1,1,1,1,1,4),(0.,0.0986691610045069),(11.6147305479243,
12.1142057049618,12.6136808619992,13.6126311760742,14.6115814901491,15.6105318042241,
16.6094821182991,17.608432432374,18.607382746449,19.6063330605239,20.6052833745989,
21.6042336886738,22.6031840027488,23.6021343168238,24.6010846308987,25.6000349449737,
26.5989852590486,27.5979355731236,28.5968858871985,29.5958362012735,30.5947865153485,
31.5937368294234,32.5926871434984,33.5916374575733,34.5905877716483,35.5895380857232,
36.5884883997982,37.5874387138731,38.5863890279481,39.5853393420231,40.584289656098,
41.583239970173,42.5821902842479,43.5811405983229,44.5800909123978,45.5790412264728,
46.5779915405478,47.5769418546227,48.5758921686977,49.5748424827726,50.5737927968476,
51.5727431109225,52.5716934249975,53.5706437390725,54.5695940531474,55.5685443672224,
56.5674946812973,57.5664449953723,58.5653953094472,59.5643456235222,60.5632959375972,
61.5622462516721,62.5611965657471,63.560146879822,64.559097193897,65.5580475079719,
66.5569978220469,67.5559481361219,68.5548984501968,69.5538487642718,70.5527990783467,
71.5517493924217,72.5506997064966,73.5496500205716,74.5486003346466,75.5475506487215,
76.5465009627965,77.5454512768714,78.5444015909464,79.5433519050213,80.5423022190963,
81.5412525331712,82.5402028472462,83.5391531613212,84.5381034753961,85.5370537894711,
86.536004103546,87.534954417621,88.5339047316959,89.5328550457709,90.5318053598459,
91.5307556739208,92.5297059879958,93.5286563020707,94.5276066161457,95.5265569302206,
96.5255072442956,97.5244575583706,98.5234078724455,99.5223581865205,100.521308500595,
101.52025881467,102.519209128745,103.51815944282,104.517109756895,105.51606007097,
106.515010385045,107.51396069912,108.512911013195,109.51186132727,110.510811641345,
111.50976195542,112.508712269495,113.50766258357,114.506612897645,115.50556321172,
116.504513525795,117.50346383987,118.502414153945,119.50136446802,120.500314782095,
121.49926509617,122.498215410244,123.497165724319,124.496116038394,125.495066352469,
126.494016666544,127.492966980619,128.491917294694,129.490867608769,130.489817922844,
131.488768236919,132.487718550994,133.486668865069,134.485619179144,135.484569493219,
136.483519807294,137.482470121369,138.481420435444,139.480370749519,140.479321063594,
141.478271377669,142.477221691744,143.476172005819,144.475122319894,145.474072633968,
146.473022948043,147.471973262118,148.470923576193,149.469873890268,150.468824204343,
151.467774518418,152.466724832493,153.465675146568,154.464625460643,155.463575774718,
156.462526088793,156.96200124583,157.461476402868),.UNSPECIFIED.);
#814=B_SPLINE_CURVE_WITH_KNOTS('',3,(#69071,#69072,#69073,#69074,#69075,
#69076,#69077,#69078,#69079,#69080),.UNSPECIFIED.,.F.,.F.,(4,3,3,4),(-4.09323272002467,
-3.99580125629983,-2.99685094222487,-2.06652207565085),.UNSPECIFIED.);
#815=B_SPLINE_CURVE_WITH_KNOTS('',3,(#69083,#69084,#69085,#69086,#69087,
#69088,#69089,#69090,#69091,#69092),.UNSPECIFIED.,.F.,.F.,(4,3,3,4),(0.,
0.499475157037477,0.998950314074958,1.1148820092159),.UNSPECIFIED.);
#816=B_SPLINE_CURVE_WITH_KNOTS('',3,(#69097,#69098,#69099,#69100,#69101,
#69102,#69103,#69104,#69105,#69106,#69107,#69108,#69109,#69110,#69111,#69112,
#69113,#69114,#69115,#69116,#69117,#69118),.UNSPECIFIED.,.F.,.F.,(4,3,3,
3,3,3,3,4),(-10.3764180272043,-9.98950314074957,-8.99055282667461,-7.99160251259965,
-6.9926521985247,-5.99370188444974,-4.99475157037478,-4.09323272002467),
 .UNSPECIFIED.);
#817=B_SPLINE_CURVE_WITH_KNOTS('',3,(#69119,#69120,#69121,#69122,#69123,
#69124,#69125,#69126,#69127,#69128,#69129,#69130,#69131,#69132,#69133,#69134,
#69135,#69136,#69137,#69138,#69139,#69140),.UNSPECIFIED.,.F.,.F.,(4,3,3,
3,3,3,3,4),(1.1148820092159,1.99790062814991,2.99685094222487,3.99580125629982,
4.99475157037478,5.99370188444973,6.99265219852469,7.39806731639549),
 .UNSPECIFIED.);
#818=B_SPLINE_CURVE_WITH_KNOTS('',3,(#69145,#69146,#69147,#69148,#69149,
#69150,#69151,#69152,#69153,#69154,#69155,#69156,#69157,#69158,#69159,#69160,
#69161,#69162,#69163,#69164,#69165,#69166),.UNSPECIFIED.,.F.,.F.,(4,3,3,
3,3,3,3,4),(-16.6596033343838,-15.9832050251993,-14.9842547111244,-13.9853043970494,
-12.9863540829744,-11.9874037688995,-10.9884534548245,-10.3764180272043),
 .UNSPECIFIED.);
#819=B_SPLINE_CURVE_WITH_KNOTS('',3,(#69167,#69168,#69169,#69170,#69171,
#69172,#69173,#69174,#69175,#69176,#69177,#69178,#69179,#69180,#69181,#69182,
#69183,#69184,#69185,#69186,#69187,#69188),.UNSPECIFIED.,.F.,.F.,(4,3,3,
3,3,3,3,4),(7.39806731639549,7.99160251259965,8.99055282667461,9.98950314074957,
10.9884534548245,11.9874037688995,12.9863540829744,13.6812526235751),
 .UNSPECIFIED.);
#820=B_SPLINE_CURVE_WITH_KNOTS('',3,(#69193,#69194,#69195,#69196,#69197,
#69198,#69199,#69200,#69201,#69202,#69203,#69204,#69205,#69206,#69207,#69208,
#69209,#69210,#69211,#69212,#69213,#69214),.UNSPECIFIED.,.F.,.F.,(4,3,3,
3,3,3,3,4),(-22.9427886415634,-21.976906909649,-20.9779565955741,-19.9790062814991,
-18.9800559674242,-17.9811056533492,-16.9821553392743,-16.6596033343838),
 .UNSPECIFIED.);
#821=B_SPLINE_CURVE_WITH_KNOTS('',3,(#69215,#69216,#69217,#69218,#69219,
#69220,#69221,#69222,#69223,#69224,#69225,#69226,#69227,#69228,#69229,#69230,
#69231,#69232,#69233,#69234,#69235,#69236),.UNSPECIFIED.,.F.,.F.,(4,3,3,
3,3,3,3,4),(13.6812526235751,13.9853043970494,14.9842547111244,15.9832050251993,
16.9821553392743,17.9811056533492,18.9800559674242,19.9644379307546),
 .UNSPECIFIED.);
#822=B_SPLINE_CURVE_WITH_KNOTS('',3,(#69241,#69242,#69243,#69244,#69245,
#69246,#69247,#69248,#69249,#69250,#69251,#69252,#69253,#69254,#69255,#69256,
#69257,#69258,#69259,#69260,#69261,#69262,#69263,#69264,#69265),
 .UNSPECIFIED.,.F.,.F.,(4,3,3,3,3,3,3,3,4),(-29.225973948743,-28.9695591081737,
-27.9706087940988,-26.9716584800238,-25.9727081659489,-24.9737578518739,
-23.974807537799,-22.975857223724,-22.9427886415634),.UNSPECIFIED.);
#823=B_SPLINE_CURVE_WITH_KNOTS('',3,(#69266,#69267,#69268,#69269,#69270,
#69271,#69272,#69273,#69274,#69275,#69276,#69277,#69278,#69279,#69280,#69281,
#69282,#69283,#69284,#69285,#69286,#69287,#69288,#69289,#69290),
 .UNSPECIFIED.,.F.,.F.,(4,3,3,3,3,3,3,3,4),(19.9644379307546,19.9790062814991,
20.9779565955741,21.976906909649,22.975857223724,23.974807537799,24.9737578518739,
25.9727081659489,26.2476232379342),.UNSPECIFIED.);
#824=B_SPLINE_CURVE_WITH_KNOTS('',3,(#69295,#69296,#69297,#69298,#69299,
#69300,#69301,#69302,#69303,#69304,#69305,#69306,#69307,#69308,#69309,#69310,
#69311,#69312,#69313,#69314,#69315,#69316),.UNSPECIFIED.,.F.,.F.,(4,3,3,
3,3,3,3,4),(-35.5091592559226,-34.9632609926235,-33.9643106785485,-32.9653603644736,
-31.9664100503986,-30.9674597363237,-29.9685094222487,-29.225973948743),
 .UNSPECIFIED.);
#825=B_SPLINE_CURVE_WITH_KNOTS('',3,(#69317,#69318,#69319,#69320,#69321,
#69322,#69323,#69324,#69325,#69326,#69327,#69328,#69329,#69330,#69331,#69332,
#69333,#69334,#69335,#69336,#69337,#69338),.UNSPECIFIED.,.F.,.F.,(4,3,3,
3,3,3,3,4),(26.2476232379342,26.9716584800238,27.9706087940988,28.9695591081738,
29.9685094222487,30.9674597363237,31.9664100503986,32.5308085451138),
 .UNSPECIFIED.);
#826=B_SPLINE_CURVE_WITH_KNOTS('',3,(#69343,#69344,#69345,#69346,#69347,
#69348,#69349,#69350,#69351,#69352,#69353,#69354,#69355,#69356,#69357,#69358,
#69359,#69360,#69361,#69362,#69363,#69364),.UNSPECIFIED.,.F.,.F.,(4,3,3,
3,3,3,3,4),(-41.7923445631022,-40.9569628770732,-39.9580125629983,-38.9590622489233,
-37.9601119348484,-36.9611616207734,-35.9622113066984,-35.5091592559226),
 .UNSPECIFIED.);
#827=B_SPLINE_CURVE_WITH_KNOTS('',3,(#69365,#69366,#69367,#69368,#69369,
#69370,#69371,#69372,#69373,#69374,#69375,#69376,#69377,#69378,#69379,#69380,
#69381,#69382,#69383,#69384,#69385,#69386),.UNSPECIFIED.,.F.,.F.,(4,3,3,
3,3,3,3,4),(32.5308085451138,32.9653603644736,33.9643106785485,34.9632609926235,
35.9622113066984,36.9611616207734,37.9601119348484,38.8139938522934),
 .UNSPECIFIED.);
#828=B_SPLINE_CURVE_WITH_KNOTS('',3,(#69391,#69392,#69393,#69394,#69395,
#69396,#69397,#69398,#69399,#69400,#69401,#69402,#69403,#69404,#69405,#69406,
#69407,#69408,#69409,#69410,#69411,#69412,#69413,#69414,#69415),
 .UNSPECIFIED.,.F.,.F.,(4,3,3,3,3,3,3,3,4),(-48.0755298702818,-47.9496150755979,
-46.950664761523,-45.951714447448,-44.9527641333731,-43.9538138192981,-42.9548635052232,
-41.9559131911482,-41.7923445631022),.UNSPECIFIED.);
#829=B_SPLINE_CURVE_WITH_KNOTS('',3,(#69416,#69417,#69418,#69419,#69420,
#69421,#69422,#69423,#69424,#69425,#69426,#69427,#69428,#69429,#69430,#69431,
#69432,#69433,#69434,#69435,#69436,#69437,#69438,#69439,#69440),
 .UNSPECIFIED.,.F.,.F.,(4,3,3,3,3,3,3,3,4),(38.8139938522934,38.9590622489233,
39.9580125629983,40.9569628770732,41.9559131911482,42.9548635052232,43.9538138192981,
44.9527641333731,45.097179159473),.UNSPECIFIED.);
#830=B_SPLINE_CURVE_WITH_KNOTS('',3,(#69445,#69446,#69447,#69448,#69449,
#69450,#69451,#69452,#69453,#69454,#69455,#69456,#69457,#69458,#69459,#69460,
#69461,#69462,#69463,#69464,#69465,#69466),.UNSPECIFIED.,.F.,.F.,(4,3,3,
3,3,3,3,4),(-54.3587151774614,-53.9433169600477,-52.9443666459727,-51.9454163318978,
-50.9464660178228,-49.9475157037478,-48.9485653896729,-48.0755298702818),
 .UNSPECIFIED.);
#831=B_SPLINE_CURVE_WITH_KNOTS('',3,(#69467,#69468,#69469,#69470,#69471,
#69472,#69473,#69474,#69475,#69476,#69477,#69478,#69479,#69480,#69481,#69482,
#69483,#69484,#69485,#69486,#69487,#69488),.UNSPECIFIED.,.F.,.F.,(4,3,3,
3,3,3,3,4),(45.097179159473,45.951714447448,46.950664761523,47.9496150755979,
48.9485653896729,49.9475157037478,50.9464660178228,51.3803644666526),
 .UNSPECIFIED.);
#832=B_SPLINE_CURVE_WITH_KNOTS('',3,(#69493,#69494,#69495,#69496,#69497,
#69498,#69499,#69500,#69501,#69502,#69503,#69504,#69505,#69506,#69507,#69508,
#69509,#69510,#69511,#69512,#69513,#69514),.UNSPECIFIED.,.F.,.F.,(4,3,3,
3,3,3,3,4),(-60.641900484641,-59.9370188444974,-58.9380685304225,-57.9391182163475,
-56.9401679022725,-55.9412175881976,-54.9422672741226,-54.3587151774614),
 .UNSPECIFIED.);
#833=B_SPLINE_CURVE_WITH_KNOTS('',3,(#69515,#69516,#69517,#69518,#69519,
#69520,#69521,#69522,#69523,#69524,#69525,#69526,#69527,#69528,#69529,#69530,
#69531,#69532,#69533,#69534,#69535,#69536),.UNSPECIFIED.,.F.,.F.,(4,3,3,
3,3,3,3,4),(51.3803644666526,51.9454163318978,52.9443666459727,53.9433169600477,
54.9422672741226,55.9412175881976,56.9401679022725,57.6635497738322),
 .UNSPECIFIED.);
#834=B_SPLINE_CURVE_WITH_KNOTS('',3,(#69541,#69542,#69543,#69544,#69545,
#69546,#69547,#69548,#69549,#69550,#69551,#69552,#69553,#69554,#69555,#69556,
#69557,#69558,#69559,#69560,#69561,#69562),.UNSPECIFIED.,.F.,.F.,(4,3,3,
3,3,3,3,4),(-66.9250857918206,-65.9307207289471,-64.9317704148722,-63.9328201007972,
-62.9338697867223,-61.9349194726473,-60.9359691585724,-60.641900484641),
 .UNSPECIFIED.);
#835=B_SPLINE_CURVE_WITH_KNOTS('',3,(#69563,#69564,#69565,#69566,#69567,
#69568,#69569,#69570,#69571,#69572,#69573,#69574,#69575,#69576,#69577,#69578,
#69579,#69580,#69581,#69582,#69583,#69584,#69585,#69586,#69587),
 .UNSPECIFIED.,.F.,.F.,(4,3,3,3,3,3,3,3,4),(57.6635497738322,57.9391182163475,
58.9380685304225,59.9370188444974,60.9359691585724,61.9349194726473,62.9338697867223,
63.9328201007973,63.9467350810118),.UNSPECIFIED.);
#836=B_SPLINE_CURVE_WITH_KNOTS('',3,(#69592,#69593,#69594,#69595,#69596,
#69597,#69598,#69599,#69600,#69601,#69602,#69603,#69604,#69605,#69606,#69607,
#69608,#69609,#69610,#69611,#69612,#69613,#69614,#69615,#69616),
 .UNSPECIFIED.,.F.,.F.,(4,3,3,3,3,3,3,3,4),(-73.2082710990002,-72.9233729274718,
-71.9244226133969,-70.9254722993219,-69.926521985247,-68.927571671172,-67.928621357097,
-66.9296710430221,-66.9250857918206),.UNSPECIFIED.);
#837=B_SPLINE_CURVE_WITH_KNOTS('',3,(#69617,#69618,#69619,#69620,#69621,
#69622,#69623,#69624,#69625,#69626,#69627,#69628,#69629,#69630,#69631,#69632,
#69633,#69634,#69635,#69636,#69637,#69638),.UNSPECIFIED.,.F.,.F.,(4,3,3,
3,3,3,3,4),(63.9467350810118,64.9317704148722,65.9307207289472,66.9296710430221,
67.9286213570971,68.927571671172,69.926521985247,70.2299203881914),
 .UNSPECIFIED.);
#838=B_SPLINE_CURVE_WITH_KNOTS('',3,(#69643,#69644,#69645,#69646,#69647,
#69648,#69649,#69650,#69651,#69652,#69653,#69654,#69655,#69656,#69657,#69658,
#69659,#69660,#69661,#69662,#69663,#69664),.UNSPECIFIED.,.F.,.F.,(4,3,3,
3,3,3,3,4),(-79.4914564061798,-78.9170748119216,-77.9181244978466,-76.9191741837717,
-75.9202238696967,-74.9212735556218,-73.9223232415468,-73.2082710990002),
 .UNSPECIFIED.);
#839=B_SPLINE_CURVE_WITH_KNOTS('',3,(#69665,#69666,#69667,#69668,#69669,
#69670,#69671,#69672,#69673,#69674,#69675,#69676,#69677,#69678,#69679,#69680,
#69681,#69682,#69683,#69684,#69685,#69686),.UNSPECIFIED.,.F.,.F.,(4,3,3,
3,3,3,3,4),(70.2299203881914,70.925472299322,71.9244226133969,72.9233729274719,
73.9223232415468,74.9212735556218,75.9202238696967,76.513105695371),
 .UNSPECIFIED.);
#840=B_SPLINE_CURVE_WITH_KNOTS('',3,(#69691,#69692,#69693,#69694,#69695,
#69696,#69697,#69698,#69699,#69700,#69701,#69702,#69703,#69704,#69705,#69706,
#69707,#69708,#69709,#69710,#69711,#69712),.UNSPECIFIED.,.F.,.F.,(4,3,3,
3,3,3,3,4),(-85.7746417133593,-84.9107766963713,-83.9118263822964,-82.9128760682214,
-81.9139257541465,-80.9149754400715,-79.9160251259965,-79.4914564061798),
 .UNSPECIFIED.);
#841=B_SPLINE_CURVE_WITH_KNOTS('',3,(#69713,#69714,#69715,#69716,#69717,
#69718,#69719,#69720,#69721,#69722,#69723,#69724,#69725,#69726,#69727,#69728,
#69729,#69730,#69731,#69732,#69733,#69734),.UNSPECIFIED.,.F.,.F.,(4,3,3,
3,3,3,3,4),(76.513105695371,76.9191741837717,77.9181244978466,78.9170748119216,
79.9160251259966,80.9149754400715,81.9139257541465,82.7962910025506),
 .UNSPECIFIED.);
#842=B_SPLINE_CURVE_WITH_KNOTS('',3,(#69739,#69740,#69741,#69742,#69743,
#69744,#69745,#69746,#69747,#69748,#69749,#69750,#69751,#69752,#69753,#69754,
#69755,#69756,#69757,#69758,#69759,#69760,#69761,#69762,#69763),
 .UNSPECIFIED.,.F.,.F.,(4,3,3,3,3,3,3,3,4),(-92.057827020539,-91.903428894896,
-90.9044785808211,-89.9055282667461,-88.9065779526712,-87.9076276385962,
-86.9086773245212,-85.9097270104463,-85.7746417133593),.UNSPECIFIED.);
#843=B_SPLINE_CURVE_WITH_KNOTS('',3,(#69764,#69765,#69766,#69767,#69768,
#69769,#69770,#69771,#69772,#69773,#69774,#69775,#69776,#69777,#69778,#69779,
#69780,#69781,#69782,#69783,#69784,#69785,#69786,#69787,#69788),
 .UNSPECIFIED.,.F.,.F.,(4,3,3,3,3,3,3,3,4),(82.7962910025506,82.9128760682214,
83.9118263822964,84.9107766963714,85.9097270104463,86.9086773245213,87.9076276385962,
88.9065779526712,89.0794763097302),.UNSPECIFIED.);
#844=B_SPLINE_CURVE_WITH_KNOTS('',3,(#69793,#69794,#69795,#69796,#69797,
#69798,#69799,#69800,#69801,#69802,#69803,#69804,#69805,#69806,#69807,#69808,
#69809,#69810,#69811,#69812,#69813,#69814),.UNSPECIFIED.,.F.,.F.,(4,3,3,
3,3,3,3,4),(-98.3410123277185,-97.8971307793458,-96.8981804652708,-95.8992301511959,
-94.9002798371209,-93.9013295230459,-92.902379208971,-92.057827020539),
 .UNSPECIFIED.);
#845=B_SPLINE_CURVE_WITH_KNOTS('',3,(#69815,#69816,#69817,#69818,#69819,
#69820,#69821,#69822,#69823,#69824,#69825,#69826,#69827,#69828,#69829,#69830,
#69831,#69832,#69833,#69834,#69835,#69836),.UNSPECIFIED.,.F.,.F.,(4,3,3,
3,3,3,3,4),(89.0794763097302,89.9055282667461,90.9044785808211,91.903428894896,
92.902379208971,93.901329523046,94.9002798371209,95.3626616169097),
 .UNSPECIFIED.);
#846=B_SPLINE_CURVE_WITH_KNOTS('',3,(#69841,#69842,#69843,#69844,#69845,
#69846,#69847,#69848,#69849,#69850,#69851,#69852,#69853,#69854,#69855,#69856,
#69857,#69858,#69859,#69860,#69861,#69862),.UNSPECIFIED.,.F.,.F.,(4,3,3,
3,3,3,3,4),(-104.624197634898,-103.890832663796,-102.891882349721,-101.892932035646,
-100.893981721571,-99.8950314074957,-98.8960810934207,-98.3410123277185),
 .UNSPECIFIED.);
#847=B_SPLINE_CURVE_WITH_KNOTS('',3,(#69863,#69864,#69865,#69866,#69867,
#69868,#69869,#69870,#69871,#69872,#69873,#69874,#69875,#69876,#69877,#69878,
#69879,#69880,#69881,#69882,#69883,#69884),.UNSPECIFIED.,.F.,.F.,(4,3,3,
3,3,3,3,4),(95.3626616169097,95.8992301511959,96.8981804652708,97.8971307793458,
98.8960810934207,99.8950314074957,100.893981721571,101.645846924089),
 .UNSPECIFIED.);
#848=B_SPLINE_CURVE_WITH_KNOTS('',3,(#69889,#69890,#69891,#69892,#69893,
#69894,#69895,#69896,#69897,#69898,#69899,#69900,#69901,#69902,#69903,#69904,
#69905,#69906,#69907,#69908,#69909,#69910,#69911,#69912,#69913),
 .UNSPECIFIED.,.F.,.F.,(4,3,3,3,3,3,3,3,4),(-110.907382942078,-110.88348486232,
-109.884534548245,-108.88558423417,-107.886633920095,-106.88768360602,-105.888733291945,
-104.88978297787,-104.624197634898),.UNSPECIFIED.);
#849=B_SPLINE_CURVE_WITH_KNOTS('',3,(#69914,#69915,#69916,#69917,#69918,
#69919,#69920,#69921,#69922,#69923,#69924,#69925,#69926,#69927,#69928,#69929,
#69930,#69931,#69932,#69933,#69934,#69935,#69936,#69937,#69938),
 .UNSPECIFIED.,.F.,.F.,(4,3,3,3,3,3,3,3,4),(101.645846924089,101.892932035646,
102.891882349721,103.890832663795,104.88978297787,105.888733291945,106.88768360602,
107.886633920095,107.929032231269),.UNSPECIFIED.);
#850=B_SPLINE_CURVE_WITH_KNOTS('',3,(#69943,#69944,#69945,#69946,#69947,
#69948,#69949,#69950,#69951,#69952,#69953,#69954,#69955,#69956,#69957,#69958,
#69959,#69960,#69961,#69962,#69963,#69964),.UNSPECIFIED.,.F.,.F.,(4,3,3,
3,3,3,3,4),(-117.190568249257,-116.87718674677,-115.878236432695,-114.87928611862,
-113.880335804545,-112.88138549047,-111.882435176395,-110.907382942078),
 .UNSPECIFIED.);
#851=B_SPLINE_CURVE_WITH_KNOTS('',3,(#69965,#69966,#69967,#69968,#69969,
#69970,#69971,#69972,#69973,#69974,#69975,#69976,#69977,#69978,#69979,#69980,
#69981,#69982,#69983,#69984,#69985,#69986),.UNSPECIFIED.,.F.,.F.,(4,3,3,
3,3,3,3,4),(107.929032231269,108.88558423417,109.884534548245,110.88348486232,
111.882435176395,112.88138549047,113.880335804545,114.212217538449),
 .UNSPECIFIED.);
#852=B_SPLINE_CURVE_WITH_KNOTS('',3,(#69991,#69992,#69993,#69994,#69995,
#69996,#69997,#69998,#69999,#70000,#70001,#70002,#70003,#70004,#70005,#70006,
#70007,#70008,#70009,#70010,#70011,#70012),.UNSPECIFIED.,.F.,.F.,(4,3,3,
3,3,3,3,4),(-123.473753556437,-122.87088863122,-121.871938317145,-120.87298800307,
-119.874037688995,-118.87508737492,-117.876137060845,-117.190568249257),
 .UNSPECIFIED.);
#853=B_SPLINE_CURVE_WITH_KNOTS('',3,(#70013,#70014,#70015,#70016,#70017,
#70018,#70019,#70020,#70021,#70022,#70023,#70024,#70025,#70026,#70027,#70028,
#70029,#70030,#70031,#70032,#70033,#70034),.UNSPECIFIED.,.F.,.F.,(4,3,3,
3,3,3,3,4),(114.212217538449,114.87928611862,115.878236432695,116.87718674677,
117.876137060845,118.87508737492,119.874037688995,120.495402845628),
 .UNSPECIFIED.);
#854=B_SPLINE_CURVE_WITH_KNOTS('',3,(#70039,#70040,#70041,#70042,#70043,
#70044,#70045,#70046,#70047,#70048,#70049,#70050,#70051,#70052,#70053,#70054,
#70055,#70056,#70057,#70058,#70059,#70060),.UNSPECIFIED.,.F.,.F.,(4,3,3,
3,3,3,3,4),(-129.756938863617,-128.864590515669,-127.865640201594,-126.86668988752,
-125.867739573445,-124.86878925937,-123.869838945295,-123.473753556437),
 .UNSPECIFIED.);
#855=B_SPLINE_CURVE_WITH_KNOTS('',3,(#70061,#70062,#70063,#70064,#70065,
#70066,#70067,#70068,#70069,#70070,#70071,#70072,#70073,#70074,#70075,#70076,
#70077,#70078,#70079,#70080,#70081,#70082),.UNSPECIFIED.,.F.,.F.,(4,3,3,
3,3,3,3,4),(120.495402845628,120.87298800307,121.871938317145,122.87088863122,
123.869838945295,124.86878925937,125.867739573445,126.778588152808),
 .UNSPECIFIED.);
#856=B_SPLINE_CURVE_WITH_KNOTS('',3,(#70087,#70088,#70089,#70090,#70091,
#70092,#70093,#70094,#70095,#70096,#70097,#70098,#70099,#70100,#70101,#70102,
#70103,#70104,#70105,#70106,#70107,#70108,#70109,#70110,#70111),
 .UNSPECIFIED.,.F.,.F.,(4,3,3,3,3,3,3,3,4),(-136.040124170796,-135.857242714194,
-134.858292400119,-133.859342086044,-132.860391771969,-131.861441457894,
-130.862491143819,-129.863540829744,-129.756938863617),.UNSPECIFIED.);
#857=B_SPLINE_CURVE_WITH_KNOTS('',3,(#70112,#70113,#70114,#70115,#70116,
#70117,#70118,#70119,#70120,#70121,#70122,#70123,#70124,#70125,#70126,#70127,
#70128,#70129,#70130,#70131,#70132,#70133,#70134,#70135,#70136),
 .UNSPECIFIED.,.F.,.F.,(4,3,3,3,3,3,3,3,4),(126.778588152808,126.86668988752,
127.865640201594,128.864590515669,129.863540829744,130.862491143819,131.861441457894,
132.860391771969,133.061773459987),.UNSPECIFIED.);
#858=B_SPLINE_CURVE_WITH_KNOTS('',3,(#70141,#70142,#70143,#70144,#70145,
#70146,#70147,#70148,#70149,#70150,#70151,#70152,#70153,#70154,#70155,#70156,
#70157,#70158,#70159,#70160,#70161,#70162),.UNSPECIFIED.,.F.,.F.,(4,3,3,
3,3,3,3,4),(-142.323309477976,-141.850944598644,-140.851994284569,-139.853043970494,
-138.854093656419,-137.855143342344,-136.856193028269,-136.040124170796),
 .UNSPECIFIED.);
#859=B_SPLINE_CURVE_WITH_KNOTS('',3,(#70163,#70164,#70165,#70166,#70167,
#70168,#70169,#70170,#70171,#70172,#70173,#70174,#70175,#70176,#70177,#70178,
#70179,#70180,#70181,#70182,#70183,#70184),.UNSPECIFIED.,.F.,.F.,(4,3,3,
3,3,3,3,4),(133.061773459987,133.859342086044,134.858292400119,135.857242714194,
136.856193028269,137.855143342344,138.854093656419,139.344958767167),
 .UNSPECIFIED.);
#860=B_SPLINE_CURVE_WITH_KNOTS('',3,(#70190,#70191,#70192,#70193,#70194),
 .UNSPECIFIED.,.F.,.F.,(4,1,4),(153.9380400259,154.464625460643,155.394954327217),
 .UNSPECIFIED.);
#861=B_SPLINE_CURVE_WITH_KNOTS('',3,(#70197,#70198,#70199,#70200),
 .UNSPECIFIED.,.F.,.F.,(4,4),(153.9380400259,154.156641806497),
 .UNSPECIFIED.);
#862=B_SPLINE_CURVE_WITH_KNOTS('',3,(#70205,#70206,#70207,#70208,#70209,
#70210,#70211,#70212,#70213,#70214),.UNSPECIFIED.,.F.,.F.,(4,1,1,1,1,1,
1,4),(147.65485471872,148.470923576193,149.469873890268,150.468824204343,
151.467774518418,152.466724832493,153.465675146568,153.9380400259),
 .UNSPECIFIED.);
#863=B_SPLINE_CURVE_WITH_KNOTS('',3,(#70215,#70216,#70217,#70218,#70219,
#70220,#70221,#70222,#70223,#70224,#70225),.UNSPECIFIED.,.F.,.F.,(4,1,1,
1,1,1,1,1,4),(147.65485471872,148.162939922047,149.161890236122,150.160840550197,
151.159790864272,152.158741178347,153.157691492422,153.65716664946,153.9380400259),
 .UNSPECIFIED.);
#864=B_SPLINE_CURVE_WITH_KNOTS('',3,(#70230,#70231,#70232,#70233,#70234,
#70235,#70236,#70237,#70238,#70239,#70240),.UNSPECIFIED.,.F.,.F.,(4,1,1,
1,1,1,1,1,4),(141.371669411541,141.478271377669,142.477221691744,143.476172005819,
144.475122319894,145.474072633968,146.473022948043,147.471973262118,147.65485471872),
 .UNSPECIFIED.);
#865=B_SPLINE_CURVE_WITH_KNOTS('',3,(#70241,#70242,#70243,#70244,#70245,
#70246,#70247,#70248,#70249,#70250),.UNSPECIFIED.,.F.,.F.,(4,1,1,1,1,1,
1,4),(141.371669411541,142.169238037598,143.168188351673,144.167138665748,
145.166088979822,146.165039293897,147.163989607972,147.65485471872),
 .UNSPECIFIED.);
#866=B_SPLINE_CURVE_WITH_KNOTS('',3,(#70255,#70256,#70257,#70258,#70259,
#70260,#70261,#70262,#70263,#70264),.UNSPECIFIED.,.F.,.F.,(4,1,1,1,1,1,
1,4),(135.088484104361,135.484569493219,136.483519807294,137.482470121369,
138.481420435444,139.480370749519,140.479321063594,141.371669411541),
 .UNSPECIFIED.);
#867=B_SPLINE_CURVE_WITH_KNOTS('',3,(#70265,#70266,#70267,#70268,#70269,
#70270,#70271,#70272,#70273,#70274,#70275),.UNSPECIFIED.,.F.,.F.,(4,1,1,
1,1,1,1,1,4),(135.088484104361,135.176585839073,136.175536153148,137.174486467223,
138.173436781298,139.172387095373,140.171337409448,141.170287723523,141.371669411541),
 .UNSPECIFIED.);
#868=B_SPLINE_CURVE_WITH_KNOTS('',3,(#70280,#70281,#70282,#70283,#70284,
#70285,#70286,#70287,#70288,#70289),.UNSPECIFIED.,.F.,.F.,(4,1,1,1,1,1,
1,4),(128.805298797182,129.490867608769,130.489817922844,131.488768236919,
132.487718550994,133.486668865069,134.485619179144,135.088484104361),
 .UNSPECIFIED.);
#869=B_SPLINE_CURVE_WITH_KNOTS('',3,(#70290,#70291,#70292,#70293,#70294,
#70295,#70296,#70297,#70298,#70299),.UNSPECIFIED.,.F.,.F.,(4,1,1,1,1,1,
1,4),(128.805298797182,129.182883954623,130.181834268698,131.180784582773,
132.179734896848,133.178685210923,134.177635524998,135.088484104361),
 .UNSPECIFIED.);
#870=B_SPLINE_CURVE_WITH_KNOTS('',3,(#70304,#70305,#70306,#70307,#70308,
#70309,#70310,#70311,#70312,#70313),.UNSPECIFIED.,.F.,.F.,(4,1,1,1,1,1,
1,4),(122.522113490002,123.497165724319,124.496116038394,125.495066352469,
126.494016666544,127.492966980619,128.491917294694,128.805298797182),
 .UNSPECIFIED.);
#871=B_SPLINE_CURVE_WITH_KNOTS('',3,(#70314,#70315,#70316,#70317,#70318,
#70319,#70320,#70321,#70322,#70323),.UNSPECIFIED.,.F.,.F.,(4,1,1,1,1,1,
1,4),(122.522113490002,123.189182070173,124.188132384248,125.187082698323,
126.186033012398,127.184983326473,128.183933640548,128.805298797182),
 .UNSPECIFIED.);
#872=B_SPLINE_CURVE_WITH_KNOTS('',3,(#70328,#70329,#70330,#70331,#70332,
#70333,#70334,#70335,#70336,#70337,#70338),.UNSPECIFIED.,.F.,.F.,(4,1,1,
1,1,1,1,1,4),(116.238928182822,116.504513525795,117.50346383987,118.502414153945,
119.50136446802,120.500314782095,121.49926509617,122.498215410244,122.522113490002),
 .UNSPECIFIED.);
#873=B_SPLINE_CURVE_WITH_KNOTS('',3,(#70339,#70340,#70341,#70342,#70343,
#70344,#70345,#70346,#70347,#70348),.UNSPECIFIED.,.F.,.F.,(4,1,1,1,1,1,
1,4),(116.238928182822,117.195480185724,118.194430499799,119.193380813874,
120.192331127949,121.191281442024,122.190231756098,122.522113490002),
 .UNSPECIFIED.);
#874=B_SPLINE_CURVE_WITH_KNOTS('',3,(#70353,#70354,#70355,#70356,#70357,
#70358,#70359,#70360,#70361,#70362),.UNSPECIFIED.,.F.,.F.,(4,1,1,1,1,1,
1,4),(109.955742875643,110.510811641345,111.50976195542,112.508712269495,
113.50766258357,114.506612897645,115.50556321172,116.238928182822),
 .UNSPECIFIED.);
#875=B_SPLINE_CURVE_WITH_KNOTS('',3,(#70363,#70364,#70365,#70366,#70367,
#70368,#70369,#70370,#70371,#70372,#70373),.UNSPECIFIED.,.F.,.F.,(4,1,1,
1,1,1,1,1,4),(109.955742875643,110.202827987199,111.201778301274,112.200728615349,
113.199678929424,114.198629243499,115.197579557574,116.196529871649,116.238928182822),
 .UNSPECIFIED.);
#876=B_SPLINE_CURVE_WITH_KNOTS('',3,(#70378,#70379,#70380,#70381,#70382,
#70383,#70384,#70385,#70386,#70387),.UNSPECIFIED.,.F.,.F.,(4,1,1,1,1,1,
1,4),(103.672557568463,104.517109756895,105.51606007097,106.515010385045,
107.51396069912,108.512911013195,109.51186132727,109.955742875643),
 .UNSPECIFIED.);
#877=B_SPLINE_CURVE_WITH_KNOTS('',3,(#70388,#70389,#70390,#70391,#70392,
#70393,#70394,#70395,#70396,#70397),.UNSPECIFIED.,.F.,.F.,(4,1,1,1,1,1,
1,4),(103.672557568463,104.209126102749,105.208076416824,106.207026730899,
107.205977044974,108.204927359049,109.203877673124,109.955742875643),
 .UNSPECIFIED.);
#878=B_SPLINE_CURVE_WITH_KNOTS('',3,(#70402,#70403,#70404,#70405,#70406,
#70407,#70408,#70409,#70410,#70411,#70412),.UNSPECIFIED.,.F.,.F.,(4,1,1,
1,1,1,1,1,4),(97.3893722612836,97.5244575583706,98.5234078724455,99.5223581865205,
100.521308500595,101.52025881467,102.519209128745,103.51815944282,103.672557568463),
 .UNSPECIFIED.);
#879=B_SPLINE_CURVE_WITH_KNOTS('',3,(#70413,#70414,#70415,#70416,#70417,
#70418,#70419,#70420,#70421,#70422),.UNSPECIFIED.,.F.,.F.,(4,1,1,1,1,1,
1,4),(97.3893722612836,98.2154242182995,99.2143745323745,100.213324846449,
101.212275160524,102.211225474599,103.210175788674,103.672557568463),
 .UNSPECIFIED.);
#880=B_SPLINE_CURVE_WITH_KNOTS('',3,(#70427,#70428,#70429,#70430,#70431,
#70432,#70433,#70434,#70435,#70436),.UNSPECIFIED.,.F.,.F.,(4,1,1,1,1,1,
1,4),(91.106186954104,91.5307556739208,92.5297059879958,93.5286563020707,
94.5276066161457,95.5265569302206,96.5255072442956,97.3893722612836),
 .UNSPECIFIED.);
#881=B_SPLINE_CURVE_WITH_KNOTS('',3,(#70437,#70438,#70439,#70440,#70441,
#70442,#70443,#70444,#70445,#70446,#70447),.UNSPECIFIED.,.F.,.F.,(4,1,1,
1,1,1,1,1,4),(91.106186954104,91.2227720197748,92.2217223338498,93.2206726479247,
94.2196229619997,95.2185732760747,96.2175235901496,97.2164739042246,97.3893722612836),
 .UNSPECIFIED.);
#882=B_SPLINE_CURVE_WITH_KNOTS('',3,(#70452,#70453,#70454,#70455,#70456,
#70457,#70458,#70459,#70460,#70461),.UNSPECIFIED.,.F.,.F.,(4,1,1,1,1,1,
1,4),(84.8230016469244,85.5370537894711,86.536004103546,87.534954417621,
88.5339047316959,89.5328550457709,90.5318053598459,91.106186954104),
 .UNSPECIFIED.);
#883=B_SPLINE_CURVE_WITH_KNOTS('',3,(#70462,#70463,#70464,#70465,#70466,
#70467,#70468,#70469,#70470,#70471),.UNSPECIFIED.,.F.,.F.,(4,1,1,1,1,1,
1,4),(84.8230016469244,85.2290701353251,86.2280204494,87.226970763475,88.2259210775499,
89.2248713916249,90.2238217056999,91.106186954104),.UNSPECIFIED.);
#884=B_SPLINE_CURVE_WITH_KNOTS('',3,(#70476,#70477,#70478,#70479,#70480,
#70481,#70482,#70483,#70484,#70485,#70486),.UNSPECIFIED.,.F.,.F.,(4,1,1,
1,1,1,1,1,4),(78.5398163397448,78.5444015909464,79.5433519050213,80.5423022190963,
81.5412525331712,82.5402028472462,83.5391531613212,84.5381034753961,84.8230016469244),
 .UNSPECIFIED.);
#885=B_SPLINE_CURVE_WITH_KNOTS('',3,(#70487,#70488,#70489,#70490,#70491,
#70492,#70493,#70494,#70495,#70496),.UNSPECIFIED.,.F.,.F.,(4,1,1,1,1,1,
1,4),(78.5398163397448,79.2353682508753,80.2343185649503,81.2332688790252,
82.2322191931002,83.2311695071752,84.2301198212501,84.8230016469244),
 .UNSPECIFIED.);
#886=B_SPLINE_CURVE_WITH_KNOTS('',3,(#70501,#70502,#70503,#70504,#70505,
#70506,#70507,#70508,#70509,#70510),.UNSPECIFIED.,.F.,.F.,(4,1,1,1,1,1,
1,4),(72.2566310325653,72.5506997064966,73.5496500205716,74.5486003346466,
75.5475506487215,76.5465009627965,77.5454512768714,78.5398163397448),
 .UNSPECIFIED.);
#887=B_SPLINE_CURVE_WITH_KNOTS('',3,(#70511,#70512,#70513,#70514,#70515,
#70516,#70517,#70518,#70519,#70520),.UNSPECIFIED.,.F.,.F.,(4,1,1,1,1,1,
1,4),(72.2566310325653,73.2416663664256,74.2406166805006,75.2395669945755,
76.2385173086505,77.2374676227254,78.2364179368004,78.5398163397448),
 .UNSPECIFIED.);
#888=B_SPLINE_CURVE_WITH_KNOTS('',3,(#70525,#70526,#70527,#70528,#70529,
#70530,#70531,#70532,#70533,#70534),.UNSPECIFIED.,.F.,.F.,(4,1,1,1,1,1,
1,4),(65.9734457253856,66.5569978220469,67.5559481361219,68.5548984501968,
69.5538487642718,70.5527990783467,71.5517493924217,72.2566310325653),
 .UNSPECIFIED.);
#889=B_SPLINE_CURVE_WITH_KNOTS('',3,(#70535,#70536,#70537,#70538,#70539,
#70540,#70541,#70542,#70543,#70544,#70545),.UNSPECIFIED.,.F.,.F.,(4,1,1,
1,1,1,1,1,4),(65.9734457253856,66.2490141679009,67.2479644819759,68.2469147960508,
69.2458651101258,70.2448154242007,71.2437657382757,72.2427160523506,72.2566310325653),
 .UNSPECIFIED.);
#890=B_SPLINE_CURVE_WITH_KNOTS('',3,(#70550,#70551,#70552,#70553,#70554,
#70555,#70556,#70557,#70558,#70559),.UNSPECIFIED.,.F.,.F.,(4,1,1,1,1,1,
1,4),(59.6902604182061,60.5632959375972,61.5622462516721,62.5611965657471,
63.560146879822,64.559097193897,65.5580475079719,65.9734457253856),
 .UNSPECIFIED.);
#891=B_SPLINE_CURVE_WITH_KNOTS('',3,(#70560,#70561,#70562,#70563,#70564,
#70565,#70566,#70567,#70568,#70569),.UNSPECIFIED.,.F.,.F.,(4,1,1,1,1,1,
1,4),(59.6902604182061,60.2553122834511,61.2542625975261,62.2532129116011,
63.252163225676,64.251113539751,65.2500638538259,65.9734457253856),
 .UNSPECIFIED.);
#892=B_SPLINE_CURVE_WITH_KNOTS('',3,(#70574,#70575,#70576,#70577,#70578,
#70579,#70580,#70581,#70582,#70583,#70584),.UNSPECIFIED.,.F.,.F.,(4,1,1,
1,1,1,1,1,4),(53.4070751110265,53.5706437390725,54.5695940531474,55.5685443672224,
56.5674946812973,57.5664449953723,58.5653953094472,59.5643456235222,59.6902604182061),
 .UNSPECIFIED.);
#893=B_SPLINE_CURVE_WITH_KNOTS('',3,(#70585,#70586,#70587,#70588,#70589,
#70590,#70591,#70592,#70593,#70594),.UNSPECIFIED.,.F.,.F.,(4,1,1,1,1,1,
1,4),(53.4070751110265,54.2616103990014,55.2605607130764,56.2595110271513,
57.2584613412263,58.2574116553012,59.2563619693762,59.6902604182061),
 .UNSPECIFIED.);
#894=B_SPLINE_CURVE_WITH_KNOTS('',3,(#70599,#70600,#70601,#70602,#70603,
#70604,#70605,#70606,#70607,#70608),.UNSPECIFIED.,.F.,.F.,(4,1,1,1,1,1,
1,4),(47.1238898038469,47.5769418546227,48.5758921686977,49.5748424827726,
50.5737927968476,51.5727431109225,52.5716934249975,53.4070751110265),
 .UNSPECIFIED.);
#895=B_SPLINE_CURVE_WITH_KNOTS('',3,(#70609,#70610,#70611,#70612,#70613,
#70614,#70615,#70616,#70617,#70618,#70619),.UNSPECIFIED.,.F.,.F.,(4,1,1,
1,1,1,1,1,4),(47.1238898038469,47.2689582004767,48.2679085145517,49.2668588286266,
50.2658091427016,51.2647594567765,52.2637097708515,53.2626600849265,53.4070751110265),
 .UNSPECIFIED.);
#896=B_SPLINE_CURVE_WITH_KNOTS('',3,(#70624,#70625,#70626,#70627,#70628,
#70629,#70630,#70631,#70632,#70633),.UNSPECIFIED.,.F.,.F.,(4,1,1,1,1,1,
1,4),(40.8407044966673,41.583239970173,42.5821902842479,43.5811405983229,
44.5800909123978,45.5790412264728,46.5779915405478,47.1238898038469),
 .UNSPECIFIED.);
#897=B_SPLINE_CURVE_WITH_KNOTS('',3,(#70634,#70635,#70636,#70637,#70638,
#70639,#70640,#70641,#70642,#70643),.UNSPECIFIED.,.F.,.F.,(4,1,1,1,1,1,
1,4),(40.8407044966673,41.275256316027,42.2742066301019,43.2731569441769,
44.2721072582518,45.2710575723268,46.2700078864018,47.1238898038469),
 .UNSPECIFIED.);
#898=B_SPLINE_CURVE_WITH_KNOTS('',3,(#70648,#70649,#70650,#70651,#70652,
#70653,#70654,#70655,#70656,#70657,#70658),.UNSPECIFIED.,.F.,.F.,(4,1,1,
1,1,1,1,1,4),(34.5575191894877,34.5905877716483,35.5895380857232,36.5884883997982,
37.5874387138731,38.5863890279481,39.5853393420231,40.584289656098,40.8407044966673),
 .UNSPECIFIED.);
#899=B_SPLINE_CURVE_WITH_KNOTS('',3,(#70659,#70660,#70661,#70662,#70663,
#70664,#70665,#70666,#70667,#70668),.UNSPECIFIED.,.F.,.F.,(4,1,1,1,1,1,
1,4),(34.5575191894877,35.2815544315772,36.2805047456522,37.2794550597271,
38.2784053738021,39.2773556878771,40.276306001952,40.8407044966673),
 .UNSPECIFIED.);
#900=B_SPLINE_CURVE_WITH_KNOTS('',3,(#70673,#70674,#70675,#70676,#70677,
#70678,#70679,#70680,#70681,#70682),.UNSPECIFIED.,.F.,.F.,(4,1,1,1,1,1,
1,4),(28.2743338823081,28.5968858871985,29.5958362012735,30.5947865153485,
31.5937368294234,32.5926871434984,33.5916374575733,34.5575191894877),
 .UNSPECIFIED.);
#901=B_SPLINE_CURVE_WITH_KNOTS('',3,(#70683,#70684,#70685,#70686,#70687,
#70688,#70689,#70690,#70691,#70692,#70693),.UNSPECIFIED.,.F.,.F.,(4,1,1,
1,1,1,1,1,4),(28.2743338823081,28.2889022330525,29.2878525471275,30.2868028612024,
31.2857531752774,32.2847034893524,33.2836538034273,34.2826041175023,34.5575191894877),
 .UNSPECIFIED.);
#902=B_SPLINE_CURVE_WITH_KNOTS('',3,(#70698,#70699,#70700,#70701,#70702,
#70703,#70704,#70705,#70706,#70707),.UNSPECIFIED.,.F.,.F.,(4,1,1,1,1,1,
1,4),(21.9911485751285,22.6031840027488,23.6021343168238,24.6010846308987,
25.6000349449737,26.5989852590486,27.5979355731236,28.2743338823081),
 .UNSPECIFIED.);
#903=B_SPLINE_CURVE_WITH_KNOTS('',3,(#70708,#70709,#70710,#70711,#70712,
#70713,#70714,#70715,#70716,#70717),.UNSPECIFIED.,.F.,.F.,(4,1,1,1,1,1,
1,4),(21.9911485751285,22.2952003486028,23.2941506626778,24.2931009767527,
25.2920512908277,26.2910016049026,27.2899519189776,28.2743338823081),
 .UNSPECIFIED.);
#904=B_SPLINE_CURVE_WITH_KNOTS('',3,(#70722,#70723,#70724,#70725,#70726,
#70727,#70728,#70729,#70730,#70731),.UNSPECIFIED.,.F.,.F.,(4,1,1,1,1,1,
1,4),(15.7079632679489,16.6094821182991,17.608432432374,18.607382746449,
19.6063330605239,20.6052833745989,21.6042336886738,21.9911485751285),
 .UNSPECIFIED.);
#905=B_SPLINE_CURVE_WITH_KNOTS('',3,(#70732,#70733,#70734,#70735,#70736,
#70737,#70738,#70739,#70740,#70741),.UNSPECIFIED.,.F.,.F.,(4,1,1,1,1,1,
1,4),(15.7079632679489,16.3014984641531,17.300448778228,18.299399092303,
19.2983494063779,20.2972997204529,21.2962500345278,21.9911485751285),
 .UNSPECIFIED.);
#906=B_SPLINE_CURVE_WITH_KNOTS('',3,(#70744,#70745,#70746,#70747,#70748,
#70749,#70750,#70751,#70752,#70753,#70754,#70755,#70756,#70757,#70758,#70759,
#70760,#70761,#70762,#70763,#70764,#70765,#70766,#70767,#70768,#70769,#70770,
#70771,#70772,#70773,#70774,#70775,#70776,#70777,#70778,#70779,#70780,#70781,
#70782,#70783,#70784,#70785,#70786,#70787,#70788,#70789,#70790,#70791,#70792,
#70793,#70794,#70795,#70796,#70797,#70798,#70799,#70800,#70801,#70802,#70803,
#70804,#70805,#70806,#70807,#70808,#70809,#70810),.UNSPECIFIED.,.F.,.F.,
(4,3,3,3,3,3,3,3,3,3,3,3,3,3,3,3,3,3,3,3,3,3,4),(-0.937740963081735,-0.909444112452461,
-0.855149209379619,-0.831654357878427,-0.809449311278671,-0.761645733327119,
-0.730551867932484,-0.705074189312176,-0.633394121071644,-0.589005347555876,
-0.552912288548607,-0.535870541484316,-0.475136415046823,-0.416990908171079,
-0.376787680507578,-0.359453625478781,-0.285000662182822,-0.242554387543848,
-0.201877636725584,-0.176408609773167,-0.0995863267715526,-0.0229337643123042,
0.),.UNSPECIFIED.);
#907=B_SPLINE_CURVE_WITH_KNOTS('',3,(#70815,#70816,#70817,#70818,#70819,
#70820,#70821,#70822,#70823,#70824,#70825,#70826,#70827,#70828,#70829,#70830,
#70831,#70832,#70833,#70834,#70835,#70836,#70837,#70838,#70839,#70840,#70841,
#70842,#70843,#70844,#70845,#70846,#70847,#70848,#70849,#70850,#70851,#70852,
#70853,#70854,#70855,#70856,#70857,#70858,#70859,#70860,#70861,#70862,#70863,
#70864,#70865,#70866,#70867,#70868,#70869,#70870,#70871,#70872,#70873,#70874,
#70875,#70876,#70877,#70878,#70879,#70880,#70881),.UNSPECIFIED.,.F.,.F.,
(4,3,3,3,3,3,3,3,3,3,3,3,3,3,3,3,3,3,3,3,3,3,4),(-0.933975894023042,-0.900245581901252,
-0.841487335486281,-0.810148385431822,-0.789962965850525,-0.713494202946813,
-0.685815600115485,-0.669124534079921,-0.594769089731299,-0.522304386990161,
-0.504106714065163,-0.485285714178158,-0.430179610581482,-0.367158525801107,
-0.338157301636647,-0.316837385332554,-0.246631602421699,-0.209998276425139,
-0.170573737200308,-0.149754029067211,-0.0814335283124309,-0.0148091980626577,
0.),.UNSPECIFIED.);
#908=B_SPLINE_CURVE_WITH_KNOTS('',3,(#71486,#71487,#71488,#71489,#71490,
#71491,#71492,#71493,#71494,#71495,#71496,#71497,#71498,#71499,#71500,#71501),
 .UNSPECIFIED.,.F.,.F.,(4,3,3,3,3,4),(139.344958767167,139.853043970494,
140.851994284569,141.850944598644,142.849894912719,143.780223779293),
 .UNSPECIFIED.);
#909=B_SPLINE_CURVE_WITH_KNOTS('',3,(#71503,#71504,#71505,#71506,#71507,
#71508,#71509,#71510,#71511,#71512,#71513,#71514,#71515,#71516,#71517,#71518,
#71519,#71520,#71521,#71522,#71523,#71524,#71525,#71526,#71527,#71528,#71529,
#71530,#71531,#71532,#71533,#71534,#71535,#71536,#71537,#71538,#71539,#71540,
#71541,#71542,#71543,#71544,#71545,#71546,#71547,#71548,#71549,#71550,#71551,
#71552,#71553,#71554,#71555,#71556,#71557,#71558,#71559,#71560,#71561,#71562,
#71563,#71564,#71565,#71566,#71567,#71568,#71569),.UNSPECIFIED.,.F.,.F.,
(4,3,3,3,3,3,3,3,3,3,3,3,3,3,3,3,3,3,3,3,3,3,4),(-0.937740963081788,-0.9094441124525,
-0.855149214466471,-0.831654450328588,-0.809449338817702,-0.761644037980892,
-0.730548230053358,-0.705074381737659,-0.633394334161421,-0.589005671228396,
-0.552912642218538,-0.535870789585526,-0.475136415046854,-0.416990908171107,
-0.37678761967171,-0.359453594967343,-0.285000689052183,-0.242554387543867,
-0.201877627854406,-0.176408608557775,-0.099585852352597,-0.0229334512306372,
0.),.UNSPECIFIED.);
#910=B_SPLINE_CURVE_WITH_KNOTS('',3,(#71570,#71571,#71572,#71573,#71574,
#71575,#71576,#71577,#71578),.UNSPECIFIED.,.F.,.F.,(4,1,1,1,1,1,4),(10.3764180272042,
11.3067468937783,12.3056972078532,13.3046475219282,14.3035978360031,15.3025481500781,
15.7079632679489),.UNSPECIFIED.);
#911=B_SPLINE_CURVE_WITH_KNOTS('',3,(#71584,#71585,#71586,#71587,#71588,
#71589,#71590,#71591,#71592,#71593,#71594,#71595,#71596,#71597,#71598,#71599,
#71600,#71601,#71602,#71603,#71604,#71605,#71606,#71607,#71608,#71609,#71610,
#71611,#71612,#71613,#71614,#71615,#71616,#71617,#71618,#71619,#71620,#71621,
#71622,#71623,#71624,#71625,#71626,#71627,#71628,#71629,#71630,#71631,#71632,
#71633,#71634,#71635,#71636,#71637,#71638,#71639,#71640,#71641,#71642,#71643,
#71644,#71645,#71646,#71647,#71648,#71649,#71650),.UNSPECIFIED.,.F.,.F.,
(4,3,3,3,3,3,3,3,3,3,3,3,3,3,3,3,3,3,3,3,3,3,4),(-0.933975894023119,-0.900245581901347,
-0.841487335486366,-0.81014833836286,-0.789962871427875,-0.713494038275052,
-0.685815425544487,-0.669124316437155,-0.594768735347489,-0.522303851190798,
-0.504103096333425,-0.48528515314046,-0.430179610581495,-0.367160405393276,
-0.338159869684524,-0.316837865674906,-0.246632351097073,-0.209998276425132,
-0.170573792092408,-0.149754039276966,-0.0814335090852424,-0.0148090667643755,
0.),.UNSPECIFIED.);
#912=B_SPLINE_CURVE_WITH_KNOTS('',3,(#71653,#71654,#71655,#71656,#71657,
#71658,#71659,#71660,#71661),.UNSPECIFIED.,.F.,.F.,(4,1,1,1,1,1,4),(11.6147305479243,
12.1142057049618,12.6136808619992,13.6126311760742,14.6115814901491,15.6105318042241,
15.7079632679489),.UNSPECIFIED.);
#913=B_SPLINE_CURVE_WITH_KNOTS('',3,(#72266,#72267,#72268,#72269,#72270,
#72271,#72272,#72273,#72274,#72275,#72276,#72277,#72278,#72279,#72280,#72281),
 .UNSPECIFIED.,.F.,.F.,(4,3,3,3,3,4),(-145.846745854944,-145.347270697906,
-144.847795540869,-143.848845226794,-142.849894912719,-142.323309477976),
 .UNSPECIFIED.);
#1017=SHAPE_REPRESENTATION_RELATIONSHIP('SRR','None',#76754,#1037);
#1037=ADVANCED_BREP_SHAPE_REPRESENTATION('',(#1077),#76658);
#1057=STYLED_ITEM('',(#76913),#1077);
#1077=MANIFOLD_SOLID_BREP('Socket head screw',#26682);
#1087=TOROIDAL_SURFACE('',#28689,0.5175,0.025);
#1462=CYLINDRICAL_SURFACE('',#28633,0.4925);
#1463=CYLINDRICAL_SURFACE('',#28635,0.4925);
#1464=CYLINDRICAL_SURFACE('',#28636,0.4925);
#1465=CYLINDRICAL_SURFACE('',#28637,0.4925);
#1466=CYLINDRICAL_SURFACE('',#28638,0.4925);
#1467=CYLINDRICAL_SURFACE('',#28639,0.4925);
#1468=CYLINDRICAL_SURFACE('',#28640,0.4925);
#1469=CYLINDRICAL_SURFACE('',#28641,0.4925);
#1470=CYLINDRICAL_SURFACE('',#28642,0.4925);
#1471=CYLINDRICAL_SURFACE('',#28643,0.4925);
#1472=CYLINDRICAL_SURFACE('',#28644,0.4925);
#1473=CYLINDRICAL_SURFACE('',#28645,0.4925);
#1474=CYLINDRICAL_SURFACE('',#28646,0.4925);
#1475=CYLINDRICAL_SURFACE('',#28647,0.4925);
#1476=CYLINDRICAL_SURFACE('',#28648,0.4925);
#1477=CYLINDRICAL_SURFACE('',#28649,0.4925);
#1478=CYLINDRICAL_SURFACE('',#28650,0.4925);
#1479=CYLINDRICAL_SURFACE('',#28651,0.4925);
#1480=CYLINDRICAL_SURFACE('',#28652,0.4925);
#1481=CYLINDRICAL_SURFACE('',#28653,0.4925);
#1482=CYLINDRICAL_SURFACE('',#28654,0.4925);
#1483=CYLINDRICAL_SURFACE('',#28655,0.4925);
#1484=CYLINDRICAL_SURFACE('',#28656,0.4925);
#1485=CYLINDRICAL_SURFACE('',#28657,0.40705);
#1486=CYLINDRICAL_SURFACE('',#28659,0.40705);
#1487=CYLINDRICAL_SURFACE('',#28660,0.40705);
#1488=CYLINDRICAL_SURFACE('',#28661,0.40705);
#1489=CYLINDRICAL_SURFACE('',#28662,0.40705);
#1490=CYLINDRICAL_SURFACE('',#28663,0.40705);
#1491=CYLINDRICAL_SURFACE('',#28664,0.40705);
#1492=CYLINDRICAL_SURFACE('',#28665,0.40705);
#1493=CYLINDRICAL_SURFACE('',#28666,0.40705);
#1494=CYLINDRICAL_SURFACE('',#28667,0.40705);
#1495=CYLINDRICAL_SURFACE('',#28668,0.40705);
#1496=CYLINDRICAL_SURFACE('',#28669,0.40705);
#1497=CYLINDRICAL_SURFACE('',#28670,0.40705);
#1498=CYLINDRICAL_SURFACE('',#28671,0.40705);
#1499=CYLINDRICAL_SURFACE('',#28672,0.40705);
#1500=CYLINDRICAL_SURFACE('',#28673,0.40705);
#1501=CYLINDRICAL_SURFACE('',#28674,0.40705);
#1502=CYLINDRICAL_SURFACE('',#28675,0.40705);
#1503=CYLINDRICAL_SURFACE('',#28676,0.40705);
#1504=CYLINDRICAL_SURFACE('',#28677,0.40705);
#1505=CYLINDRICAL_SURFACE('',#28678,0.40705);
#1506=CYLINDRICAL_SURFACE('',#28679,0.40705);
#1507=CYLINDRICAL_SURFACE('',#28680,0.40705);
#1508=CYLINDRICAL_SURFACE('',#28688,0.40705);
#1509=CYLINDRICAL_SURFACE('',#28693,0.4925);
#1510=CYLINDRICAL_SURFACE('',#28938,0.8);
#1652=FACE_BOUND('',#5354,.T.);
#1653=FACE_BOUND('',#5518,.T.);
#2202=PLANE('',#28681);
#2203=PLANE('',#28684);
#2204=PLANE('',#28694);
#2205=PLANE('',#28696);
#2206=PLANE('',#28698);
#2207=PLANE('',#28700);
#2208=PLANE('',#28702);
#2209=PLANE('',#28704);
#2210=PLANE('',#28706);
#2211=PLANE('',#28709);
#2212=PLANE('',#28710);
#2213=PLANE('',#28711);
#2214=PLANE('',#28712);
#2215=PLANE('',#28713);
#2216=PLANE('',#28714);
#2217=PLANE('',#28715);
#2218=PLANE('',#28716);
#2219=PLANE('',#28718);
#2220=PLANE('',#28719);
#2221=PLANE('',#28721);
#2222=PLANE('',#28722);
#2223=PLANE('',#28724);
#2224=PLANE('',#28725);
#2225=PLANE('',#28727);
#2226=PLANE('',#28728);
#2227=PLANE('',#28730);
#2228=PLANE('',#28731);
#2229=PLANE('',#28733);
#2230=PLANE('',#28734);
#2231=PLANE('',#28736);
#2232=PLANE('',#28737);
#2233=PLANE('',#28739);
#2234=PLANE('',#28740);
#2235=PLANE('',#28742);
#2236=PLANE('',#28743);
#2237=PLANE('',#28745);
#2238=PLANE('',#28746);
#2239=PLANE('',#28748);
#2240=PLANE('',#28749);
#2241=PLANE('',#28751);
#2242=PLANE('',#28752);
#2243=PLANE('',#28754);
#2244=PLANE('',#28755);
#2245=PLANE('',#28757);
#2246=PLANE('',#28758);
#2247=PLANE('',#28760);
#2248=PLANE('',#28761);
#2249=PLANE('',#28763);
#2250=PLANE('',#28764);
#2251=PLANE('',#28767);
#2252=PLANE('',#28768);
#2253=PLANE('',#28771);
#2254=PLANE('',#28772);
#2255=PLANE('',#28774);
#2256=PLANE('',#28775);
#2257=PLANE('',#28777);
#2258=PLANE('',#28778);
#2259=PLANE('',#28780);
#2260=PLANE('',#28781);
#2261=PLANE('',#28783);
#2262=PLANE('',#28784);
#2263=PLANE('',#28786);
#2264=PLANE('',#28787);
#2265=PLANE('',#28789);
#2266=PLANE('',#28790);
#2267=PLANE('',#28792);
#2268=PLANE('',#28793);
#2269=PLANE('',#28795);
#2270=PLANE('',#28796);
#2271=PLANE('',#28798);
#2272=PLANE('',#28799);
#2273=PLANE('',#28801);
#2274=PLANE('',#28802);
#2275=PLANE('',#28804);
#2276=PLANE('',#28805);
#2277=PLANE('',#28807);
#2278=PLANE('',#28808);
#2279=PLANE('',#28810);
#2280=PLANE('',#28811);
#2281=PLANE('',#28813);
#2282=PLANE('',#28814);
#2283=PLANE('',#28816);
#2284=PLANE('',#28817);
#2285=PLANE('',#28819);
#2286=PLANE('',#28820);
#2287=PLANE('',#28822);
#2288=PLANE('',#28823);
#2289=PLANE('',#28825);
#2290=PLANE('',#28826);
#2291=PLANE('',#28828);
#2292=PLANE('',#28829);
#2293=PLANE('',#28831);
#2294=PLANE('',#28832);
#2295=PLANE('',#28834);
#2296=PLANE('',#28835);
#2297=PLANE('',#28837);
#2298=PLANE('',#28838);
#2299=PLANE('',#28840);
#2300=PLANE('',#28841);
#2301=PLANE('',#28843);
#2302=PLANE('',#28844);
#2303=PLANE('',#28846);
#2304=PLANE('',#28847);
#2305=PLANE('',#28849);
#2306=PLANE('',#28850);
#2307=PLANE('',#28852);
#2308=PLANE('',#28853);
#2309=PLANE('',#28855);
#2310=PLANE('',#28856);
#2311=PLANE('',#28858);
#2312=PLANE('',#28859);
#2313=PLANE('',#28861);
#2314=PLANE('',#28862);
#2315=PLANE('',#28864);
#2316=PLANE('',#28865);
#2317=PLANE('',#28867);
#2318=PLANE('',#28868);
#2319=PLANE('',#28870);
#2320=PLANE('',#28871);
#2321=PLANE('',#28873);
#2322=PLANE('',#28875);
#2323=PLANE('',#28876);
#2324=PLANE('',#28877);
#2325=PLANE('',#28879);
#2326=PLANE('',#28880);
#2327=PLANE('',#28882);
#2328=PLANE('',#28883);
#2329=PLANE('',#28885);
#2330=PLANE('',#28886);
#2331=PLANE('',#28888);
#2332=PLANE('',#28889);
#2333=PLANE('',#28891);
#2334=PLANE('',#28892);
#2335=PLANE('',#28894);
#2336=PLANE('',#28895);
#2337=PLANE('',#28897);
#2338=PLANE('',#28898);
#2339=PLANE('',#28900);
#2340=PLANE('',#28901);
#2341=PLANE('',#28903);
#2342=PLANE('',#28904);
#2343=PLANE('',#28906);
#2344=PLANE('',#28907);
#2345=PLANE('',#28909);
#2346=PLANE('',#28910);
#2347=PLANE('',#28912);
#2348=PLANE('',#28913);
#2349=PLANE('',#28915);
#2350=PLANE('',#28916);
#2351=PLANE('',#28918);
#2352=PLANE('',#28919);
#2353=PLANE('',#28921);
#2354=PLANE('',#28922);
#2355=PLANE('',#28924);
#2356=PLANE('',#28925);
#2357=PLANE('',#28927);
#2358=PLANE('',#28928);
#2359=PLANE('',#28930);
#2360=PLANE('',#28931);
#2361=PLANE('',#28933);
#2362=PLANE('',#28977);
#3649=FACE_OUTER_BOUND('',#5300,.T.);
#3650=FACE_OUTER_BOUND('',#5301,.T.);
#3651=FACE_OUTER_BOUND('',#5302,.T.);
#3652=FACE_OUTER_BOUND('',#5303,.T.);
#3653=FACE_OUTER_BOUND('',#5304,.T.);
#3654=FACE_OUTER_BOUND('',#5305,.T.);
#3655=FACE_OUTER_BOUND('',#5306,.T.);
#3656=FACE_OUTER_BOUND('',#5307,.T.);
#3657=FACE_OUTER_BOUND('',#5308,.T.);
#3658=FACE_OUTER_BOUND('',#5309,.T.);
#3659=FACE_OUTER_BOUND('',#5310,.T.);
#3660=FACE_OUTER_BOUND('',#5311,.T.);
#3661=FACE_OUTER_BOUND('',#5312,.T.);
#3662=FACE_OUTER_BOUND('',#5313,.T.);
#3663=FACE_OUTER_BOUND('',#5314,.T.);
#3664=FACE_OUTER_BOUND('',#5315,.T.);
#3665=FACE_OUTER_BOUND('',#5316,.T.);
#3666=FACE_OUTER_BOUND('',#5317,.T.);
#3667=FACE_OUTER_BOUND('',#5318,.T.);
#3668=FACE_OUTER_BOUND('',#5319,.T.);
#3669=FACE_OUTER_BOUND('',#5320,.T.);
#3670=FACE_OUTER_BOUND('',#5321,.T.);
#3671=FACE_OUTER_BOUND('',#5322,.T.);
#3672=FACE_OUTER_BOUND('',#5323,.T.);
#3673=FACE_OUTER_BOUND('',#5324,.T.);
#3674=FACE_OUTER_BOUND('',#5325,.T.);
#3675=FACE_OUTER_BOUND('',#5326,.T.);
#3676=FACE_OUTER_BOUND('',#5327,.T.);
#3677=FACE_OUTER_BOUND('',#5328,.T.);
#3678=FACE_OUTER_BOUND('',#5329,.T.);
#3679=FACE_OUTER_BOUND('',#5330,.T.);
#3680=FACE_OUTER_BOUND('',#5331,.T.);
#3681=FACE_OUTER_BOUND('',#5332,.T.);
#3682=FACE_OUTER_BOUND('',#5333,.T.);
#3683=FACE_OUTER_BOUND('',#5334,.T.);
#3684=FACE_OUTER_BOUND('',#5335,.T.);
#3685=FACE_OUTER_BOUND('',#5336,.T.);
#3686=FACE_OUTER_BOUND('',#5337,.T.);
#3687=FACE_OUTER_BOUND('',#5338,.T.);
#3688=FACE_OUTER_BOUND('',#5339,.T.);
#3689=FACE_OUTER_BOUND('',#5340,.T.);
#3690=FACE_OUTER_BOUND('',#5341,.T.);
#3691=FACE_OUTER_BOUND('',#5342,.T.);
#3692=FACE_OUTER_BOUND('',#5343,.T.);
#3693=FACE_OUTER_BOUND('',#5344,.T.);
#3694=FACE_OUTER_BOUND('',#5345,.T.);
#3695=FACE_OUTER_BOUND('',#5346,.T.);
#3696=FACE_OUTER_BOUND('',#5347,.T.);
#3697=FACE_OUTER_BOUND('',#5348,.T.);
#3698=FACE_OUTER_BOUND('',#5349,.T.);
#3699=FACE_OUTER_BOUND('',#5350,.T.);
#3700=FACE_OUTER_BOUND('',#5351,.T.);
#3701=FACE_OUTER_BOUND('',#5352,.T.);
#3702=FACE_OUTER_BOUND('',#5353,.T.);
#3703=FACE_OUTER_BOUND('',#5355,.T.);
#3704=FACE_OUTER_BOUND('',#5356,.T.);
#3705=FACE_OUTER_BOUND('',#5357,.T.);
#3706=FACE_OUTER_BOUND('',#5358,.T.);
#3707=FACE_OUTER_BOUND('',#5359,.T.);
#3708=FACE_OUTER_BOUND('',#5360,.T.);
#3709=FACE_OUTER_BOUND('',#5361,.T.);
#3710=FACE_OUTER_BOUND('',#5362,.T.);
#3711=FACE_OUTER_BOUND('',#5363,.T.);
#3712=FACE_OUTER_BOUND('',#5364,.T.);
#3713=FACE_OUTER_BOUND('',#5365,.T.);
#3714=FACE_OUTER_BOUND('',#5366,.T.);
#3715=FACE_OUTER_BOUND('',#5367,.T.);
#3716=FACE_OUTER_BOUND('',#5368,.T.);
#3717=FACE_OUTER_BOUND('',#5369,.T.);
#3718=FACE_OUTER_BOUND('',#5370,.T.);
#3719=FACE_OUTER_BOUND('',#5371,.T.);
#3720=FACE_OUTER_BOUND('',#5372,.T.);
#3721=FACE_OUTER_BOUND('',#5373,.T.);
#3722=FACE_OUTER_BOUND('',#5374,.T.);
#3723=FACE_OUTER_BOUND('',#5375,.T.);
#3724=FACE_OUTER_BOUND('',#5376,.T.);
#3725=FACE_OUTER_BOUND('',#5377,.T.);
#3726=FACE_OUTER_BOUND('',#5378,.T.);
#3727=FACE_OUTER_BOUND('',#5379,.T.);
#3728=FACE_OUTER_BOUND('',#5380,.T.);
#3729=FACE_OUTER_BOUND('',#5381,.T.);
#3730=FACE_OUTER_BOUND('',#5382,.T.);
#3731=FACE_OUTER_BOUND('',#5383,.T.);
#3732=FACE_OUTER_BOUND('',#5384,.T.);
#3733=FACE_OUTER_BOUND('',#5385,.T.);
#3734=FACE_OUTER_BOUND('',#5386,.T.);
#3735=FACE_OUTER_BOUND('',#5387,.T.);
#3736=FACE_OUTER_BOUND('',#5388,.T.);
#3737=FACE_OUTER_BOUND('',#5389,.T.);
#3738=FACE_OUTER_BOUND('',#5390,.T.);
#3739=FACE_OUTER_BOUND('',#5391,.T.);
#3740=FACE_OUTER_BOUND('',#5392,.T.);
#3741=FACE_OUTER_BOUND('',#5393,.T.);
#3742=FACE_OUTER_BOUND('',#5394,.T.);
#3743=FACE_OUTER_BOUND('',#5395,.T.);
#3744=FACE_OUTER_BOUND('',#5396,.T.);
#3745=FACE_OUTER_BOUND('',#5397,.T.);
#3746=FACE_OUTER_BOUND('',#5398,.T.);
#3747=FACE_OUTER_BOUND('',#5399,.T.);
#3748=FACE_OUTER_BOUND('',#5400,.T.);
#3749=FACE_OUTER_BOUND('',#5401,.T.);
#3750=FACE_OUTER_BOUND('',#5402,.T.);
#3751=FACE_OUTER_BOUND('',#5403,.T.);
#3752=FACE_OUTER_BOUND('',#5404,.T.);
#3753=FACE_OUTER_BOUND('',#5405,.T.);
#3754=FACE_OUTER_BOUND('',#5406,.T.);
#3755=FACE_OUTER_BOUND('',#5407,.T.);
#3756=FACE_OUTER_BOUND('',#5408,.T.);
#3757=FACE_OUTER_BOUND('',#5409,.T.);
#3758=FACE_OUTER_BOUND('',#5410,.T.);
#3759=FACE_OUTER_BOUND('',#5411,.T.);
#3760=FACE_OUTER_BOUND('',#5412,.T.);
#3761=FACE_OUTER_BOUND('',#5413,.T.);
#3762=FACE_OUTER_BOUND('',#5414,.T.);
#3763=FACE_OUTER_BOUND('',#5415,.T.);
#3764=FACE_OUTER_BOUND('',#5416,.T.);
#3765=FACE_OUTER_BOUND('',#5417,.T.);
#3766=FACE_OUTER_BOUND('',#5418,.T.);
#3767=FACE_OUTER_BOUND('',#5419,.T.);
#3768=FACE_OUTER_BOUND('',#5420,.T.);
#3769=FACE_OUTER_BOUND('',#5421,.T.);
#3770=FACE_OUTER_BOUND('',#5422,.T.);
#3771=FACE_OUTER_BOUND('',#5423,.T.);
#3772=FACE_OUTER_BOUND('',#5424,.T.);
#3773=FACE_OUTER_BOUND('',#5425,.T.);
#3774=FACE_OUTER_BOUND('',#5426,.T.);
#3775=FACE_OUTER_BOUND('',#5427,.T.);
#3776=FACE_OUTER_BOUND('',#5428,.T.);
#3777=FACE_OUTER_BOUND('',#5429,.T.);
#3778=FACE_OUTER_BOUND('',#5430,.T.);
#3779=FACE_OUTER_BOUND('',#5431,.T.);
#3780=FACE_OUTER_BOUND('',#5432,.T.);
#3781=FACE_OUTER_BOUND('',#5433,.T.);
#3782=FACE_OUTER_BOUND('',#5434,.T.);
#3783=FACE_OUTER_BOUND('',#5435,.T.);
#3784=FACE_OUTER_BOUND('',#5436,.T.);
#3785=FACE_OUTER_BOUND('',#5437,.T.);
#3786=FACE_OUTER_BOUND('',#5438,.T.);
#3787=FACE_OUTER_BOUND('',#5439,.T.);
#3788=FACE_OUTER_BOUND('',#5440,.T.);
#3789=FACE_OUTER_BOUND('',#5441,.T.);
#3790=FACE_OUTER_BOUND('',#5442,.T.);
#3791=FACE_OUTER_BOUND('',#5443,.T.);
#3792=FACE_OUTER_BOUND('',#5444,.T.);
#3793=FACE_OUTER_BOUND('',#5445,.T.);
#3794=FACE_OUTER_BOUND('',#5446,.T.);
#3795=FACE_OUTER_BOUND('',#5447,.T.);
#3796=FACE_OUTER_BOUND('',#5448,.T.);
#3797=FACE_OUTER_BOUND('',#5449,.T.);
#3798=FACE_OUTER_BOUND('',#5450,.T.);
#3799=FACE_OUTER_BOUND('',#5451,.T.);
#3800=FACE_OUTER_BOUND('',#5452,.T.);
#3801=FACE_OUTER_BOUND('',#5453,.T.);
#3802=FACE_OUTER_BOUND('',#5454,.T.);
#3803=FACE_OUTER_BOUND('',#5455,.T.);
#3804=FACE_OUTER_BOUND('',#5456,.T.);
#3805=FACE_OUTER_BOUND('',#5457,.T.);
#3806=FACE_OUTER_BOUND('',#5458,.T.);
#3807=FACE_OUTER_BOUND('',#5459,.T.);
#3808=FACE_OUTER_BOUND('',#5460,.T.);
#3809=FACE_OUTER_BOUND('',#5461,.T.);
#3810=FACE_OUTER_BOUND('',#5462,.T.);
#3811=FACE_OUTER_BOUND('',#5463,.T.);
#3812=FACE_OUTER_BOUND('',#5464,.T.);
#3813=FACE_OUTER_BOUND('',#5465,.T.);
#3814=FACE_OUTER_BOUND('',#5466,.T.);
#3815=FACE_OUTER_BOUND('',#5467,.T.);
#3816=FACE_OUTER_BOUND('',#5468,.T.);
#3817=FACE_OUTER_BOUND('',#5469,.T.);
#3818=FACE_OUTER_BOUND('',#5470,.T.);
#3819=FACE_OUTER_BOUND('',#5471,.T.);
#3820=FACE_OUTER_BOUND('',#5472,.T.);
#3821=FACE_OUTER_BOUND('',#5473,.T.);
#3822=FACE_OUTER_BOUND('',#5474,.T.);
#3823=FACE_OUTER_BOUND('',#5475,.T.);
#3824=FACE_OUTER_BOUND('',#5476,.T.);
#3825=FACE_OUTER_BOUND('',#5477,.T.);
#3826=FACE_OUTER_BOUND('',#5478,.T.);
#3827=FACE_OUTER_BOUND('',#5479,.T.);
#3828=FACE_OUTER_BOUND('',#5480,.T.);
#3829=FACE_OUTER_BOUND('',#5481,.T.);
#3830=FACE_OUTER_BOUND('',#5482,.T.);
#3831=FACE_OUTER_BOUND('',#5483,.T.);
#3832=FACE_OUTER_BOUND('',#5484,.T.);
#3833=FACE_OUTER_BOUND('',#5485,.T.);
#3834=FACE_OUTER_BOUND('',#5486,.T.);
#3835=FACE_OUTER_BOUND('',#5487,.T.);
#3836=FACE_OUTER_BOUND('',#5488,.T.);
#3837=FACE_OUTER_BOUND('',#5489,.T.);
#3838=FACE_OUTER_BOUND('',#5490,.T.);
#3839=FACE_OUTER_BOUND('',#5491,.T.);
#3840=FACE_OUTER_BOUND('',#5492,.T.);
#3841=FACE_OUTER_BOUND('',#5493,.T.);
#3842=FACE_OUTER_BOUND('',#5494,.T.);
#3843=FACE_OUTER_BOUND('',#5495,.T.);
#3844=FACE_OUTER_BOUND('',#5496,.T.);
#3845=FACE_OUTER_BOUND('',#5497,.T.);
#3846=FACE_OUTER_BOUND('',#5498,.T.);
#3847=FACE_OUTER_BOUND('',#5499,.T.);
#3848=FACE_OUTER_BOUND('',#5500,.T.);
#3849=FACE_OUTER_BOUND('',#5501,.T.);
#3850=FACE_OUTER_BOUND('',#5502,.T.);
#3851=FACE_OUTER_BOUND('',#5503,.T.);
#3852=FACE_OUTER_BOUND('',#5504,.T.);
#3853=FACE_OUTER_BOUND('',#5505,.T.);
#3854=FACE_OUTER_BOUND('',#5506,.T.);
#3855=FACE_OUTER_BOUND('',#5507,.T.);
#3856=FACE_OUTER_BOUND('',#5508,.T.);
#3857=FACE_OUTER_BOUND('',#5509,.T.);
#3858=FACE_OUTER_BOUND('',#5510,.T.);
#3859=FACE_OUTER_BOUND('',#5511,.T.);
#3860=FACE_OUTER_BOUND('',#5512,.T.);
#3861=FACE_OUTER_BOUND('',#5513,.T.);
#3862=FACE_OUTER_BOUND('',#5514,.T.);
#3863=FACE_OUTER_BOUND('',#5515,.T.);
#3864=FACE_OUTER_BOUND('',#5516,.T.);
#3865=FACE_OUTER_BOUND('',#5517,.T.);
#5300=EDGE_LOOP('',(#22765,#22766,#22767,#22768));
#5301=EDGE_LOOP('',(#22769,#22770,#22771,#22772));
#5302=EDGE_LOOP('',(#22773,#22774,#22775,#22776));
#5303=EDGE_LOOP('',(#22777,#22778,#22779,#22780));
#5304=EDGE_LOOP('',(#22781,#22782,#22783,#22784));
#5305=EDGE_LOOP('',(#22785,#22786,#22787,#22788));
#5306=EDGE_LOOP('',(#22789,#22790,#22791,#22792));
#5307=EDGE_LOOP('',(#22793,#22794,#22795,#22796));
#5308=EDGE_LOOP('',(#22797,#22798,#22799,#22800));
#5309=EDGE_LOOP('',(#22801,#22802,#22803,#22804));
#5310=EDGE_LOOP('',(#22805,#22806,#22807,#22808));
#5311=EDGE_LOOP('',(#22809,#22810,#22811,#22812));
#5312=EDGE_LOOP('',(#22813,#22814,#22815,#22816));
#5313=EDGE_LOOP('',(#22817,#22818,#22819,#22820));
#5314=EDGE_LOOP('',(#22821,#22822,#22823,#22824));
#5315=EDGE_LOOP('',(#22825,#22826,#22827,#22828));
#5316=EDGE_LOOP('',(#22829,#22830,#22831,#22832));
#5317=EDGE_LOOP('',(#22833,#22834,#22835,#22836));
#5318=EDGE_LOOP('',(#22837,#22838,#22839,#22840));
#5319=EDGE_LOOP('',(#22841,#22842,#22843,#22844));
#5320=EDGE_LOOP('',(#22845,#22846,#22847,#22848));
#5321=EDGE_LOOP('',(#22849,#22850,#22851,#22852));
#5322=EDGE_LOOP('',(#22853,#22854,#22855,#22856));
#5323=EDGE_LOOP('',(#22857,#22858,#22859,#22860));
#5324=EDGE_LOOP('',(#22861,#22862,#22863,#22864));
#5325=EDGE_LOOP('',(#22865,#22866,#22867,#22868));
#5326=EDGE_LOOP('',(#22869,#22870,#22871,#22872));
#5327=EDGE_LOOP('',(#22873,#22874,#22875,#22876));
#5328=EDGE_LOOP('',(#22877,#22878,#22879,#22880));
#5329=EDGE_LOOP('',(#22881,#22882,#22883,#22884));
#5330=EDGE_LOOP('',(#22885,#22886,#22887,#22888));
#5331=EDGE_LOOP('',(#22889,#22890,#22891,#22892));
#5332=EDGE_LOOP('',(#22893,#22894,#22895,#22896));
#5333=EDGE_LOOP('',(#22897,#22898,#22899,#22900));
#5334=EDGE_LOOP('',(#22901,#22902,#22903,#22904));
#5335=EDGE_LOOP('',(#22905,#22906,#22907,#22908));
#5336=EDGE_LOOP('',(#22909,#22910,#22911,#22912));
#5337=EDGE_LOOP('',(#22913,#22914,#22915,#22916));
#5338=EDGE_LOOP('',(#22917,#22918,#22919,#22920));
#5339=EDGE_LOOP('',(#22921,#22922,#22923,#22924));
#5340=EDGE_LOOP('',(#22925,#22926,#22927,#22928));
#5341=EDGE_LOOP('',(#22929,#22930,#22931,#22932));
#5342=EDGE_LOOP('',(#22933,#22934,#22935,#22936));
#5343=EDGE_LOOP('',(#22937,#22938,#22939,#22940));
#5344=EDGE_LOOP('',(#22941,#22942,#22943,#22944));
#5345=EDGE_LOOP('',(#22945,#22946,#22947,#22948));
#5346=EDGE_LOOP('',(#22949,#22950,#22951,#22952,#22953));
#5347=EDGE_LOOP('',(#22954,#22955,#22956,#22957,#22958,#22959,#22960,#22961,
#22962,#22963,#22964,#22965,#22966,#22967,#22968,#22969,#22970,#22971,#22972,
#22973,#22974,#22975,#22976,#22977,#22978,#22979,#22980,#22981,#22982,#22983,
#22984,#22985,#22986,#22987,#22988,#22989,#22990,#22991,#22992,#22993,#22994,
#22995,#22996,#22997,#22998,#22999,#23000,#23001,#23002,#23003));
#5348=EDGE_LOOP('',(#23004,#23005,#23006,#23007,#23008));
#5349=EDGE_LOOP('',(#23009,#23010,#23011,#23012));
#5350=EDGE_LOOP('',(#23013,#23014,#23015,#23016,#23017,#23018,#23019,#23020,
#23021,#23022,#23023,#23024,#23025,#23026,#23027,#23028,#23029,#23030,#23031,
#23032,#23033,#23034,#23035,#23036,#23037,#23038,#23039,#23040,#23041,#23042,
#23043,#23044,#23045,#23046,#23047,#23048,#23049,#23050,#23051,#23052,#23053,
#23054,#23055,#23056,#23057,#23058,#23059,#23060,#23061,#23062));
#5351=EDGE_LOOP('',(#23063,#23064,#23065,#23066,#23067,#23068));
#5352=EDGE_LOOP('',(#23069,#23070,#23071,#23072));
#5353=EDGE_LOOP('',(#23073));
#5354=EDGE_LOOP('',(#23074));
#5355=EDGE_LOOP('',(#23075,#23076));
#5356=EDGE_LOOP('',(#23077,#23078));
#5357=EDGE_LOOP('',(#23079,#23080));
#5358=EDGE_LOOP('',(#23081,#23082));
#5359=EDGE_LOOP('',(#23083,#23084));
#5360=EDGE_LOOP('',(#23085,#23086));
#5361=EDGE_LOOP('',(#23087,#23088,#23089,#23090,#23091,#23092,#23093,#23094));
#5362=EDGE_LOOP('',(#23095,#23096,#23097,#23098));
#5363=EDGE_LOOP('',(#23099,#23100,#23101,#23102));
#5364=EDGE_LOOP('',(#23103,#23104,#23105,#23106));
#5365=EDGE_LOOP('',(#23107,#23108,#23109,#23110));
#5366=EDGE_LOOP('',(#23111,#23112,#23113,#23114));
#5367=EDGE_LOOP('',(#23115,#23116,#23117,#23118));
#5368=EDGE_LOOP('',(#23119,#23120,#23121,#23122));
#5369=EDGE_LOOP('',(#23123,#23124,#23125));
#5370=EDGE_LOOP('',(#23126,#23127,#23128,#23129));
#5371=EDGE_LOOP('',(#23130,#23131,#23132));
#5372=EDGE_LOOP('',(#23133,#23134,#23135,#23136));
#5373=EDGE_LOOP('',(#23137,#23138,#23139));
#5374=EDGE_LOOP('',(#23140,#23141,#23142,#23143));
#5375=EDGE_LOOP('',(#23144,#23145,#23146));
#5376=EDGE_LOOP('',(#23147,#23148,#23149,#23150));
#5377=EDGE_LOOP('',(#23151,#23152,#23153));
#5378=EDGE_LOOP('',(#23154,#23155,#23156,#23157));
#5379=EDGE_LOOP('',(#23158,#23159,#23160));
#5380=EDGE_LOOP('',(#23161,#23162,#23163,#23164));
#5381=EDGE_LOOP('',(#23165,#23166,#23167));
#5382=EDGE_LOOP('',(#23168,#23169,#23170,#23171));
#5383=EDGE_LOOP('',(#23172,#23173,#23174));
#5384=EDGE_LOOP('',(#23175,#23176,#23177,#23178));
#5385=EDGE_LOOP('',(#23179,#23180,#23181));
#5386=EDGE_LOOP('',(#23182,#23183,#23184,#23185));
#5387=EDGE_LOOP('',(#23186,#23187,#23188));
#5388=EDGE_LOOP('',(#23189,#23190,#23191,#23192));
#5389=EDGE_LOOP('',(#23193,#23194,#23195));
#5390=EDGE_LOOP('',(#23196,#23197,#23198,#23199));
#5391=EDGE_LOOP('',(#23200,#23201,#23202));
#5392=EDGE_LOOP('',(#23203,#23204,#23205,#23206));
#5393=EDGE_LOOP('',(#23207,#23208,#23209));
#5394=EDGE_LOOP('',(#23210,#23211,#23212,#23213));
#5395=EDGE_LOOP('',(#23214,#23215,#23216));
#5396=EDGE_LOOP('',(#23217,#23218,#23219,#23220));
#5397=EDGE_LOOP('',(#23221,#23222,#23223));
#5398=EDGE_LOOP('',(#23224,#23225,#23226,#23227));
#5399=EDGE_LOOP('',(#23228,#23229,#23230));
#5400=EDGE_LOOP('',(#23231,#23232,#23233,#23234));
#5401=EDGE_LOOP('',(#23235,#23236,#23237,#23238));
#5402=EDGE_LOOP('',(#23239,#23240,#23241,#23242));
#5403=EDGE_LOOP('',(#23243,#23244,#23245,#23246));
#5404=EDGE_LOOP('',(#23247,#23248,#23249,#23250));
#5405=EDGE_LOOP('',(#23251,#23252,#23253));
#5406=EDGE_LOOP('',(#23254,#23255,#23256,#23257));
#5407=EDGE_LOOP('',(#23258,#23259,#23260));
#5408=EDGE_LOOP('',(#23261,#23262,#23263,#23264));
#5409=EDGE_LOOP('',(#23265,#23266,#23267));
#5410=EDGE_LOOP('',(#23268,#23269,#23270,#23271));
#5411=EDGE_LOOP('',(#23272,#23273,#23274));
#5412=EDGE_LOOP('',(#23275,#23276,#23277,#23278));
#5413=EDGE_LOOP('',(#23279,#23280,#23281));
#5414=EDGE_LOOP('',(#23282,#23283,#23284,#23285));
#5415=EDGE_LOOP('',(#23286,#23287,#23288));
#5416=EDGE_LOOP('',(#23289,#23290,#23291,#23292));
#5417=EDGE_LOOP('',(#23293,#23294,#23295));
#5418=EDGE_LOOP('',(#23296,#23297,#23298,#23299));
#5419=EDGE_LOOP('',(#23300,#23301,#23302));
#5420=EDGE_LOOP('',(#23303,#23304,#23305,#23306));
#5421=EDGE_LOOP('',(#23307,#23308,#23309));
#5422=EDGE_LOOP('',(#23310,#23311,#23312,#23313));
#5423=EDGE_LOOP('',(#23314,#23315,#23316));
#5424=EDGE_LOOP('',(#23317,#23318,#23319,#23320));
#5425=EDGE_LOOP('',(#23321,#23322,#23323));
#5426=EDGE_LOOP('',(#23324,#23325,#23326,#23327));
#5427=EDGE_LOOP('',(#23328,#23329,#23330));
#5428=EDGE_LOOP('',(#23331,#23332,#23333,#23334));
#5429=EDGE_LOOP('',(#23335,#23336,#23337));
#5430=EDGE_LOOP('',(#23338,#23339,#23340,#23341));
#5431=EDGE_LOOP('',(#23342,#23343,#23344));
#5432=EDGE_LOOP('',(#23345,#23346,#23347,#23348));
#5433=EDGE_LOOP('',(#23349,#23350,#23351));
#5434=EDGE_LOOP('',(#23352,#23353,#23354,#23355));
#5435=EDGE_LOOP('',(#23356,#23357,#23358));
#5436=EDGE_LOOP('',(#23359,#23360,#23361,#23362));
#5437=EDGE_LOOP('',(#23363,#23364,#23365));
#5438=EDGE_LOOP('',(#23366,#23367,#23368,#23369));
#5439=EDGE_LOOP('',(#23370,#23371,#23372));
#5440=EDGE_LOOP('',(#23373,#23374,#23375,#23376));
#5441=EDGE_LOOP('',(#23377,#23378,#23379));
#5442=EDGE_LOOP('',(#23380,#23381,#23382,#23383));
#5443=EDGE_LOOP('',(#23384,#23385,#23386));
#5444=EDGE_LOOP('',(#23387,#23388,#23389,#23390));
#5445=EDGE_LOOP('',(#23391,#23392,#23393));
#5446=EDGE_LOOP('',(#23394,#23395,#23396,#23397));
#5447=EDGE_LOOP('',(#23398,#23399,#23400));
#5448=EDGE_LOOP('',(#23401,#23402,#23403,#23404));
#5449=EDGE_LOOP('',(#23405,#23406,#23407));
#5450=EDGE_LOOP('',(#23408,#23409,#23410,#23411));
#5451=EDGE_LOOP('',(#23412,#23413,#23414));
#5452=EDGE_LOOP('',(#23415,#23416,#23417,#23418));
#5453=EDGE_LOOP('',(#23419,#23420,#23421));
#5454=EDGE_LOOP('',(#23422,#23423,#23424,#23425));
#5455=EDGE_LOOP('',(#23426,#23427,#23428));
#5456=EDGE_LOOP('',(#23429,#23430,#23431,#23432));
#5457=EDGE_LOOP('',(#23433,#23434,#23435));
#5458=EDGE_LOOP('',(#23436,#23437,#23438,#23439));
#5459=EDGE_LOOP('',(#23440,#23441,#23442));
#5460=EDGE_LOOP('',(#23443,#23444,#23445,#23446));
#5461=EDGE_LOOP('',(#23447,#23448,#23449));
#5462=EDGE_LOOP('',(#23450,#23451,#23452,#23453));
#5463=EDGE_LOOP('',(#23454,#23455,#23456));
#5464=EDGE_LOOP('',(#23457,#23458,#23459,#23460));
#5465=EDGE_LOOP('',(#23461,#23462,#23463));
#5466=EDGE_LOOP('',(#23464,#23465,#23466,#23467));
#5467=EDGE_LOOP('',(#23468,#23469,#23470));
#5468=EDGE_LOOP('',(#23471,#23472,#23473,#23474));
#5469=EDGE_LOOP('',(#23475,#23476,#23477));
#5470=EDGE_LOOP('',(#23478,#23479,#23480,#23481));
#5471=EDGE_LOOP('',(#23482,#23483,#23484));
#5472=EDGE_LOOP('',(#23485,#23486,#23487));
#5473=EDGE_LOOP('',(#23488,#23489,#23490,#23491));
#5474=EDGE_LOOP('',(#23492,#23493,#23494,#23495));
#5475=EDGE_LOOP('',(#23496,#23497,#23498));
#5476=EDGE_LOOP('',(#23499,#23500,#23501,#23502));
#5477=EDGE_LOOP('',(#23503,#23504,#23505));
#5478=EDGE_LOOP('',(#23506,#23507,#23508,#23509));
#5479=EDGE_LOOP('',(#23510,#23511,#23512));
#5480=EDGE_LOOP('',(#23513,#23514,#23515,#23516));
#5481=EDGE_LOOP('',(#23517,#23518,#23519));
#5482=EDGE_LOOP('',(#23520,#23521,#23522,#23523));
#5483=EDGE_LOOP('',(#23524,#23525,#23526));
#5484=EDGE_LOOP('',(#23527,#23528,#23529,#23530));
#5485=EDGE_LOOP('',(#23531,#23532,#23533));
#5486=EDGE_LOOP('',(#23534,#23535,#23536,#23537));
#5487=EDGE_LOOP('',(#23538,#23539,#23540));
#5488=EDGE_LOOP('',(#23541,#23542,#23543,#23544));
#5489=EDGE_LOOP('',(#23545,#23546,#23547));
#5490=EDGE_LOOP('',(#23548,#23549,#23550,#23551));
#5491=EDGE_LOOP('',(#23552,#23553,#23554));
#5492=EDGE_LOOP('',(#23555,#23556,#23557,#23558));
#5493=EDGE_LOOP('',(#23559,#23560,#23561));
#5494=EDGE_LOOP('',(#23562,#23563,#23564,#23565));
#5495=EDGE_LOOP('',(#23566,#23567,#23568));
#5496=EDGE_LOOP('',(#23569,#23570,#23571,#23572));
#5497=EDGE_LOOP('',(#23573,#23574,#23575));
#5498=EDGE_LOOP('',(#23576,#23577,#23578,#23579));
#5499=EDGE_LOOP('',(#23580,#23581,#23582));
#5500=EDGE_LOOP('',(#23583,#23584,#23585,#23586));
#5501=EDGE_LOOP('',(#23587,#23588,#23589));
#5502=EDGE_LOOP('',(#23590,#23591,#23592,#23593));
#5503=EDGE_LOOP('',(#23594,#23595,#23596));
#5504=EDGE_LOOP('',(#23597,#23598,#23599,#23600));
#5505=EDGE_LOOP('',(#23601,#23602,#23603));
#5506=EDGE_LOOP('',(#23604,#23605,#23606,#23607));
#5507=EDGE_LOOP('',(#23608,#23609,#23610));
#5508=EDGE_LOOP('',(#23611,#23612,#23613,#23614));
#5509=EDGE_LOOP('',(#23615,#23616,#23617));
#5510=EDGE_LOOP('',(#23618,#23619,#23620,#23621));
#5511=EDGE_LOOP('',(#23622,#23623,#23624));
#5512=EDGE_LOOP('',(#23625));
#5513=EDGE_LOOP('',(#23626,#23627,#23628,#23629,#23630,#23631));
#5514=EDGE_LOOP('',(#23632,#23633,#23634,#23635));
#5515=EDGE_LOOP('',(#23636,#23637,#23638,#23639,#23640,#23641,#23642,#23643,
#23644,#23645,#23646,#23647,#23648,#23649,#23650,#23651,#23652,#23653,#23654,
#23655,#23656,#23657,#23658,#23659,#23660,#23661,#23662,#23663,#23664,#23665,
#23666,#23667,#23668,#23669,#23670,#23671,#23672,#23673,#23674,#23675,#23676,
#23677,#23678,#23679,#23680,#23681,#23682,#23683,#23684,#23685,#23686,#23687,
#23688,#23689,#23690,#23691,#23692,#23693,#23694,#23695,#23696,#23697,#23698,
#23699,#23700,#23701,#23702,#23703,#23704,#23705,#23706,#23707,#23708,#23709,
#23710,#23711,#23712,#23713,#23714,#23715,#23716,#23717,#23718,#23719,#23720,
#23721,#23722,#23723,#23724,#23725,#23726,#23727,#23728,#23729,#23730,#23731,
#23732,#23733,#23734,#23735,#23736,#23737,#23738,#23739,#23740,#23741,#23742,
#23743,#23744,#23745,#23746,#23747,#23748,#23749,#23750,#23751,#23752,#23753,
#23754,#23755,#23756,#23757,#23758,#23759,#23760,#23761,#23762,#23763,#23764,
#23765,#23766,#23767,#23768,#23769,#23770,#23771,#23772,#23773,#23774,#23775,
#23776,#23777,#23778,#23779,#23780,#23781,#23782,#23783));
#5516=EDGE_LOOP('',(#23784,#23785,#23786,#23787,#23788,#23789,#23790,#23791,
#23792,#23793,#23794,#23795,#23796,#23797,#23798,#23799,#23800,#23801,#23802,
#23803,#23804,#23805,#23806,#23807,#23808,#23809,#23810,#23811,#23812,#23813,
#23814,#23815,#23816,#23817,#23818,#23819,#23820,#23821,#23822,#23823,#23824,
#23825,#23826,#23827,#23828,#23829,#23830,#23831,#23832,#23833,#23834,#23835,
#23836,#23837,#23838,#23839,#23840,#23841,#23842,#23843,#23844,#23845,#23846,
#23847,#23848,#23849,#23850,#23851,#23852,#23853,#23854,#23855,#23856,#23857,
#23858,#23859));
#5517=EDGE_LOOP('',(#23860));
#5518=EDGE_LOOP('',(#23861,#23862,#23863,#23864,#23865,#23866));
#6332=CIRCLE('',#28634,0.4925);
#6333=CIRCLE('',#28658,0.40705);
#6334=CIRCLE('',#28682,0.4925);
#6335=CIRCLE('',#28683,0.4925);
#6336=CIRCLE('',#28685,0.4925);
#6337=CIRCLE('',#28686,0.4925);
#6338=CIRCLE('',#28687,0.40705);
#6339=CIRCLE('',#28690,0.025);
#6340=CIRCLE('',#28691,0.5175);
#6341=CIRCLE('',#28692,0.4925);
#6342=CIRCLE('',#28695,0.77);
#6343=CIRCLE('',#28697,0.461880215351701);
#6344=CIRCLE('',#28699,0.461880215351701);
#6345=CIRCLE('',#28701,0.461880215351701);
#6346=CIRCLE('',#28703,0.461880215351701);
#6347=CIRCLE('',#28705,0.461880215351701);
#6348=CIRCLE('',#28707,0.461880215351701);
#6349=CIRCLE('',#28717,0.8);
#6350=CIRCLE('',#28720,0.8);
#6351=CIRCLE('',#28723,0.8);
#6352=CIRCLE('',#28726,0.8);
#6353=CIRCLE('',#28729,0.8);
#6354=CIRCLE('',#28732,0.8);
#6355=CIRCLE('',#28735,0.8);
#6356=CIRCLE('',#28738,0.8);
#6357=CIRCLE('',#28741,0.8);
#6358=CIRCLE('',#28744,0.8);
#6359=CIRCLE('',#28747,0.8);
#6360=CIRCLE('',#28750,0.8);
#6361=CIRCLE('',#28753,0.8);
#6362=CIRCLE('',#28756,0.8);
#6363=CIRCLE('',#28759,0.8);
#6364=CIRCLE('',#28762,0.8);
#6365=CIRCLE('',#28765,0.8);
#6366=CIRCLE('',#28766,0.8);
#6367=CIRCLE('',#28769,0.8);
#6368=CIRCLE('',#28770,0.8);
#6369=CIRCLE('',#28773,0.8);
#6370=CIRCLE('',#28776,0.8);
#6371=CIRCLE('',#28779,0.8);
#6372=CIRCLE('',#28782,0.8);
#6373=CIRCLE('',#28785,0.8);
#6374=CIRCLE('',#28788,0.8);
#6375=CIRCLE('',#28791,0.8);
#6376=CIRCLE('',#28794,0.8);
#6377=CIRCLE('',#28797,0.8);
#6378=CIRCLE('',#28800,0.8);
#6379=CIRCLE('',#28803,0.8);
#6380=CIRCLE('',#28806,0.8);
#6381=CIRCLE('',#28809,0.8);
#6382=CIRCLE('',#28812,0.8);
#6383=CIRCLE('',#28815,0.8);
#6384=CIRCLE('',#28818,0.8);
#6385=CIRCLE('',#28821,0.8);
#6386=CIRCLE('',#28824,0.8);
#6387=CIRCLE('',#28827,0.8);
#6388=CIRCLE('',#28830,0.8);
#6389=CIRCLE('',#28833,0.8);
#6390=CIRCLE('',#28836,0.8);
#6391=CIRCLE('',#28839,0.8);
#6392=CIRCLE('',#28842,0.8);
#6393=CIRCLE('',#28845,0.8);
#6394=CIRCLE('',#28848,0.8);
#6395=CIRCLE('',#28851,0.8);
#6396=CIRCLE('',#28854,0.8);
#6397=CIRCLE('',#28857,0.8);
#6398=CIRCLE('',#28860,0.8);
#6399=CIRCLE('',#28863,0.8);
#6400=CIRCLE('',#28866,0.8);
#6401=CIRCLE('',#28869,0.8);
#6402=CIRCLE('',#28872,0.8);
#6403=CIRCLE('',#28874,0.8);
#6404=CIRCLE('',#28878,0.8);
#6405=CIRCLE('',#28881,0.8);
#6406=CIRCLE('',#28884,0.8);
#6407=CIRCLE('',#28887,0.8);
#6408=CIRCLE('',#28890,0.8);
#6409=CIRCLE('',#28893,0.8);
#6410=CIRCLE('',#28896,0.8);
#6411=CIRCLE('',#28899,0.8);
#6412=CIRCLE('',#28902,0.8);
#6413=CIRCLE('',#28905,0.8);
#6414=CIRCLE('',#28908,0.8);
#6415=CIRCLE('',#28911,0.8);
#6416=CIRCLE('',#28914,0.8);
#6417=CIRCLE('',#28917,0.8);
#6418=CIRCLE('',#28920,0.8);
#6419=CIRCLE('',#28923,0.8);
#6420=CIRCLE('',#28926,0.8);
#6421=CIRCLE('',#28929,0.8);
#6422=CIRCLE('',#28932,0.8);
#6423=CIRCLE('',#28934,0.45);
#6424=CIRCLE('',#28937,0.8);
#6425=CIRCLE('',#28939,0.8);
#6426=CIRCLE('',#28940,0.8);
#6427=CIRCLE('',#28941,0.8);
#6428=CIRCLE('',#28942,0.8);
#6429=CIRCLE('',#28943,0.8);
#6430=CIRCLE('',#28944,0.8);
#6431=CIRCLE('',#28945,0.8);
#6432=CIRCLE('',#28946,0.8);
#6433=CIRCLE('',#28947,0.8);
#6434=CIRCLE('',#28948,0.8);
#6435=CIRCLE('',#28949,0.8);
#6436=CIRCLE('',#28950,0.8);
#6437=CIRCLE('',#28951,0.8);
#6438=CIRCLE('',#28952,0.8);
#6439=CIRCLE('',#28953,0.8);
#6440=CIRCLE('',#28954,0.8);
#6441=CIRCLE('',#28955,0.8);
#6442=CIRCLE('',#28956,0.8);
#6443=CIRCLE('',#28957,0.8);
#6444=CIRCLE('',#28958,0.8);
#6445=CIRCLE('',#28959,0.8);
#6446=CIRCLE('',#28960,0.8);
#6447=CIRCLE('',#28961,0.8);
#6448=CIRCLE('',#28962,0.8);
#6449=CIRCLE('',#28963,0.8);
#6450=CIRCLE('',#28964,0.8);
#6451=CIRCLE('',#28965,0.8);
#6452=CIRCLE('',#28966,0.8);
#6453=CIRCLE('',#28967,0.8);
#6454=CIRCLE('',#28968,0.8);
#6455=CIRCLE('',#28969,0.8);
#6456=CIRCLE('',#28970,0.8);
#6457=CIRCLE('',#28971,0.8);
#6458=CIRCLE('',#28972,0.8);
#6459=CIRCLE('',#28973,0.8);
#6460=CIRCLE('',#28974,0.8);
#6461=CIRCLE('',#28976,0.75);
#8113=LINE('',#69069,#10269);
#8114=LINE('',#69096,#10270);
#8115=LINE('',#69144,#10271);
#8116=LINE('',#69192,#10272);
#8117=LINE('',#69240,#10273);
#8118=LINE('',#69294,#10274);
#8119=LINE('',#69342,#10275);
#8120=LINE('',#69390,#10276);
#8121=LINE('',#69444,#10277);
#8122=LINE('',#69492,#10278);
#8123=LINE('',#69540,#10279);
#8124=LINE('',#69591,#10280);
#8125=LINE('',#69642,#10281);
#8126=LINE('',#69690,#10282);
#8127=LINE('',#69738,#10283);
#8128=LINE('',#69792,#10284);
#8129=LINE('',#69840,#10285);
#8130=LINE('',#69888,#10286);
#8131=LINE('',#69942,#10287);
#8132=LINE('',#69990,#10288);
#8133=LINE('',#70038,#10289);
#8134=LINE('',#70086,#10290);
#8135=LINE('',#70140,#10291);
#8136=LINE('',#70188,#10292);
#8137=LINE('',#70204,#10293);
#8138=LINE('',#70229,#10294);
#8139=LINE('',#70254,#10295);
#8140=LINE('',#70279,#10296);
#8141=LINE('',#70303,#10297);
#8142=LINE('',#70327,#10298);
#8143=LINE('',#70352,#10299);
#8144=LINE('',#70377,#10300);
#8145=LINE('',#70401,#10301);
#8146=LINE('',#70426,#10302);
#8147=LINE('',#70451,#10303);
#8148=LINE('',#70475,#10304);
#8149=LINE('',#70500,#10305);
#8150=LINE('',#70524,#10306);
#8151=LINE('',#70549,#10307);
#8152=LINE('',#70573,#10308);
#8153=LINE('',#70598,#10309);
#8154=LINE('',#70623,#10310);
#8155=LINE('',#70647,#10311);
#8156=LINE('',#70672,#10312);
#8157=LINE('',#70697,#10313);
#8158=LINE('',#70721,#10314);
#8159=LINE('',#72294,#10315);
#8160=LINE('',#72298,#10316);
#8161=LINE('',#72302,#10317);
#8162=LINE('',#72306,#10318);
#8163=LINE('',#72310,#10319);
#8164=LINE('',#72313,#10320);
#8165=LINE('',#72317,#10321);
#8166=LINE('',#72321,#10322);
#8167=LINE('',#72322,#10323);
#8168=LINE('',#72323,#10324);
#8169=LINE('',#72326,#10325);
#8170=LINE('',#72327,#10326);
#8171=LINE('',#72330,#10327);
#8172=LINE('',#72331,#10328);
#8173=LINE('',#72334,#10329);
#8174=LINE('',#72335,#10330);
#8175=LINE('',#72338,#10331);
#8176=LINE('',#72339,#10332);
#8177=LINE('',#72341,#10333);
#8178=LINE('',#72345,#10334);
#8179=LINE('',#72347,#10335);
#8180=LINE('',#72349,#10336);
#8181=LINE('',#72350,#10337);
#8182=LINE('',#72354,#10338);
#8183=LINE('',#72357,#10339);
#8184=LINE('',#72358,#10340);
#8185=LINE('',#72364,#10341);
#8186=LINE('',#72366,#10342);
#8187=LINE('',#72368,#10343);
#8188=LINE('',#72369,#10344);
#8189=LINE('',#72373,#10345);
#8190=LINE('',#72376,#10346);
#8191=LINE('',#72377,#10347);
#8192=LINE('',#72383,#10348);
#8193=LINE('',#72385,#10349);
#8194=LINE('',#72387,#10350);
#8195=LINE('',#72388,#10351);
#8196=LINE('',#72392,#10352);
#8197=LINE('',#72395,#10353);
#8198=LINE('',#72396,#10354);
#8199=LINE('',#72402,#10355);
#8200=LINE('',#72404,#10356);
#8201=LINE('',#72406,#10357);
#8202=LINE('',#72407,#10358);
#8203=LINE('',#72411,#10359);
#8204=LINE('',#72414,#10360);
#8205=LINE('',#72415,#10361);
#8206=LINE('',#72421,#10362);
#8207=LINE('',#72423,#10363);
#8208=LINE('',#72425,#10364);
#8209=LINE('',#72426,#10365);
#8210=LINE('',#72430,#10366);
#8211=LINE('',#72433,#10367);
#8212=LINE('',#72434,#10368);
#8213=LINE('',#72440,#10369);
#8214=LINE('',#72442,#10370);
#8215=LINE('',#72444,#10371);
#8216=LINE('',#72445,#10372);
#8217=LINE('',#72449,#10373);
#8218=LINE('',#72452,#10374);
#8219=LINE('',#72453,#10375);
#8220=LINE('',#72459,#10376);
#8221=LINE('',#72461,#10377);
#8222=LINE('',#72463,#10378);
#8223=LINE('',#72464,#10379);
#8224=LINE('',#72468,#10380);
#8225=LINE('',#72471,#10381);
#8226=LINE('',#72472,#10382);
#8227=LINE('',#72478,#10383);
#8228=LINE('',#72480,#10384);
#8229=LINE('',#72482,#10385);
#8230=LINE('',#72483,#10386);
#8231=LINE('',#72487,#10387);
#8232=LINE('',#72490,#10388);
#8233=LINE('',#72491,#10389);
#8234=LINE('',#72497,#10390);
#8235=LINE('',#72499,#10391);
#8236=LINE('',#72501,#10392);
#8237=LINE('',#72502,#10393);
#8238=LINE('',#72507,#10394);
#8239=LINE('',#72511,#10395);
#8240=LINE('',#72512,#10396);
#8241=LINE('',#72520,#10397);
#8242=LINE('',#72522,#10398);
#8243=LINE('',#72524,#10399);
#8244=LINE('',#72525,#10400);
#8245=LINE('',#72529,#10401);
#8246=LINE('',#72532,#10402);
#8247=LINE('',#72533,#10403);
#8248=LINE('',#72539,#10404);
#8249=LINE('',#72541,#10405);
#8250=LINE('',#72543,#10406);
#8251=LINE('',#72544,#10407);
#8252=LINE('',#72548,#10408);
#8253=LINE('',#72551,#10409);
#8254=LINE('',#72552,#10410);
#8255=LINE('',#72558,#10411);
#8256=LINE('',#72560,#10412);
#8257=LINE('',#72562,#10413);
#8258=LINE('',#72563,#10414);
#8259=LINE('',#72567,#10415);
#8260=LINE('',#72570,#10416);
#8261=LINE('',#72571,#10417);
#8262=LINE('',#72577,#10418);
#8263=LINE('',#72579,#10419);
#8264=LINE('',#72581,#10420);
#8265=LINE('',#72582,#10421);
#8266=LINE('',#72586,#10422);
#8267=LINE('',#72589,#10423);
#8268=LINE('',#72590,#10424);
#8269=LINE('',#72596,#10425);
#8270=LINE('',#72598,#10426);
#8271=LINE('',#72600,#10427);
#8272=LINE('',#72601,#10428);
#8273=LINE('',#72605,#10429);
#8274=LINE('',#72608,#10430);
#8275=LINE('',#72609,#10431);
#8276=LINE('',#72615,#10432);
#8277=LINE('',#72617,#10433);
#8278=LINE('',#72619,#10434);
#8279=LINE('',#72620,#10435);
#8280=LINE('',#72624,#10436);
#8281=LINE('',#72627,#10437);
#8282=LINE('',#72628,#10438);
#8283=LINE('',#72634,#10439);
#8284=LINE('',#72636,#10440);
#8285=LINE('',#72638,#10441);
#8286=LINE('',#72639,#10442);
#8287=LINE('',#72643,#10443);
#8288=LINE('',#72646,#10444);
#8289=LINE('',#72647,#10445);
#8290=LINE('',#72653,#10446);
#8291=LINE('',#72655,#10447);
#8292=LINE('',#72657,#10448);
#8293=LINE('',#72658,#10449);
#8294=LINE('',#72662,#10450);
#8295=LINE('',#72665,#10451);
#8296=LINE('',#72666,#10452);
#8297=LINE('',#72672,#10453);
#8298=LINE('',#72674,#10454);
#8299=LINE('',#72676,#10455);
#8300=LINE('',#72677,#10456);
#8301=LINE('',#72681,#10457);
#8302=LINE('',#72684,#10458);
#8303=LINE('',#72685,#10459);
#8304=LINE('',#72691,#10460);
#8305=LINE('',#72693,#10461);
#8306=LINE('',#72695,#10462);
#8307=LINE('',#72696,#10463);
#8308=LINE('',#72700,#10464);
#8309=LINE('',#72703,#10465);
#8310=LINE('',#72704,#10466);
#8311=LINE('',#72710,#10467);
#8312=LINE('',#72712,#10468);
#8313=LINE('',#72714,#10469);
#8314=LINE('',#72715,#10470);
#8315=LINE('',#72719,#10471);
#8316=LINE('',#72722,#10472);
#8317=LINE('',#72723,#10473);
#8318=LINE('',#72729,#10474);
#8319=LINE('',#72731,#10475);
#8320=LINE('',#72733,#10476);
#8321=LINE('',#72734,#10477);
#8322=LINE('',#72738,#10478);
#8323=LINE('',#72741,#10479);
#8324=LINE('',#72742,#10480);
#8325=LINE('',#72748,#10481);
#8326=LINE('',#72750,#10482);
#8327=LINE('',#72752,#10483);
#8328=LINE('',#72753,#10484);
#8329=LINE('',#72757,#10485);
#8330=LINE('',#72760,#10486);
#8331=LINE('',#72761,#10487);
#8332=LINE('',#72767,#10488);
#8333=LINE('',#72769,#10489);
#8334=LINE('',#72771,#10490);
#8335=LINE('',#72772,#10491);
#8336=LINE('',#72776,#10492);
#8337=LINE('',#72779,#10493);
#8338=LINE('',#72780,#10494);
#8339=LINE('',#72786,#10495);
#8340=LINE('',#72788,#10496);
#8341=LINE('',#72790,#10497);
#8342=LINE('',#72791,#10498);
#8343=LINE('',#72795,#10499);
#8344=LINE('',#72798,#10500);
#8345=LINE('',#72799,#10501);
#8346=LINE('',#72805,#10502);
#8347=LINE('',#72807,#10503);
#8348=LINE('',#72809,#10504);
#8349=LINE('',#72810,#10505);
#8350=LINE('',#72814,#10506);
#8351=LINE('',#72817,#10507);
#8352=LINE('',#72818,#10508);
#8353=LINE('',#72824,#10509);
#8354=LINE('',#72826,#10510);
#8355=LINE('',#72828,#10511);
#8356=LINE('',#72829,#10512);
#8357=LINE('',#72833,#10513);
#8358=LINE('',#72836,#10514);
#8359=LINE('',#72837,#10515);
#8360=LINE('',#72845,#10516);
#8361=LINE('',#72846,#10517);
#8362=LINE('',#72849,#10518);
#8363=LINE('',#72851,#10519);
#8364=LINE('',#72852,#10520);
#8365=LINE('',#72855,#10521);
#8366=LINE('',#72856,#10522);
#8367=LINE('',#72862,#10523);
#8368=LINE('',#72864,#10524);
#8369=LINE('',#72866,#10525);
#8370=LINE('',#72867,#10526);
#8371=LINE('',#72871,#10527);
#8372=LINE('',#72874,#10528);
#8373=LINE('',#72875,#10529);
#8374=LINE('',#72881,#10530);
#8375=LINE('',#72883,#10531);
#8376=LINE('',#72885,#10532);
#8377=LINE('',#72886,#10533);
#8378=LINE('',#72890,#10534);
#8379=LINE('',#72893,#10535);
#8380=LINE('',#72894,#10536);
#8381=LINE('',#72900,#10537);
#8382=LINE('',#72902,#10538);
#8383=LINE('',#72904,#10539);
#8384=LINE('',#72905,#10540);
#8385=LINE('',#72909,#10541);
#8386=LINE('',#72912,#10542);
#8387=LINE('',#72913,#10543);
#8388=LINE('',#72919,#10544);
#8389=LINE('',#72921,#10545);
#8390=LINE('',#72923,#10546);
#8391=LINE('',#72924,#10547);
#8392=LINE('',#72928,#10548);
#8393=LINE('',#72931,#10549);
#8394=LINE('',#72932,#10550);
#8395=LINE('',#72938,#10551);
#8396=LINE('',#72940,#10552);
#8397=LINE('',#72942,#10553);
#8398=LINE('',#72943,#10554);
#8399=LINE('',#72947,#10555);
#8400=LINE('',#72950,#10556);
#8401=LINE('',#72951,#10557);
#8402=LINE('',#72957,#10558);
#8403=LINE('',#72959,#10559);
#8404=LINE('',#72961,#10560);
#8405=LINE('',#72962,#10561);
#8406=LINE('',#72966,#10562);
#8407=LINE('',#72969,#10563);
#8408=LINE('',#72970,#10564);
#8409=LINE('',#72976,#10565);
#8410=LINE('',#72978,#10566);
#8411=LINE('',#72980,#10567);
#8412=LINE('',#72981,#10568);
#8413=LINE('',#72985,#10569);
#8414=LINE('',#72988,#10570);
#8415=LINE('',#72989,#10571);
#8416=LINE('',#72995,#10572);
#8417=LINE('',#72997,#10573);
#8418=LINE('',#72999,#10574);
#8419=LINE('',#73000,#10575);
#8420=LINE('',#73004,#10576);
#8421=LINE('',#73007,#10577);
#8422=LINE('',#73008,#10578);
#8423=LINE('',#73014,#10579);
#8424=LINE('',#73016,#10580);
#8425=LINE('',#73018,#10581);
#8426=LINE('',#73019,#10582);
#8427=LINE('',#73023,#10583);
#8428=LINE('',#73026,#10584);
#8429=LINE('',#73027,#10585);
#8430=LINE('',#73034,#10586);
#8431=LINE('',#73038,#10587);
#8432=LINE('',#73056,#10588);
#8433=LINE('',#73080,#10589);
#10269=VECTOR('',#34324,0.5);
#10270=VECTOR('',#34329,0.5);
#10271=VECTOR('',#34332,0.5);
#10272=VECTOR('',#34335,0.5);
#10273=VECTOR('',#34338,0.5);
#10274=VECTOR('',#34341,0.5);
#10275=VECTOR('',#34344,0.5);
#10276=VECTOR('',#34347,0.5);
#10277=VECTOR('',#34350,0.5);
#10278=VECTOR('',#34353,0.5);
#10279=VECTOR('',#34356,0.5);
#10280=VECTOR('',#34359,0.5);
#10281=VECTOR('',#34362,0.5);
#10282=VECTOR('',#34365,0.5);
#10283=VECTOR('',#34368,0.5);
#10284=VECTOR('',#34371,0.5);
#10285=VECTOR('',#34374,0.5);
#10286=VECTOR('',#34377,0.5);
#10287=VECTOR('',#34380,0.5);
#10288=VECTOR('',#34383,0.5);
#10289=VECTOR('',#34386,0.5);
#10290=VECTOR('',#34389,0.5);
#10291=VECTOR('',#34392,0.5);
#10292=VECTOR('',#34395,0.40705);
#10293=VECTOR('',#34400,0.40705);
#10294=VECTOR('',#34403,0.40705);
#10295=VECTOR('',#34406,0.40705);
#10296=VECTOR('',#34409,0.40705);
#10297=VECTOR('',#34412,0.40705);
#10298=VECTOR('',#34415,0.40705);
#10299=VECTOR('',#34418,0.40705);
#10300=VECTOR('',#34421,0.40705);
#10301=VECTOR('',#34424,0.40705);
#10302=VECTOR('',#34427,0.40705);
#10303=VECTOR('',#34430,0.40705);
#10304=VECTOR('',#34433,0.40705);
#10305=VECTOR('',#34436,0.40705);
#10306=VECTOR('',#34439,0.40705);
#10307=VECTOR('',#34442,0.40705);
#10308=VECTOR('',#34445,0.40705);
#10309=VECTOR('',#34448,0.40705);
#10310=VECTOR('',#34451,0.40705);
#10311=VECTOR('',#34454,0.40705);
#10312=VECTOR('',#34457,0.40705);
#10313=VECTOR('',#34460,0.40705);
#10314=VECTOR('',#34463,0.40705);
#10315=VECTOR('',#34496,1.);
#10316=VECTOR('',#34501,1.);
#10317=VECTOR('',#34506,1.);
#10318=VECTOR('',#34511,1.);
#10319=VECTOR('',#34516,1.);
#10320=VECTOR('',#34521,1.);
#10321=VECTOR('',#34526,0.23094010767585);
#10322=VECTOR('',#34529,1.);
#10323=VECTOR('',#34530,1.);
#10324=VECTOR('',#34531,1.);
#10325=VECTOR('',#34534,1.);
#10326=VECTOR('',#34535,1.);
#10327=VECTOR('',#34538,1.);
#10328=VECTOR('',#34539,1.);
#10329=VECTOR('',#34542,1.);
#10330=VECTOR('',#34543,1.);
#10331=VECTOR('',#34546,1.);
#10332=VECTOR('',#34547,1.);
#10333=VECTOR('',#34550,1.);
#10334=VECTOR('',#34553,1.);
#10335=VECTOR('',#34554,1.);
#10336=VECTOR('',#34555,1.);
#10337=VECTOR('',#34556,1.);
#10338=VECTOR('',#34561,1.);
#10339=VECTOR('',#34564,1.);
#10340=VECTOR('',#34565,1.);
#10341=VECTOR('',#34572,1.);
#10342=VECTOR('',#34573,1.);
#10343=VECTOR('',#34574,1.);
#10344=VECTOR('',#34575,1.);
#10345=VECTOR('',#34580,1.);
#10346=VECTOR('',#34583,1.);
#10347=VECTOR('',#34584,1.);
#10348=VECTOR('',#34591,1.);
#10349=VECTOR('',#34592,1.);
#10350=VECTOR('',#34593,1.);
#10351=VECTOR('',#34594,1.);
#10352=VECTOR('',#34599,1.);
#10353=VECTOR('',#34602,1.);
#10354=VECTOR('',#34603,1.);
#10355=VECTOR('',#34610,1.);
#10356=VECTOR('',#34611,1.);
#10357=VECTOR('',#34612,1.);
#10358=VECTOR('',#34613,1.);
#10359=VECTOR('',#34618,1.);
#10360=VECTOR('',#34621,1.);
#10361=VECTOR('',#34622,1.);
#10362=VECTOR('',#34629,1.);
#10363=VECTOR('',#34630,1.);
#10364=VECTOR('',#34631,1.);
#10365=VECTOR('',#34632,1.);
#10366=VECTOR('',#34637,1.);
#10367=VECTOR('',#34640,1.);
#10368=VECTOR('',#34641,1.);
#10369=VECTOR('',#34648,1.);
#10370=VECTOR('',#34649,1.);
#10371=VECTOR('',#34650,1.);
#10372=VECTOR('',#34651,1.);
#10373=VECTOR('',#34656,1.);
#10374=VECTOR('',#34659,1.);
#10375=VECTOR('',#34660,1.);
#10376=VECTOR('',#34667,1.);
#10377=VECTOR('',#34668,1.);
#10378=VECTOR('',#34669,1.);
#10379=VECTOR('',#34670,1.);
#10380=VECTOR('',#34675,1.);
#10381=VECTOR('',#34678,1.);
#10382=VECTOR('',#34679,1.);
#10383=VECTOR('',#34686,1.);
#10384=VECTOR('',#34687,1.);
#10385=VECTOR('',#34688,1.);
#10386=VECTOR('',#34689,1.);
#10387=VECTOR('',#34694,1.);
#10388=VECTOR('',#34697,1.);
#10389=VECTOR('',#34698,1.);
#10390=VECTOR('',#34705,1.);
#10391=VECTOR('',#34706,1.);
#10392=VECTOR('',#34707,1.);
#10393=VECTOR('',#34708,1.);
#10394=VECTOR('',#34713,1.);
#10395=VECTOR('',#34718,1.);
#10396=VECTOR('',#34719,1.);
#10397=VECTOR('',#34728,1.);
#10398=VECTOR('',#34729,1.);
#10399=VECTOR('',#34730,1.);
#10400=VECTOR('',#34731,1.);
#10401=VECTOR('',#34736,1.);
#10402=VECTOR('',#34739,1.);
#10403=VECTOR('',#34740,1.);
#10404=VECTOR('',#34747,1.);
#10405=VECTOR('',#34748,1.);
#10406=VECTOR('',#34749,1.);
#10407=VECTOR('',#34750,1.);
#10408=VECTOR('',#34755,1.);
#10409=VECTOR('',#34758,1.);
#10410=VECTOR('',#34759,1.);
#10411=VECTOR('',#34766,1.);
#10412=VECTOR('',#34767,1.);
#10413=VECTOR('',#34768,1.);
#10414=VECTOR('',#34769,1.);
#10415=VECTOR('',#34774,1.);
#10416=VECTOR('',#34777,1.);
#10417=VECTOR('',#34778,1.);
#10418=VECTOR('',#34785,1.);
#10419=VECTOR('',#34786,1.);
#10420=VECTOR('',#34787,1.);
#10421=VECTOR('',#34788,1.);
#10422=VECTOR('',#34793,1.);
#10423=VECTOR('',#34796,1.);
#10424=VECTOR('',#34797,1.);
#10425=VECTOR('',#34804,1.);
#10426=VECTOR('',#34805,1.);
#10427=VECTOR('',#34806,1.);
#10428=VECTOR('',#34807,1.);
#10429=VECTOR('',#34812,1.);
#10430=VECTOR('',#34815,1.);
#10431=VECTOR('',#34816,1.);
#10432=VECTOR('',#34823,1.);
#10433=VECTOR('',#34824,1.);
#10434=VECTOR('',#34825,1.);
#10435=VECTOR('',#34826,1.);
#10436=VECTOR('',#34831,1.);
#10437=VECTOR('',#34834,1.);
#10438=VECTOR('',#34835,1.);
#10439=VECTOR('',#34842,1.);
#10440=VECTOR('',#34843,1.);
#10441=VECTOR('',#34844,1.);
#10442=VECTOR('',#34845,1.);
#10443=VECTOR('',#34850,1.);
#10444=VECTOR('',#34853,1.);
#10445=VECTOR('',#34854,1.);
#10446=VECTOR('',#34861,1.);
#10447=VECTOR('',#34862,1.);
#10448=VECTOR('',#34863,1.);
#10449=VECTOR('',#34864,1.);
#10450=VECTOR('',#34869,1.);
#10451=VECTOR('',#34872,1.);
#10452=VECTOR('',#34873,1.);
#10453=VECTOR('',#34880,1.);
#10454=VECTOR('',#34881,1.);
#10455=VECTOR('',#34882,1.);
#10456=VECTOR('',#34883,1.);
#10457=VECTOR('',#34888,1.);
#10458=VECTOR('',#34891,1.);
#10459=VECTOR('',#34892,1.);
#10460=VECTOR('',#34899,1.);
#10461=VECTOR('',#34900,1.);
#10462=VECTOR('',#34901,1.);
#10463=VECTOR('',#34902,1.);
#10464=VECTOR('',#34907,1.);
#10465=VECTOR('',#34910,1.);
#10466=VECTOR('',#34911,1.);
#10467=VECTOR('',#34918,1.);
#10468=VECTOR('',#34919,1.);
#10469=VECTOR('',#34920,1.);
#10470=VECTOR('',#34921,1.);
#10471=VECTOR('',#34926,1.);
#10472=VECTOR('',#34929,1.);
#10473=VECTOR('',#34930,1.);
#10474=VECTOR('',#34937,1.);
#10475=VECTOR('',#34938,1.);
#10476=VECTOR('',#34939,1.);
#10477=VECTOR('',#34940,1.);
#10478=VECTOR('',#34945,1.);
#10479=VECTOR('',#34948,1.);
#10480=VECTOR('',#34949,1.);
#10481=VECTOR('',#34956,1.);
#10482=VECTOR('',#34957,1.);
#10483=VECTOR('',#34958,1.);
#10484=VECTOR('',#34959,1.);
#10485=VECTOR('',#34964,1.);
#10486=VECTOR('',#34967,1.);
#10487=VECTOR('',#34968,1.);
#10488=VECTOR('',#34975,1.);
#10489=VECTOR('',#34976,1.);
#10490=VECTOR('',#34977,1.);
#10491=VECTOR('',#34978,1.);
#10492=VECTOR('',#34983,1.);
#10493=VECTOR('',#34986,1.);
#10494=VECTOR('',#34987,1.);
#10495=VECTOR('',#34994,1.);
#10496=VECTOR('',#34995,1.);
#10497=VECTOR('',#34996,1.);
#10498=VECTOR('',#34997,1.);
#10499=VECTOR('',#35002,1.);
#10500=VECTOR('',#35005,1.);
#10501=VECTOR('',#35006,1.);
#10502=VECTOR('',#35013,1.);
#10503=VECTOR('',#35014,1.);
#10504=VECTOR('',#35015,1.);
#10505=VECTOR('',#35016,1.);
#10506=VECTOR('',#35021,1.);
#10507=VECTOR('',#35024,1.);
#10508=VECTOR('',#35025,1.);
#10509=VECTOR('',#35032,1.);
#10510=VECTOR('',#35033,1.);
#10511=VECTOR('',#35034,1.);
#10512=VECTOR('',#35035,1.);
#10513=VECTOR('',#35040,1.);
#10514=VECTOR('',#35043,1.);
#10515=VECTOR('',#35044,1.);
#10516=VECTOR('',#35053,1.);
#10517=VECTOR('',#35054,1.);
#10518=VECTOR('',#35057,1.);
#10519=VECTOR('',#35058,1.);
#10520=VECTOR('',#35059,1.);
#10521=VECTOR('',#35062,1.);
#10522=VECTOR('',#35063,1.);
#10523=VECTOR('',#35070,1.);
#10524=VECTOR('',#35071,1.);
#10525=VECTOR('',#35072,1.);
#10526=VECTOR('',#35073,1.);
#10527=VECTOR('',#35078,1.);
#10528=VECTOR('',#35081,1.);
#10529=VECTOR('',#35082,1.);
#10530=VECTOR('',#35089,1.);
#10531=VECTOR('',#35090,1.);
#10532=VECTOR('',#35091,1.);
#10533=VECTOR('',#35092,1.);
#10534=VECTOR('',#35097,1.);
#10535=VECTOR('',#35100,1.);
#10536=VECTOR('',#35101,1.);
#10537=VECTOR('',#35108,1.);
#10538=VECTOR('',#35109,1.);
#10539=VECTOR('',#35110,1.);
#10540=VECTOR('',#35111,1.);
#10541=VECTOR('',#35116,1.);
#10542=VECTOR('',#35119,1.);
#10543=VECTOR('',#35120,1.);
#10544=VECTOR('',#35127,1.);
#10545=VECTOR('',#35128,1.);
#10546=VECTOR('',#35129,1.);
#10547=VECTOR('',#35130,1.);
#10548=VECTOR('',#35135,1.);
#10549=VECTOR('',#35138,1.);
#10550=VECTOR('',#35139,1.);
#10551=VECTOR('',#35146,1.);
#10552=VECTOR('',#35147,1.);
#10553=VECTOR('',#35148,1.);
#10554=VECTOR('',#35149,1.);
#10555=VECTOR('',#35154,1.);
#10556=VECTOR('',#35157,1.);
#10557=VECTOR('',#35158,1.);
#10558=VECTOR('',#35165,1.);
#10559=VECTOR('',#35166,1.);
#10560=VECTOR('',#35167,1.);
#10561=VECTOR('',#35168,1.);
#10562=VECTOR('',#35173,1.);
#10563=VECTOR('',#35176,1.);
#10564=VECTOR('',#35177,1.);
#10565=VECTOR('',#35184,1.);
#10566=VECTOR('',#35185,1.);
#10567=VECTOR('',#35186,1.);
#10568=VECTOR('',#35187,1.);
#10569=VECTOR('',#35192,1.);
#10570=VECTOR('',#35195,1.);
#10571=VECTOR('',#35196,1.);
#10572=VECTOR('',#35203,1.);
#10573=VECTOR('',#35204,1.);
#10574=VECTOR('',#35205,1.);
#10575=VECTOR('',#35206,1.);
#10576=VECTOR('',#35211,1.);
#10577=VECTOR('',#35214,1.);
#10578=VECTOR('',#35215,1.);
#10579=VECTOR('',#35222,1.);
#10580=VECTOR('',#35223,1.);
#10581=VECTOR('',#35224,1.);
#10582=VECTOR('',#35225,1.);
#10583=VECTOR('',#35230,1.);
#10584=VECTOR('',#35233,1.);
#10585=VECTOR('',#35234,1.);
#10586=VECTOR('',#35245,0.475);
#10587=VECTOR('',#35250,0.785);
#10588=VECTOR('',#35285,0.8);
#10589=VECTOR('',#35330,0.775);
#12654=VERTEX_POINT('',#69067);
#12655=VERTEX_POINT('',#69068);
#12656=VERTEX_POINT('',#69070);
#12657=VERTEX_POINT('',#69081);
#12658=VERTEX_POINT('',#69094);
#12659=VERTEX_POINT('',#69095);
#12660=VERTEX_POINT('',#69142);
#12661=VERTEX_POINT('',#69143);
#12662=VERTEX_POINT('',#69190);
#12663=VERTEX_POINT('',#69191);
#12664=VERTEX_POINT('',#69238);
#12665=VERTEX_POINT('',#69239);
#12666=VERTEX_POINT('',#69292);
#12667=VERTEX_POINT('',#69293);
#12668=VERTEX_POINT('',#69340);
#12669=VERTEX_POINT('',#69341);
#12670=VERTEX_POINT('',#69388);
#12671=VERTEX_POINT('',#69389);
#12672=VERTEX_POINT('',#69442);
#12673=VERTEX_POINT('',#69443);
#12674=VERTEX_POINT('',#69490);
#12675=VERTEX_POINT('',#69491);
#12676=VERTEX_POINT('',#69538);
#12677=VERTEX_POINT('',#69539);
#12678=VERTEX_POINT('',#69589);
#12679=VERTEX_POINT('',#69590);
#12680=VERTEX_POINT('',#69640);
#12681=VERTEX_POINT('',#69641);
#12682=VERTEX_POINT('',#69688);
#12683=VERTEX_POINT('',#69689);
#12684=VERTEX_POINT('',#69736);
#12685=VERTEX_POINT('',#69737);
#12686=VERTEX_POINT('',#69790);
#12687=VERTEX_POINT('',#69791);
#12688=VERTEX_POINT('',#69838);
#12689=VERTEX_POINT('',#69839);
#12690=VERTEX_POINT('',#69886);
#12691=VERTEX_POINT('',#69887);
#12692=VERTEX_POINT('',#69940);
#12693=VERTEX_POINT('',#69941);
#12694=VERTEX_POINT('',#69988);
#12695=VERTEX_POINT('',#69989);
#12696=VERTEX_POINT('',#70036);
#12697=VERTEX_POINT('',#70037);
#12698=VERTEX_POINT('',#70084);
#12699=VERTEX_POINT('',#70085);
#12700=VERTEX_POINT('',#70138);
#12701=VERTEX_POINT('',#70139);
#12702=VERTEX_POINT('',#70186);
#12703=VERTEX_POINT('',#70187);
#12704=VERTEX_POINT('',#70189);
#12705=VERTEX_POINT('',#70195);
#12706=VERTEX_POINT('',#70202);
#12707=VERTEX_POINT('',#70203);
#12708=VERTEX_POINT('',#70227);
#12709=VERTEX_POINT('',#70228);
#12710=VERTEX_POINT('',#70252);
#12711=VERTEX_POINT('',#70253);
#12712=VERTEX_POINT('',#70277);
#12713=VERTEX_POINT('',#70278);
#12714=VERTEX_POINT('',#70301);
#12715=VERTEX_POINT('',#70302);
#12716=VERTEX_POINT('',#70325);
#12717=VERTEX_POINT('',#70326);
#12718=VERTEX_POINT('',#70350);
#12719=VERTEX_POINT('',#70351);
#12720=VERTEX_POINT('',#70375);
#12721=VERTEX_POINT('',#70376);
#12722=VERTEX_POINT('',#70399);
#12723=VERTEX_POINT('',#70400);
#12724=VERTEX_POINT('',#70424);
#12725=VERTEX_POINT('',#70425);
#12726=VERTEX_POINT('',#70449);
#12727=VERTEX_POINT('',#70450);
#12728=VERTEX_POINT('',#70473);
#12729=VERTEX_POINT('',#70474);
#12730=VERTEX_POINT('',#70498);
#12731=VERTEX_POINT('',#70499);
#12732=VERTEX_POINT('',#70522);
#12733=VERTEX_POINT('',#70523);
#12734=VERTEX_POINT('',#70547);
#12735=VERTEX_POINT('',#70548);
#12736=VERTEX_POINT('',#70571);
#12737=VERTEX_POINT('',#70572);
#12738=VERTEX_POINT('',#70596);
#12739=VERTEX_POINT('',#70597);
#12740=VERTEX_POINT('',#70621);
#12741=VERTEX_POINT('',#70622);
#12742=VERTEX_POINT('',#70645);
#12743=VERTEX_POINT('',#70646);
#12744=VERTEX_POINT('',#70670);
#12745=VERTEX_POINT('',#70671);
#12746=VERTEX_POINT('',#70695);
#12747=VERTEX_POINT('',#70696);
#12748=VERTEX_POINT('',#70719);
#12749=VERTEX_POINT('',#70720);
#12750=VERTEX_POINT('',#70743);
#12751=VERTEX_POINT('',#70811);
#12752=VERTEX_POINT('',#70813);
#12753=VERTEX_POINT('',#71502);
#12754=VERTEX_POINT('',#71580);
#12755=VERTEX_POINT('',#71583);
#12756=VERTEX_POINT('',#72283);
#12757=VERTEX_POINT('',#72289);
#12758=VERTEX_POINT('',#72292);
#12759=VERTEX_POINT('',#72293);
#12760=VERTEX_POINT('',#72297);
#12761=VERTEX_POINT('',#72301);
#12762=VERTEX_POINT('',#72305);
#12763=VERTEX_POINT('',#72309);
#12764=VERTEX_POINT('',#72316);
#12765=VERTEX_POINT('',#72319);
#12766=VERTEX_POINT('',#72320);
#12767=VERTEX_POINT('',#72325);
#12768=VERTEX_POINT('',#72329);
#12769=VERTEX_POINT('',#72333);
#12770=VERTEX_POINT('',#72337);
#12771=VERTEX_POINT('',#72343);
#12772=VERTEX_POINT('',#72344);
#12773=VERTEX_POINT('',#72346);
#12774=VERTEX_POINT('',#72348);
#12775=VERTEX_POINT('',#72352);
#12776=VERTEX_POINT('',#72356);
#12777=VERTEX_POINT('',#72362);
#12778=VERTEX_POINT('',#72363);
#12779=VERTEX_POINT('',#72365);
#12780=VERTEX_POINT('',#72367);
#12781=VERTEX_POINT('',#72371);
#12782=VERTEX_POINT('',#72375);
#12783=VERTEX_POINT('',#72381);
#12784=VERTEX_POINT('',#72382);
#12785=VERTEX_POINT('',#72384);
#12786=VERTEX_POINT('',#72386);
#12787=VERTEX_POINT('',#72390);
#12788=VERTEX_POINT('',#72394);
#12789=VERTEX_POINT('',#72400);
#12790=VERTEX_POINT('',#72401);
#12791=VERTEX_POINT('',#72403);
#12792=VERTEX_POINT('',#72405);
#12793=VERTEX_POINT('',#72409);
#12794=VERTEX_POINT('',#72413);
#12795=VERTEX_POINT('',#72419);
#12796=VERTEX_POINT('',#72420);
#12797=VERTEX_POINT('',#72422);
#12798=VERTEX_POINT('',#72424);
#12799=VERTEX_POINT('',#72428);
#12800=VERTEX_POINT('',#72432);
#12801=VERTEX_POINT('',#72438);
#12802=VERTEX_POINT('',#72439);
#12803=VERTEX_POINT('',#72441);
#12804=VERTEX_POINT('',#72443);
#12805=VERTEX_POINT('',#72447);
#12806=VERTEX_POINT('',#72451);
#12807=VERTEX_POINT('',#72457);
#12808=VERTEX_POINT('',#72458);
#12809=VERTEX_POINT('',#72460);
#12810=VERTEX_POINT('',#72462);
#12811=VERTEX_POINT('',#72466);
#12812=VERTEX_POINT('',#72470);
#12813=VERTEX_POINT('',#72476);
#12814=VERTEX_POINT('',#72477);
#12815=VERTEX_POINT('',#72479);
#12816=VERTEX_POINT('',#72481);
#12817=VERTEX_POINT('',#72485);
#12818=VERTEX_POINT('',#72489);
#12819=VERTEX_POINT('',#72495);
#12820=VERTEX_POINT('',#72496);
#12821=VERTEX_POINT('',#72498);
#12822=VERTEX_POINT('',#72500);
#12823=VERTEX_POINT('',#72504);
#12824=VERTEX_POINT('',#72506);
#12825=VERTEX_POINT('',#72510);
#12826=VERTEX_POINT('',#72514);
#12827=VERTEX_POINT('',#72518);
#12828=VERTEX_POINT('',#72519);
#12829=VERTEX_POINT('',#72521);
#12830=VERTEX_POINT('',#72523);
#12831=VERTEX_POINT('',#72527);
#12832=VERTEX_POINT('',#72531);
#12833=VERTEX_POINT('',#72537);
#12834=VERTEX_POINT('',#72538);
#12835=VERTEX_POINT('',#72540);
#12836=VERTEX_POINT('',#72542);
#12837=VERTEX_POINT('',#72546);
#12838=VERTEX_POINT('',#72550);
#12839=VERTEX_POINT('',#72556);
#12840=VERTEX_POINT('',#72557);
#12841=VERTEX_POINT('',#72559);
#12842=VERTEX_POINT('',#72561);
#12843=VERTEX_POINT('',#72565);
#12844=VERTEX_POINT('',#72569);
#12845=VERTEX_POINT('',#72575);
#12846=VERTEX_POINT('',#72576);
#12847=VERTEX_POINT('',#72578);
#12848=VERTEX_POINT('',#72580);
#12849=VERTEX_POINT('',#72584);
#12850=VERTEX_POINT('',#72588);
#12851=VERTEX_POINT('',#72594);
#12852=VERTEX_POINT('',#72595);
#12853=VERTEX_POINT('',#72597);
#12854=VERTEX_POINT('',#72599);
#12855=VERTEX_POINT('',#72603);
#12856=VERTEX_POINT('',#72607);
#12857=VERTEX_POINT('',#72613);
#12858=VERTEX_POINT('',#72614);
#12859=VERTEX_POINT('',#72616);
#12860=VERTEX_POINT('',#72618);
#12861=VERTEX_POINT('',#72622);
#12862=VERTEX_POINT('',#72626);
#12863=VERTEX_POINT('',#72632);
#12864=VERTEX_POINT('',#72633);
#12865=VERTEX_POINT('',#72635);
#12866=VERTEX_POINT('',#72637);
#12867=VERTEX_POINT('',#72641);
#12868=VERTEX_POINT('',#72645);
#12869=VERTEX_POINT('',#72651);
#12870=VERTEX_POINT('',#72652);
#12871=VERTEX_POINT('',#72654);
#12872=VERTEX_POINT('',#72656);
#12873=VERTEX_POINT('',#72660);
#12874=VERTEX_POINT('',#72664);
#12875=VERTEX_POINT('',#72670);
#12876=VERTEX_POINT('',#72671);
#12877=VERTEX_POINT('',#72673);
#12878=VERTEX_POINT('',#72675);
#12879=VERTEX_POINT('',#72679);
#12880=VERTEX_POINT('',#72683);
#12881=VERTEX_POINT('',#72689);
#12882=VERTEX_POINT('',#72690);
#12883=VERTEX_POINT('',#72692);
#12884=VERTEX_POINT('',#72694);
#12885=VERTEX_POINT('',#72698);
#12886=VERTEX_POINT('',#72702);
#12887=VERTEX_POINT('',#72708);
#12888=VERTEX_POINT('',#72709);
#12889=VERTEX_POINT('',#72711);
#12890=VERTEX_POINT('',#72713);
#12891=VERTEX_POINT('',#72717);
#12892=VERTEX_POINT('',#72721);
#12893=VERTEX_POINT('',#72727);
#12894=VERTEX_POINT('',#72728);
#12895=VERTEX_POINT('',#72730);
#12896=VERTEX_POINT('',#72732);
#12897=VERTEX_POINT('',#72736);
#12898=VERTEX_POINT('',#72740);
#12899=VERTEX_POINT('',#72746);
#12900=VERTEX_POINT('',#72747);
#12901=VERTEX_POINT('',#72749);
#12902=VERTEX_POINT('',#72751);
#12903=VERTEX_POINT('',#72755);
#12904=VERTEX_POINT('',#72759);
#12905=VERTEX_POINT('',#72765);
#12906=VERTEX_POINT('',#72766);
#12907=VERTEX_POINT('',#72768);
#12908=VERTEX_POINT('',#72770);
#12909=VERTEX_POINT('',#72774);
#12910=VERTEX_POINT('',#72778);
#12911=VERTEX_POINT('',#72784);
#12912=VERTEX_POINT('',#72785);
#12913=VERTEX_POINT('',#72787);
#12914=VERTEX_POINT('',#72789);
#12915=VERTEX_POINT('',#72793);
#12916=VERTEX_POINT('',#72797);
#12917=VERTEX_POINT('',#72803);
#12918=VERTEX_POINT('',#72804);
#12919=VERTEX_POINT('',#72806);
#12920=VERTEX_POINT('',#72808);
#12921=VERTEX_POINT('',#72812);
#12922=VERTEX_POINT('',#72816);
#12923=VERTEX_POINT('',#72822);
#12924=VERTEX_POINT('',#72823);
#12925=VERTEX_POINT('',#72825);
#12926=VERTEX_POINT('',#72827);
#12927=VERTEX_POINT('',#72831);
#12928=VERTEX_POINT('',#72835);
#12929=VERTEX_POINT('',#72841);
#12930=VERTEX_POINT('',#72842);
#12931=VERTEX_POINT('',#72844);
#12932=VERTEX_POINT('',#72848);
#12933=VERTEX_POINT('',#72850);
#12934=VERTEX_POINT('',#72854);
#12935=VERTEX_POINT('',#72860);
#12936=VERTEX_POINT('',#72861);
#12937=VERTEX_POINT('',#72863);
#12938=VERTEX_POINT('',#72865);
#12939=VERTEX_POINT('',#72869);
#12940=VERTEX_POINT('',#72873);
#12941=VERTEX_POINT('',#72879);
#12942=VERTEX_POINT('',#72880);
#12943=VERTEX_POINT('',#72882);
#12944=VERTEX_POINT('',#72884);
#12945=VERTEX_POINT('',#72888);
#12946=VERTEX_POINT('',#72892);
#12947=VERTEX_POINT('',#72898);
#12948=VERTEX_POINT('',#72899);
#12949=VERTEX_POINT('',#72901);
#12950=VERTEX_POINT('',#72903);
#12951=VERTEX_POINT('',#72907);
#12952=VERTEX_POINT('',#72911);
#12953=VERTEX_POINT('',#72917);
#12954=VERTEX_POINT('',#72918);
#12955=VERTEX_POINT('',#72920);
#12956=VERTEX_POINT('',#72922);
#12957=VERTEX_POINT('',#72926);
#12958=VERTEX_POINT('',#72930);
#12959=VERTEX_POINT('',#72936);
#12960=VERTEX_POINT('',#72937);
#12961=VERTEX_POINT('',#72939);
#12962=VERTEX_POINT('',#72941);
#12963=VERTEX_POINT('',#72945);
#12964=VERTEX_POINT('',#72949);
#12965=VERTEX_POINT('',#72955);
#12966=VERTEX_POINT('',#72956);
#12967=VERTEX_POINT('',#72958);
#12968=VERTEX_POINT('',#72960);
#12969=VERTEX_POINT('',#72964);
#12970=VERTEX_POINT('',#72968);
#12971=VERTEX_POINT('',#72974);
#12972=VERTEX_POINT('',#72975);
#12973=VERTEX_POINT('',#72977);
#12974=VERTEX_POINT('',#72979);
#12975=VERTEX_POINT('',#72983);
#12976=VERTEX_POINT('',#72987);
#12977=VERTEX_POINT('',#72993);
#12978=VERTEX_POINT('',#72994);
#12979=VERTEX_POINT('',#72996);
#12980=VERTEX_POINT('',#72998);
#12981=VERTEX_POINT('',#73002);
#12982=VERTEX_POINT('',#73006);
#12983=VERTEX_POINT('',#73012);
#12984=VERTEX_POINT('',#73013);
#12985=VERTEX_POINT('',#73015);
#12986=VERTEX_POINT('',#73017);
#12987=VERTEX_POINT('',#73021);
#12988=VERTEX_POINT('',#73025);
#12989=VERTEX_POINT('',#73031);
#12990=VERTEX_POINT('',#73036);
#12991=VERTEX_POINT('',#73078);
#16105=EDGE_CURVE('',#12654,#12655,#8113,.T.);
#16106=EDGE_CURVE('',#12654,#12656,#814,.T.);
#16107=EDGE_CURVE('',#12656,#12657,#6332,.T.);
#16108=EDGE_CURVE('',#12657,#12655,#815,.T.);
#16109=EDGE_CURVE('',#12658,#12659,#8114,.T.);
#16110=EDGE_CURVE('',#12658,#12654,#816,.T.);
#16111=EDGE_CURVE('',#12655,#12659,#817,.T.);
#16112=EDGE_CURVE('',#12660,#12661,#8115,.T.);
#16113=EDGE_CURVE('',#12660,#12658,#818,.T.);
#16114=EDGE_CURVE('',#12659,#12661,#819,.T.);
#16115=EDGE_CURVE('',#12662,#12663,#8116,.T.);
#16116=EDGE_CURVE('',#12662,#12660,#820,.T.);
#16117=EDGE_CURVE('',#12661,#12663,#821,.T.);
#16118=EDGE_CURVE('',#12664,#12665,#8117,.T.);
#16119=EDGE_CURVE('',#12664,#12662,#822,.T.);
#16120=EDGE_CURVE('',#12663,#12665,#823,.T.);
#16121=EDGE_CURVE('',#12666,#12667,#8118,.T.);
#16122=EDGE_CURVE('',#12666,#12664,#824,.T.);
#16123=EDGE_CURVE('',#12665,#12667,#825,.T.);
#16124=EDGE_CURVE('',#12668,#12669,#8119,.T.);
#16125=EDGE_CURVE('',#12668,#12666,#826,.T.);
#16126=EDGE_CURVE('',#12667,#12669,#827,.T.);
#16127=EDGE_CURVE('',#12670,#12671,#8120,.T.);
#16128=EDGE_CURVE('',#12670,#12668,#828,.T.);
#16129=EDGE_CURVE('',#12669,#12671,#829,.T.);
#16130=EDGE_CURVE('',#12672,#12673,#8121,.T.);
#16131=EDGE_CURVE('',#12672,#12670,#830,.T.);
#16132=EDGE_CURVE('',#12671,#12673,#831,.T.);
#16133=EDGE_CURVE('',#12674,#12675,#8122,.T.);
#16134=EDGE_CURVE('',#12674,#12672,#832,.T.);
#16135=EDGE_CURVE('',#12673,#12675,#833,.T.);
#16136=EDGE_CURVE('',#12676,#12677,#8123,.T.);
#16137=EDGE_CURVE('',#12676,#12674,#834,.T.);
#16138=EDGE_CURVE('',#12675,#12677,#835,.T.);
#16139=EDGE_CURVE('',#12678,#12679,#8124,.T.);
#16140=EDGE_CURVE('',#12678,#12676,#836,.T.);
#16141=EDGE_CURVE('',#12677,#12679,#837,.T.);
#16142=EDGE_CURVE('',#12680,#12681,#8125,.T.);
#16143=EDGE_CURVE('',#12680,#12678,#838,.T.);
#16144=EDGE_CURVE('',#12679,#12681,#839,.T.);
#16145=EDGE_CURVE('',#12682,#12683,#8126,.T.);
#16146=EDGE_CURVE('',#12682,#12680,#840,.T.);
#16147=EDGE_CURVE('',#12681,#12683,#841,.T.);
#16148=EDGE_CURVE('',#12684,#12685,#8127,.T.);
#16149=EDGE_CURVE('',#12684,#12682,#842,.T.);
#16150=EDGE_CURVE('',#12683,#12685,#843,.T.);
#16151=EDGE_CURVE('',#12686,#12687,#8128,.T.);
#16152=EDGE_CURVE('',#12686,#12684,#844,.T.);
#16153=EDGE_CURVE('',#12685,#12687,#845,.T.);
#16154=EDGE_CURVE('',#12688,#12689,#8129,.T.);
#16155=EDGE_CURVE('',#12688,#12686,#846,.T.);
#16156=EDGE_CURVE('',#12687,#12689,#847,.T.);
#16157=EDGE_CURVE('',#12690,#12691,#8130,.T.);
#16158=EDGE_CURVE('',#12690,#12688,#848,.T.);
#16159=EDGE_CURVE('',#12689,#12691,#849,.T.);
#16160=EDGE_CURVE('',#12692,#12693,#8131,.T.);
#16161=EDGE_CURVE('',#12692,#12690,#850,.T.);
#16162=EDGE_CURVE('',#12691,#12693,#851,.T.);
#16163=EDGE_CURVE('',#12694,#12695,#8132,.T.);
#16164=EDGE_CURVE('',#12694,#12692,#852,.T.);
#16165=EDGE_CURVE('',#12693,#12695,#853,.T.);
#16166=EDGE_CURVE('',#12696,#12697,#8133,.T.);
#16167=EDGE_CURVE('',#12696,#12694,#854,.T.);
#16168=EDGE_CURVE('',#12695,#12697,#855,.T.);
#16169=EDGE_CURVE('',#12698,#12699,#8134,.T.);
#16170=EDGE_CURVE('',#12698,#12696,#856,.T.);
#16171=EDGE_CURVE('',#12697,#12699,#857,.T.);
#16172=EDGE_CURVE('',#12700,#12701,#8135,.T.);
#16173=EDGE_CURVE('',#12700,#12698,#858,.T.);
#16174=EDGE_CURVE('',#12699,#12701,#859,.T.);
#16175=EDGE_CURVE('',#12702,#12703,#8136,.T.);
#16176=EDGE_CURVE('',#12702,#12704,#860,.T.);
#16177=EDGE_CURVE('',#12705,#12704,#6333,.T.);
#16178=EDGE_CURVE('',#12703,#12705,#861,.T.);
#16179=EDGE_CURVE('',#12706,#12707,#8137,.T.);
#16180=EDGE_CURVE('',#12706,#12702,#862,.T.);
#16181=EDGE_CURVE('',#12707,#12703,#863,.T.);
#16182=EDGE_CURVE('',#12708,#12709,#8138,.T.);
#16183=EDGE_CURVE('',#12708,#12706,#864,.T.);
#16184=EDGE_CURVE('',#12709,#12707,#865,.T.);
#16185=EDGE_CURVE('',#12710,#12711,#8139,.T.);
#16186=EDGE_CURVE('',#12710,#12708,#866,.T.);
#16187=EDGE_CURVE('',#12711,#12709,#867,.T.);
#16188=EDGE_CURVE('',#12712,#12713,#8140,.T.);
#16189=EDGE_CURVE('',#12712,#12710,#868,.T.);
#16190=EDGE_CURVE('',#12713,#12711,#869,.T.);
#16191=EDGE_CURVE('',#12714,#12715,#8141,.T.);
#16192=EDGE_CURVE('',#12714,#12712,#870,.T.);
#16193=EDGE_CURVE('',#12715,#12713,#871,.T.);
#16194=EDGE_CURVE('',#12716,#12717,#8142,.T.);
#16195=EDGE_CURVE('',#12716,#12714,#872,.T.);
#16196=EDGE_CURVE('',#12717,#12715,#873,.T.);
#16197=EDGE_CURVE('',#12718,#12719,#8143,.T.);
#16198=EDGE_CURVE('',#12718,#12716,#874,.T.);
#16199=EDGE_CURVE('',#12719,#12717,#875,.T.);
#16200=EDGE_CURVE('',#12720,#12721,#8144,.T.);
#16201=EDGE_CURVE('',#12720,#12718,#876,.T.);
#16202=EDGE_CURVE('',#12721,#12719,#877,.T.);
#16203=EDGE_CURVE('',#12722,#12723,#8145,.T.);
#16204=EDGE_CURVE('',#12722,#12720,#878,.T.);
#16205=EDGE_CURVE('',#12723,#12721,#879,.T.);
#16206=EDGE_CURVE('',#12724,#12725,#8146,.T.);
#16207=EDGE_CURVE('',#12724,#12722,#880,.T.);
#16208=EDGE_CURVE('',#12725,#12723,#881,.T.);
#16209=EDGE_CURVE('',#12726,#12727,#8147,.T.);
#16210=EDGE_CURVE('',#12726,#12724,#882,.T.);
#16211=EDGE_CURVE('',#12727,#12725,#883,.T.);
#16212=EDGE_CURVE('',#12728,#12729,#8148,.T.);
#16213=EDGE_CURVE('',#12728,#12726,#884,.T.);
#16214=EDGE_CURVE('',#12729,#12727,#885,.T.);
#16215=EDGE_CURVE('',#12730,#12731,#8149,.T.);
#16216=EDGE_CURVE('',#12730,#12728,#886,.T.);
#16217=EDGE_CURVE('',#12731,#12729,#887,.T.);
#16218=EDGE_CURVE('',#12732,#12733,#8150,.T.);
#16219=EDGE_CURVE('',#12732,#12730,#888,.T.);
#16220=EDGE_CURVE('',#12733,#12731,#889,.T.);
#16221=EDGE_CURVE('',#12734,#12735,#8151,.T.);
#16222=EDGE_CURVE('',#12734,#12732,#890,.T.);
#16223=EDGE_CURVE('',#12735,#12733,#891,.T.);
#16224=EDGE_CURVE('',#12736,#12737,#8152,.T.);
#16225=EDGE_CURVE('',#12736,#12734,#892,.T.);
#16226=EDGE_CURVE('',#12737,#12735,#893,.T.);
#16227=EDGE_CURVE('',#12738,#12739,#8153,.T.);
#16228=EDGE_CURVE('',#12738,#12736,#894,.T.);
#16229=EDGE_CURVE('',#12739,#12737,#895,.T.);
#16230=EDGE_CURVE('',#12740,#12741,#8154,.T.);
#16231=EDGE_CURVE('',#12740,#12738,#896,.T.);
#16232=EDGE_CURVE('',#12741,#12739,#897,.T.);
#16233=EDGE_CURVE('',#12742,#12743,#8155,.T.);
#16234=EDGE_CURVE('',#12742,#12740,#898,.T.);
#16235=EDGE_CURVE('',#12743,#12741,#899,.T.);
#16236=EDGE_CURVE('',#12744,#12745,#8156,.T.);
#16237=EDGE_CURVE('',#12744,#12742,#900,.T.);
#16238=EDGE_CURVE('',#12745,#12743,#901,.T.);
#16239=EDGE_CURVE('',#12746,#12747,#8157,.T.);
#16240=EDGE_CURVE('',#12746,#12744,#902,.T.);
#16241=EDGE_CURVE('',#12747,#12745,#903,.T.);
#16242=EDGE_CURVE('',#12748,#12749,#8158,.T.);
#16243=EDGE_CURVE('',#12748,#12746,#904,.T.);
#16244=EDGE_CURVE('',#12749,#12747,#905,.T.);
#16245=EDGE_CURVE('',#12704,#12750,#906,.T.);
#16246=EDGE_CURVE('',#12751,#12750,#6334,.T.);
#16247=EDGE_CURVE('',#12752,#12751,#6335,.T.);
#16248=EDGE_CURVE('',#12752,#12705,#907,.T.);
#16249=EDGE_CURVE('',#12701,#12752,#908,.T.);
#16250=EDGE_CURVE('',#12753,#12657,#909,.T.);
#16251=EDGE_CURVE('',#12753,#12749,#910,.T.);
#16252=EDGE_CURVE('',#12657,#12754,#6336,.T.);
#16253=EDGE_CURVE('',#12754,#12656,#6337,.T.);
#16254=EDGE_CURVE('',#12656,#12755,#911,.T.);
#16255=EDGE_CURVE('',#12755,#12753,#6338,.T.);
#16256=EDGE_CURVE('',#12755,#12748,#912,.T.);
#16257=EDGE_CURVE('',#12750,#12700,#913,.T.);
#16258=EDGE_CURVE('',#12751,#12756,#6339,.T.);
#16259=EDGE_CURVE('',#12756,#12756,#6340,.T.);
#16260=EDGE_CURVE('',#12750,#12752,#6341,.T.);
#16261=EDGE_CURVE('',#12757,#12757,#6342,.T.);
#16262=EDGE_CURVE('',#12758,#12759,#8159,.T.);
#16263=EDGE_CURVE('',#12759,#12758,#6343,.T.);
#16264=EDGE_CURVE('',#12759,#12760,#8160,.T.);
#16265=EDGE_CURVE('',#12760,#12759,#6344,.T.);
#16266=EDGE_CURVE('',#12760,#12761,#8161,.T.);
#16267=EDGE_CURVE('',#12761,#12760,#6345,.T.);
#16268=EDGE_CURVE('',#12761,#12762,#8162,.T.);
#16269=EDGE_CURVE('',#12762,#12761,#6346,.T.);
#16270=EDGE_CURVE('',#12762,#12763,#8163,.T.);
#16271=EDGE_CURVE('',#12763,#12762,#6347,.T.);
#16272=EDGE_CURVE('',#12763,#12758,#8164,.T.);
#16273=EDGE_CURVE('',#12758,#12763,#6348,.T.);
#16274=EDGE_CURVE('',#12764,#12762,#8165,.T.);
#16275=EDGE_CURVE('',#12765,#12766,#8166,.T.);
#16276=EDGE_CURVE('',#12765,#12758,#8167,.T.);
#16277=EDGE_CURVE('',#12766,#12759,#8168,.T.);
#16278=EDGE_CURVE('',#12767,#12765,#8169,.T.);
#16279=EDGE_CURVE('',#12767,#12763,#8170,.T.);
#16280=EDGE_CURVE('',#12768,#12767,#8171,.T.);
#16281=EDGE_CURVE('',#12768,#12762,#8172,.T.);
#16282=EDGE_CURVE('',#12769,#12768,#8173,.T.);
#16283=EDGE_CURVE('',#12769,#12761,#8174,.T.);
#16284=EDGE_CURVE('',#12770,#12769,#8175,.T.);
#16285=EDGE_CURVE('',#12770,#12760,#8176,.T.);
#16286=EDGE_CURVE('',#12766,#12770,#8177,.T.);
#16287=EDGE_CURVE('',#12771,#12772,#8178,.T.);
#16288=EDGE_CURVE('',#12771,#12773,#8179,.T.);
#16289=EDGE_CURVE('',#12774,#12773,#8180,.T.);
#16290=EDGE_CURVE('',#12772,#12774,#8181,.T.);
#16291=EDGE_CURVE('',#12772,#12775,#6349,.T.);
#16292=EDGE_CURVE('',#12774,#12775,#8182,.T.);
#16293=EDGE_CURVE('',#12775,#12776,#8183,.T.);
#16294=EDGE_CURVE('',#12773,#12776,#8184,.T.);
#16295=EDGE_CURVE('',#12776,#12771,#6350,.T.);
#16296=EDGE_CURVE('',#12777,#12778,#8185,.T.);
#16297=EDGE_CURVE('',#12777,#12779,#8186,.T.);
#16298=EDGE_CURVE('',#12780,#12779,#8187,.T.);
#16299=EDGE_CURVE('',#12778,#12780,#8188,.T.);
#16300=EDGE_CURVE('',#12778,#12781,#6351,.T.);
#16301=EDGE_CURVE('',#12780,#12781,#8189,.T.);
#16302=EDGE_CURVE('',#12781,#12782,#8190,.T.);
#16303=EDGE_CURVE('',#12779,#12782,#8191,.T.);
#16304=EDGE_CURVE('',#12782,#12777,#6352,.T.);
#16305=EDGE_CURVE('',#12783,#12784,#8192,.T.);
#16306=EDGE_CURVE('',#12783,#12785,#8193,.T.);
#16307=EDGE_CURVE('',#12786,#12785,#8194,.T.);
#16308=EDGE_CURVE('',#12784,#12786,#8195,.T.);
#16309=EDGE_CURVE('',#12784,#12787,#6353,.T.);
#16310=EDGE_CURVE('',#12786,#12787,#8196,.T.);
#16311=EDGE_CURVE('',#12787,#12788,#8197,.T.);
#16312=EDGE_CURVE('',#12785,#12788,#8198,.T.);
#16313=EDGE_CURVE('',#12788,#12783,#6354,.T.);
#16314=EDGE_CURVE('',#12789,#12790,#8199,.T.);
#16315=EDGE_CURVE('',#12789,#12791,#8200,.T.);
#16316=EDGE_CURVE('',#12792,#12791,#8201,.T.);
#16317=EDGE_CURVE('',#12790,#12792,#8202,.T.);
#16318=EDGE_CURVE('',#12790,#12793,#6355,.T.);
#16319=EDGE_CURVE('',#12792,#12793,#8203,.T.);
#16320=EDGE_CURVE('',#12793,#12794,#8204,.T.);
#16321=EDGE_CURVE('',#12791,#12794,#8205,.T.);
#16322=EDGE_CURVE('',#12794,#12789,#6356,.T.);
#16323=EDGE_CURVE('',#12795,#12796,#8206,.T.);
#16324=EDGE_CURVE('',#12795,#12797,#8207,.T.);
#16325=EDGE_CURVE('',#12798,#12797,#8208,.T.);
#16326=EDGE_CURVE('',#12796,#12798,#8209,.T.);
#16327=EDGE_CURVE('',#12796,#12799,#6357,.T.);
#16328=EDGE_CURVE('',#12798,#12799,#8210,.T.);
#16329=EDGE_CURVE('',#12799,#12800,#8211,.T.);
#16330=EDGE_CURVE('',#12797,#12800,#8212,.T.);
#16331=EDGE_CURVE('',#12800,#12795,#6358,.T.);
#16332=EDGE_CURVE('',#12801,#12802,#8213,.T.);
#16333=EDGE_CURVE('',#12801,#12803,#8214,.T.);
#16334=EDGE_CURVE('',#12804,#12803,#8215,.T.);
#16335=EDGE_CURVE('',#12802,#12804,#8216,.T.);
#16336=EDGE_CURVE('',#12802,#12805,#6359,.T.);
#16337=EDGE_CURVE('',#12804,#12805,#8217,.T.);
#16338=EDGE_CURVE('',#12805,#12806,#8218,.T.);
#16339=EDGE_CURVE('',#12803,#12806,#8219,.T.);
#16340=EDGE_CURVE('',#12806,#12801,#6360,.T.);
#16341=EDGE_CURVE('',#12807,#12808,#8220,.T.);
#16342=EDGE_CURVE('',#12807,#12809,#8221,.T.);
#16343=EDGE_CURVE('',#12810,#12809,#8222,.T.);
#16344=EDGE_CURVE('',#12808,#12810,#8223,.T.);
#16345=EDGE_CURVE('',#12808,#12811,#6361,.T.);
#16346=EDGE_CURVE('',#12810,#12811,#8224,.T.);
#16347=EDGE_CURVE('',#12811,#12812,#8225,.T.);
#16348=EDGE_CURVE('',#12809,#12812,#8226,.T.);
#16349=EDGE_CURVE('',#12812,#12807,#6362,.T.);
#16350=EDGE_CURVE('',#12813,#12814,#8227,.T.);
#16351=EDGE_CURVE('',#12813,#12815,#8228,.T.);
#16352=EDGE_CURVE('',#12816,#12815,#8229,.T.);
#16353=EDGE_CURVE('',#12814,#12816,#8230,.T.);
#16354=EDGE_CURVE('',#12814,#12817,#6363,.T.);
#16355=EDGE_CURVE('',#12816,#12817,#8231,.T.);
#16356=EDGE_CURVE('',#12817,#12818,#8232,.T.);
#16357=EDGE_CURVE('',#12815,#12818,#8233,.T.);
#16358=EDGE_CURVE('',#12818,#12813,#6364,.T.);
#16359=EDGE_CURVE('',#12819,#12820,#8234,.T.);
#16360=EDGE_CURVE('',#12819,#12821,#8235,.T.);
#16361=EDGE_CURVE('',#12822,#12821,#8236,.T.);
#16362=EDGE_CURVE('',#12820,#12822,#8237,.T.);
#16363=EDGE_CURVE('',#12820,#12823,#6365,.T.);
#16364=EDGE_CURVE('',#12822,#12824,#8238,.T.);
#16365=EDGE_CURVE('',#12823,#12824,#6366,.T.);
#16366=EDGE_CURVE('',#12824,#12825,#8239,.T.);
#16367=EDGE_CURVE('',#12821,#12825,#8240,.T.);
#16368=EDGE_CURVE('',#12825,#12826,#6367,.T.);
#16369=EDGE_CURVE('',#12826,#12819,#6368,.T.);
#16370=EDGE_CURVE('',#12827,#12828,#8241,.T.);
#16371=EDGE_CURVE('',#12827,#12829,#8242,.T.);
#16372=EDGE_CURVE('',#12830,#12829,#8243,.T.);
#16373=EDGE_CURVE('',#12828,#12830,#8244,.T.);
#16374=EDGE_CURVE('',#12828,#12831,#6369,.T.);
#16375=EDGE_CURVE('',#12830,#12831,#8245,.T.);
#16376=EDGE_CURVE('',#12831,#12832,#8246,.T.);
#16377=EDGE_CURVE('',#12829,#12832,#8247,.T.);
#16378=EDGE_CURVE('',#12832,#12827,#6370,.T.);
#16379=EDGE_CURVE('',#12833,#12834,#8248,.T.);
#16380=EDGE_CURVE('',#12833,#12835,#8249,.T.);
#16381=EDGE_CURVE('',#12836,#12835,#8250,.T.);
#16382=EDGE_CURVE('',#12834,#12836,#8251,.T.);
#16383=EDGE_CURVE('',#12834,#12837,#6371,.T.);
#16384=EDGE_CURVE('',#12836,#12837,#8252,.T.);
#16385=EDGE_CURVE('',#12837,#12838,#8253,.T.);
#16386=EDGE_CURVE('',#12835,#12838,#8254,.T.);
#16387=EDGE_CURVE('',#12838,#12833,#6372,.T.);
#16388=EDGE_CURVE('',#12839,#12840,#8255,.T.);
#16389=EDGE_CURVE('',#12839,#12841,#8256,.T.);
#16390=EDGE_CURVE('',#12842,#12841,#8257,.T.);
#16391=EDGE_CURVE('',#12840,#12842,#8258,.T.);
#16392=EDGE_CURVE('',#12840,#12843,#6373,.T.);
#16393=EDGE_CURVE('',#12842,#12843,#8259,.T.);
#16394=EDGE_CURVE('',#12843,#12844,#8260,.T.);
#16395=EDGE_CURVE('',#12841,#12844,#8261,.T.);
#16396=EDGE_CURVE('',#12844,#12839,#6374,.T.);
#16397=EDGE_CURVE('',#12845,#12846,#8262,.T.);
#16398=EDGE_CURVE('',#12845,#12847,#8263,.T.);
#16399=EDGE_CURVE('',#12848,#12847,#8264,.T.);
#16400=EDGE_CURVE('',#12846,#12848,#8265,.T.);
#16401=EDGE_CURVE('',#12846,#12849,#6375,.T.);
#16402=EDGE_CURVE('',#12848,#12849,#8266,.T.);
#16403=EDGE_CURVE('',#12849,#12850,#8267,.T.);
#16404=EDGE_CURVE('',#12847,#12850,#8268,.T.);
#16405=EDGE_CURVE('',#12850,#12845,#6376,.T.);
#16406=EDGE_CURVE('',#12851,#12852,#8269,.T.);
#16407=EDGE_CURVE('',#12851,#12853,#8270,.T.);
#16408=EDGE_CURVE('',#12854,#12853,#8271,.T.);
#16409=EDGE_CURVE('',#12852,#12854,#8272,.T.);
#16410=EDGE_CURVE('',#12852,#12855,#6377,.T.);
#16411=EDGE_CURVE('',#12854,#12855,#8273,.T.);
#16412=EDGE_CURVE('',#12855,#12856,#8274,.T.);
#16413=EDGE_CURVE('',#12853,#12856,#8275,.T.);
#16414=EDGE_CURVE('',#12856,#12851,#6378,.T.);
#16415=EDGE_CURVE('',#12857,#12858,#8276,.T.);
#16416=EDGE_CURVE('',#12857,#12859,#8277,.T.);
#16417=EDGE_CURVE('',#12860,#12859,#8278,.T.);
#16418=EDGE_CURVE('',#12858,#12860,#8279,.T.);
#16419=EDGE_CURVE('',#12858,#12861,#6379,.T.);
#16420=EDGE_CURVE('',#12860,#12861,#8280,.T.);
#16421=EDGE_CURVE('',#12861,#12862,#8281,.T.);
#16422=EDGE_CURVE('',#12859,#12862,#8282,.T.);
#16423=EDGE_CURVE('',#12862,#12857,#6380,.T.);
#16424=EDGE_CURVE('',#12863,#12864,#8283,.T.);
#16425=EDGE_CURVE('',#12863,#12865,#8284,.T.);
#16426=EDGE_CURVE('',#12866,#12865,#8285,.T.);
#16427=EDGE_CURVE('',#12864,#12866,#8286,.T.);
#16428=EDGE_CURVE('',#12864,#12867,#6381,.T.);
#16429=EDGE_CURVE('',#12866,#12867,#8287,.T.);
#16430=EDGE_CURVE('',#12867,#12868,#8288,.T.);
#16431=EDGE_CURVE('',#12865,#12868,#8289,.T.);
#16432=EDGE_CURVE('',#12868,#12863,#6382,.T.);
#16433=EDGE_CURVE('',#12869,#12870,#8290,.T.);
#16434=EDGE_CURVE('',#12869,#12871,#8291,.T.);
#16435=EDGE_CURVE('',#12872,#12871,#8292,.T.);
#16436=EDGE_CURVE('',#12870,#12872,#8293,.T.);
#16437=EDGE_CURVE('',#12870,#12873,#6383,.T.);
#16438=EDGE_CURVE('',#12872,#12873,#8294,.T.);
#16439=EDGE_CURVE('',#12873,#12874,#8295,.T.);
#16440=EDGE_CURVE('',#12871,#12874,#8296,.T.);
#16441=EDGE_CURVE('',#12874,#12869,#6384,.T.);
#16442=EDGE_CURVE('',#12875,#12876,#8297,.T.);
#16443=EDGE_CURVE('',#12875,#12877,#8298,.T.);
#16444=EDGE_CURVE('',#12878,#12877,#8299,.T.);
#16445=EDGE_CURVE('',#12876,#12878,#8300,.T.);
#16446=EDGE_CURVE('',#12876,#12879,#6385,.T.);
#16447=EDGE_CURVE('',#12878,#12879,#8301,.T.);
#16448=EDGE_CURVE('',#12879,#12880,#8302,.T.);
#16449=EDGE_CURVE('',#12877,#12880,#8303,.T.);
#16450=EDGE_CURVE('',#12880,#12875,#6386,.T.);
#16451=EDGE_CURVE('',#12881,#12882,#8304,.T.);
#16452=EDGE_CURVE('',#12881,#12883,#8305,.T.);
#16453=EDGE_CURVE('',#12884,#12883,#8306,.T.);
#16454=EDGE_CURVE('',#12882,#12884,#8307,.T.);
#16455=EDGE_CURVE('',#12882,#12885,#6387,.T.);
#16456=EDGE_CURVE('',#12884,#12885,#8308,.T.);
#16457=EDGE_CURVE('',#12885,#12886,#8309,.T.);
#16458=EDGE_CURVE('',#12883,#12886,#8310,.T.);
#16459=EDGE_CURVE('',#12886,#12881,#6388,.T.);
#16460=EDGE_CURVE('',#12887,#12888,#8311,.T.);
#16461=EDGE_CURVE('',#12887,#12889,#8312,.T.);
#16462=EDGE_CURVE('',#12890,#12889,#8313,.T.);
#16463=EDGE_CURVE('',#12888,#12890,#8314,.T.);
#16464=EDGE_CURVE('',#12888,#12891,#6389,.T.);
#16465=EDGE_CURVE('',#12890,#12891,#8315,.T.);
#16466=EDGE_CURVE('',#12891,#12892,#8316,.T.);
#16467=EDGE_CURVE('',#12889,#12892,#8317,.T.);
#16468=EDGE_CURVE('',#12892,#12887,#6390,.T.);
#16469=EDGE_CURVE('',#12893,#12894,#8318,.T.);
#16470=EDGE_CURVE('',#12893,#12895,#8319,.T.);
#16471=EDGE_CURVE('',#12896,#12895,#8320,.T.);
#16472=EDGE_CURVE('',#12894,#12896,#8321,.T.);
#16473=EDGE_CURVE('',#12894,#12897,#6391,.T.);
#16474=EDGE_CURVE('',#12896,#12897,#8322,.T.);
#16475=EDGE_CURVE('',#12897,#12898,#8323,.T.);
#16476=EDGE_CURVE('',#12895,#12898,#8324,.T.);
#16477=EDGE_CURVE('',#12898,#12893,#6392,.T.);
#16478=EDGE_CURVE('',#12899,#12900,#8325,.T.);
#16479=EDGE_CURVE('',#12899,#12901,#8326,.T.);
#16480=EDGE_CURVE('',#12902,#12901,#8327,.T.);
#16481=EDGE_CURVE('',#12900,#12902,#8328,.T.);
#16482=EDGE_CURVE('',#12900,#12903,#6393,.T.);
#16483=EDGE_CURVE('',#12902,#12903,#8329,.T.);
#16484=EDGE_CURVE('',#12903,#12904,#8330,.T.);
#16485=EDGE_CURVE('',#12901,#12904,#8331,.T.);
#16486=EDGE_CURVE('',#12904,#12899,#6394,.T.);
#16487=EDGE_CURVE('',#12905,#12906,#8332,.T.);
#16488=EDGE_CURVE('',#12905,#12907,#8333,.T.);
#16489=EDGE_CURVE('',#12908,#12907,#8334,.T.);
#16490=EDGE_CURVE('',#12906,#12908,#8335,.T.);
#16491=EDGE_CURVE('',#12906,#12909,#6395,.T.);
#16492=EDGE_CURVE('',#12908,#12909,#8336,.T.);
#16493=EDGE_CURVE('',#12909,#12910,#8337,.T.);
#16494=EDGE_CURVE('',#12907,#12910,#8338,.T.);
#16495=EDGE_CURVE('',#12910,#12905,#6396,.T.);
#16496=EDGE_CURVE('',#12911,#12912,#8339,.T.);
#16497=EDGE_CURVE('',#12911,#12913,#8340,.T.);
#16498=EDGE_CURVE('',#12914,#12913,#8341,.T.);
#16499=EDGE_CURVE('',#12912,#12914,#8342,.T.);
#16500=EDGE_CURVE('',#12912,#12915,#6397,.T.);
#16501=EDGE_CURVE('',#12914,#12915,#8343,.T.);
#16502=EDGE_CURVE('',#12915,#12916,#8344,.T.);
#16503=EDGE_CURVE('',#12913,#12916,#8345,.T.);
#16504=EDGE_CURVE('',#12916,#12911,#6398,.T.);
#16505=EDGE_CURVE('',#12917,#12918,#8346,.T.);
#16506=EDGE_CURVE('',#12917,#12919,#8347,.T.);
#16507=EDGE_CURVE('',#12920,#12919,#8348,.T.);
#16508=EDGE_CURVE('',#12918,#12920,#8349,.T.);
#16509=EDGE_CURVE('',#12918,#12921,#6399,.T.);
#16510=EDGE_CURVE('',#12920,#12921,#8350,.T.);
#16511=EDGE_CURVE('',#12921,#12922,#8351,.T.);
#16512=EDGE_CURVE('',#12919,#12922,#8352,.T.);
#16513=EDGE_CURVE('',#12922,#12917,#6400,.T.);
#16514=EDGE_CURVE('',#12923,#12924,#8353,.T.);
#16515=EDGE_CURVE('',#12923,#12925,#8354,.T.);
#16516=EDGE_CURVE('',#12926,#12925,#8355,.T.);
#16517=EDGE_CURVE('',#12924,#12926,#8356,.T.);
#16518=EDGE_CURVE('',#12924,#12927,#6401,.T.);
#16519=EDGE_CURVE('',#12926,#12927,#8357,.T.);
#16520=EDGE_CURVE('',#12927,#12928,#8358,.T.);
#16521=EDGE_CURVE('',#12925,#12928,#8359,.T.);
#16522=EDGE_CURVE('',#12928,#12923,#6402,.T.);
#16523=EDGE_CURVE('',#12929,#12930,#6403,.T.);
#16524=EDGE_CURVE('',#12929,#12931,#8360,.T.);
#16525=EDGE_CURVE('',#12931,#12930,#8361,.T.);
#16526=EDGE_CURVE('',#12932,#12929,#8362,.T.);
#16527=EDGE_CURVE('',#12932,#12933,#8363,.T.);
#16528=EDGE_CURVE('',#12931,#12933,#8364,.T.);
#16529=EDGE_CURVE('',#12930,#12934,#8365,.T.);
#16530=EDGE_CURVE('',#12933,#12934,#8366,.T.);
#16531=EDGE_CURVE('',#12934,#12932,#6404,.T.);
#16532=EDGE_CURVE('',#12935,#12936,#8367,.T.);
#16533=EDGE_CURVE('',#12935,#12937,#8368,.T.);
#16534=EDGE_CURVE('',#12938,#12937,#8369,.T.);
#16535=EDGE_CURVE('',#12936,#12938,#8370,.T.);
#16536=EDGE_CURVE('',#12936,#12939,#6405,.T.);
#16537=EDGE_CURVE('',#12938,#12939,#8371,.T.);
#16538=EDGE_CURVE('',#12939,#12940,#8372,.T.);
#16539=EDGE_CURVE('',#12937,#12940,#8373,.T.);
#16540=EDGE_CURVE('',#12940,#12935,#6406,.T.);
#16541=EDGE_CURVE('',#12941,#12942,#8374,.T.);
#16542=EDGE_CURVE('',#12941,#12943,#8375,.T.);
#16543=EDGE_CURVE('',#12944,#12943,#8376,.T.);
#16544=EDGE_CURVE('',#12942,#12944,#8377,.T.);
#16545=EDGE_CURVE('',#12942,#12945,#6407,.T.);
#16546=EDGE_CURVE('',#12944,#12945,#8378,.T.);
#16547=EDGE_CURVE('',#12945,#12946,#8379,.T.);
#16548=EDGE_CURVE('',#12943,#12946,#8380,.T.);
#16549=EDGE_CURVE('',#12946,#12941,#6408,.T.);
#16550=EDGE_CURVE('',#12947,#12948,#8381,.T.);
#16551=EDGE_CURVE('',#12947,#12949,#8382,.T.);
#16552=EDGE_CURVE('',#12950,#12949,#8383,.T.);
#16553=EDGE_CURVE('',#12948,#12950,#8384,.T.);
#16554=EDGE_CURVE('',#12948,#12951,#6409,.T.);
#16555=EDGE_CURVE('',#12950,#12951,#8385,.T.);
#16556=EDGE_CURVE('',#12951,#12952,#8386,.T.);
#16557=EDGE_CURVE('',#12949,#12952,#8387,.T.);
#16558=EDGE_CURVE('',#12952,#12947,#6410,.T.);
#16559=EDGE_CURVE('',#12953,#12954,#8388,.T.);
#16560=EDGE_CURVE('',#12953,#12955,#8389,.T.);
#16561=EDGE_CURVE('',#12956,#12955,#8390,.T.);
#16562=EDGE_CURVE('',#12954,#12956,#8391,.T.);
#16563=EDGE_CURVE('',#12954,#12957,#6411,.T.);
#16564=EDGE_CURVE('',#12956,#12957,#8392,.T.);
#16565=EDGE_CURVE('',#12957,#12958,#8393,.T.);
#16566=EDGE_CURVE('',#12955,#12958,#8394,.T.);
#16567=EDGE_CURVE('',#12958,#12953,#6412,.T.);
#16568=EDGE_CURVE('',#12959,#12960,#8395,.T.);
#16569=EDGE_CURVE('',#12959,#12961,#8396,.T.);
#16570=EDGE_CURVE('',#12962,#12961,#8397,.T.);
#16571=EDGE_CURVE('',#12960,#12962,#8398,.T.);
#16572=EDGE_CURVE('',#12960,#12963,#6413,.T.);
#16573=EDGE_CURVE('',#12962,#12963,#8399,.T.);
#16574=EDGE_CURVE('',#12963,#12964,#8400,.T.);
#16575=EDGE_CURVE('',#12961,#12964,#8401,.T.);
#16576=EDGE_CURVE('',#12964,#12959,#6414,.T.);
#16577=EDGE_CURVE('',#12965,#12966,#8402,.T.);
#16578=EDGE_CURVE('',#12965,#12967,#8403,.T.);
#16579=EDGE_CURVE('',#12968,#12967,#8404,.T.);
#16580=EDGE_CURVE('',#12966,#12968,#8405,.T.);
#16581=EDGE_CURVE('',#12966,#12969,#6415,.T.);
#16582=EDGE_CURVE('',#12968,#12969,#8406,.T.);
#16583=EDGE_CURVE('',#12969,#12970,#8407,.T.);
#16584=EDGE_CURVE('',#12967,#12970,#8408,.T.);
#16585=EDGE_CURVE('',#12970,#12965,#6416,.T.);
#16586=EDGE_CURVE('',#12971,#12972,#8409,.T.);
#16587=EDGE_CURVE('',#12971,#12973,#8410,.T.);
#16588=EDGE_CURVE('',#12974,#12973,#8411,.T.);
#16589=EDGE_CURVE('',#12972,#12974,#8412,.T.);
#16590=EDGE_CURVE('',#12972,#12975,#6417,.T.);
#16591=EDGE_CURVE('',#12974,#12975,#8413,.T.);
#16592=EDGE_CURVE('',#12975,#12976,#8414,.T.);
#16593=EDGE_CURVE('',#12973,#12976,#8415,.T.);
#16594=EDGE_CURVE('',#12976,#12971,#6418,.T.);
#16595=EDGE_CURVE('',#12977,#12978,#8416,.T.);
#16596=EDGE_CURVE('',#12977,#12979,#8417,.T.);
#16597=EDGE_CURVE('',#12980,#12979,#8418,.T.);
#16598=EDGE_CURVE('',#12978,#12980,#8419,.T.);
#16599=EDGE_CURVE('',#12978,#12981,#6419,.T.);
#16600=EDGE_CURVE('',#12980,#12981,#8420,.T.);
#16601=EDGE_CURVE('',#12981,#12982,#8421,.T.);
#16602=EDGE_CURVE('',#12979,#12982,#8422,.T.);
#16603=EDGE_CURVE('',#12982,#12977,#6420,.T.);
#16604=EDGE_CURVE('',#12983,#12984,#8423,.T.);
#16605=EDGE_CURVE('',#12983,#12985,#8424,.T.);
#16606=EDGE_CURVE('',#12986,#12985,#8425,.T.);
#16607=EDGE_CURVE('',#12984,#12986,#8426,.T.);
#16608=EDGE_CURVE('',#12984,#12987,#6421,.T.);
#16609=EDGE_CURVE('',#12986,#12987,#8427,.T.);
#16610=EDGE_CURVE('',#12987,#12988,#8428,.T.);
#16611=EDGE_CURVE('',#12985,#12988,#8429,.T.);
#16612=EDGE_CURVE('',#12988,#12983,#6422,.T.);
#16613=EDGE_CURVE('',#12989,#12989,#6423,.T.);
#16614=EDGE_CURVE('',#12754,#12989,#8430,.T.);
#16615=EDGE_CURVE('',#12990,#12990,#6424,.T.);
#16616=EDGE_CURVE('',#12990,#12757,#8431,.T.);
#16617=EDGE_CURVE('',#12981,#12772,#6425,.T.);
#16618=EDGE_CURVE('',#12781,#12978,#6426,.T.);
#16619=EDGE_CURVE('',#12975,#12778,#6427,.T.);
#16620=EDGE_CURVE('',#12787,#12972,#6428,.T.);
#16621=EDGE_CURVE('',#12969,#12784,#6429,.T.);
#16622=EDGE_CURVE('',#12793,#12966,#6430,.T.);
#16623=EDGE_CURVE('',#12963,#12790,#6431,.T.);
#16624=EDGE_CURVE('',#12799,#12960,#6432,.T.);
#16625=EDGE_CURVE('',#12957,#12796,#6433,.T.);
#16626=EDGE_CURVE('',#12805,#12954,#6434,.T.);
#16627=EDGE_CURVE('',#12951,#12802,#6435,.T.);
#16628=EDGE_CURVE('',#12811,#12948,#6436,.T.);
#16629=EDGE_CURVE('',#12945,#12808,#6437,.T.);
#16630=EDGE_CURVE('',#12817,#12942,#6438,.T.);
#16631=EDGE_CURVE('',#12939,#12814,#6439,.T.);
#16632=EDGE_CURVE('',#12824,#12936,#6440,.T.);
#16633=EDGE_CURVE('',#12826,#12990,#8432,.T.);
#16634=EDGE_CURVE('',#12831,#12820,#6441,.T.);
#16635=EDGE_CURVE('',#12927,#12828,#6442,.T.);
#16636=EDGE_CURVE('',#12837,#12924,#6443,.T.);
#16637=EDGE_CURVE('',#12921,#12834,#6444,.T.);
#16638=EDGE_CURVE('',#12843,#12918,#6445,.T.);
#16639=EDGE_CURVE('',#12915,#12840,#6446,.T.);
#16640=EDGE_CURVE('',#12849,#12912,#6447,.T.);
#16641=EDGE_CURVE('',#12909,#12846,#6448,.T.);
#16642=EDGE_CURVE('',#12855,#12906,#6449,.T.);
#16643=EDGE_CURVE('',#12903,#12852,#6450,.T.);
#16644=EDGE_CURVE('',#12861,#12900,#6451,.T.);
#16645=EDGE_CURVE('',#12897,#12858,#6452,.T.);
#16646=EDGE_CURVE('',#12867,#12894,#6453,.T.);
#16647=EDGE_CURVE('',#12891,#12864,#6454,.T.);
#16648=EDGE_CURVE('',#12873,#12888,#6455,.T.);
#16649=EDGE_CURVE('',#12885,#12870,#6456,.T.);
#16650=EDGE_CURVE('',#12879,#12882,#6457,.T.);
#16651=EDGE_CURVE('',#12930,#12876,#6458,.T.);
#16652=EDGE_CURVE('',#12987,#12929,#6459,.T.);
#16653=EDGE_CURVE('',#12775,#12984,#6460,.T.);
#16654=EDGE_CURVE('',#12991,#12991,#6461,.T.);
#16655=EDGE_CURVE('',#12991,#12823,#8433,.T.);
#22765=ORIENTED_EDGE('',*,*,#16105,.F.);
#22766=ORIENTED_EDGE('',*,*,#16106,.T.);
#22767=ORIENTED_EDGE('',*,*,#16107,.T.);
#22768=ORIENTED_EDGE('',*,*,#16108,.T.);
#22769=ORIENTED_EDGE('',*,*,#16109,.F.);
#22770=ORIENTED_EDGE('',*,*,#16110,.T.);
#22771=ORIENTED_EDGE('',*,*,#16105,.T.);
#22772=ORIENTED_EDGE('',*,*,#16111,.T.);
#22773=ORIENTED_EDGE('',*,*,#16112,.F.);
#22774=ORIENTED_EDGE('',*,*,#16113,.T.);
#22775=ORIENTED_EDGE('',*,*,#16109,.T.);
#22776=ORIENTED_EDGE('',*,*,#16114,.T.);
#22777=ORIENTED_EDGE('',*,*,#16115,.F.);
#22778=ORIENTED_EDGE('',*,*,#16116,.T.);
#22779=ORIENTED_EDGE('',*,*,#16112,.T.);
#22780=ORIENTED_EDGE('',*,*,#16117,.T.);
#22781=ORIENTED_EDGE('',*,*,#16118,.F.);
#22782=ORIENTED_EDGE('',*,*,#16119,.T.);
#22783=ORIENTED_EDGE('',*,*,#16115,.T.);
#22784=ORIENTED_EDGE('',*,*,#16120,.T.);
#22785=ORIENTED_EDGE('',*,*,#16121,.F.);
#22786=ORIENTED_EDGE('',*,*,#16122,.T.);
#22787=ORIENTED_EDGE('',*,*,#16118,.T.);
#22788=ORIENTED_EDGE('',*,*,#16123,.T.);
#22789=ORIENTED_EDGE('',*,*,#16124,.F.);
#22790=ORIENTED_EDGE('',*,*,#16125,.T.);
#22791=ORIENTED_EDGE('',*,*,#16121,.T.);
#22792=ORIENTED_EDGE('',*,*,#16126,.T.);
#22793=ORIENTED_EDGE('',*,*,#16127,.F.);
#22794=ORIENTED_EDGE('',*,*,#16128,.T.);
#22795=ORIENTED_EDGE('',*,*,#16124,.T.);
#22796=ORIENTED_EDGE('',*,*,#16129,.T.);
#22797=ORIENTED_EDGE('',*,*,#16130,.F.);
#22798=ORIENTED_EDGE('',*,*,#16131,.T.);
#22799=ORIENTED_EDGE('',*,*,#16127,.T.);
#22800=ORIENTED_EDGE('',*,*,#16132,.T.);
#22801=ORIENTED_EDGE('',*,*,#16133,.F.);
#22802=ORIENTED_EDGE('',*,*,#16134,.T.);
#22803=ORIENTED_EDGE('',*,*,#16130,.T.);
#22804=ORIENTED_EDGE('',*,*,#16135,.T.);
#22805=ORIENTED_EDGE('',*,*,#16136,.F.);
#22806=ORIENTED_EDGE('',*,*,#16137,.T.);
#22807=ORIENTED_EDGE('',*,*,#16133,.T.);
#22808=ORIENTED_EDGE('',*,*,#16138,.T.);
#22809=ORIENTED_EDGE('',*,*,#16139,.F.);
#22810=ORIENTED_EDGE('',*,*,#16140,.T.);
#22811=ORIENTED_EDGE('',*,*,#16136,.T.);
#22812=ORIENTED_EDGE('',*,*,#16141,.T.);
#22813=ORIENTED_EDGE('',*,*,#16142,.F.);
#22814=ORIENTED_EDGE('',*,*,#16143,.T.);
#22815=ORIENTED_EDGE('',*,*,#16139,.T.);
#22816=ORIENTED_EDGE('',*,*,#16144,.T.);
#22817=ORIENTED_EDGE('',*,*,#16145,.F.);
#22818=ORIENTED_EDGE('',*,*,#16146,.T.);
#22819=ORIENTED_EDGE('',*,*,#16142,.T.);
#22820=ORIENTED_EDGE('',*,*,#16147,.T.);
#22821=ORIENTED_EDGE('',*,*,#16148,.F.);
#22822=ORIENTED_EDGE('',*,*,#16149,.T.);
#22823=ORIENTED_EDGE('',*,*,#16145,.T.);
#22824=ORIENTED_EDGE('',*,*,#16150,.T.);
#22825=ORIENTED_EDGE('',*,*,#16151,.F.);
#22826=ORIENTED_EDGE('',*,*,#16152,.T.);
#22827=ORIENTED_EDGE('',*,*,#16148,.T.);
#22828=ORIENTED_EDGE('',*,*,#16153,.T.);
#22829=ORIENTED_EDGE('',*,*,#16154,.F.);
#22830=ORIENTED_EDGE('',*,*,#16155,.T.);
#22831=ORIENTED_EDGE('',*,*,#16151,.T.);
#22832=ORIENTED_EDGE('',*,*,#16156,.T.);
#22833=ORIENTED_EDGE('',*,*,#16157,.F.);
#22834=ORIENTED_EDGE('',*,*,#16158,.T.);
#22835=ORIENTED_EDGE('',*,*,#16154,.T.);
#22836=ORIENTED_EDGE('',*,*,#16159,.T.);
#22837=ORIENTED_EDGE('',*,*,#16160,.F.);
#22838=ORIENTED_EDGE('',*,*,#16161,.T.);
#22839=ORIENTED_EDGE('',*,*,#16157,.T.);
#22840=ORIENTED_EDGE('',*,*,#16162,.T.);
#22841=ORIENTED_EDGE('',*,*,#16163,.F.);
#22842=ORIENTED_EDGE('',*,*,#16164,.T.);
#22843=ORIENTED_EDGE('',*,*,#16160,.T.);
#22844=ORIENTED_EDGE('',*,*,#16165,.T.);
#22845=ORIENTED_EDGE('',*,*,#16166,.F.);
#22846=ORIENTED_EDGE('',*,*,#16167,.T.);
#22847=ORIENTED_EDGE('',*,*,#16163,.T.);
#22848=ORIENTED_EDGE('',*,*,#16168,.T.);
#22849=ORIENTED_EDGE('',*,*,#16169,.F.);
#22850=ORIENTED_EDGE('',*,*,#16170,.T.);
#22851=ORIENTED_EDGE('',*,*,#16166,.T.);
#22852=ORIENTED_EDGE('',*,*,#16171,.T.);
#22853=ORIENTED_EDGE('',*,*,#16172,.F.);
#22854=ORIENTED_EDGE('',*,*,#16173,.T.);
#22855=ORIENTED_EDGE('',*,*,#16169,.T.);
#22856=ORIENTED_EDGE('',*,*,#16174,.T.);
#22857=ORIENTED_EDGE('',*,*,#16175,.F.);
#22858=ORIENTED_EDGE('',*,*,#16176,.T.);
#22859=ORIENTED_EDGE('',*,*,#16177,.F.);
#22860=ORIENTED_EDGE('',*,*,#16178,.F.);
#22861=ORIENTED_EDGE('',*,*,#16179,.F.);
#22862=ORIENTED_EDGE('',*,*,#16180,.T.);
#22863=ORIENTED_EDGE('',*,*,#16175,.T.);
#22864=ORIENTED_EDGE('',*,*,#16181,.F.);
#22865=ORIENTED_EDGE('',*,*,#16182,.F.);
#22866=ORIENTED_EDGE('',*,*,#16183,.T.);
#22867=ORIENTED_EDGE('',*,*,#16179,.T.);
#22868=ORIENTED_EDGE('',*,*,#16184,.F.);
#22869=ORIENTED_EDGE('',*,*,#16185,.F.);
#22870=ORIENTED_EDGE('',*,*,#16186,.T.);
#22871=ORIENTED_EDGE('',*,*,#16182,.T.);
#22872=ORIENTED_EDGE('',*,*,#16187,.F.);
#22873=ORIENTED_EDGE('',*,*,#16188,.F.);
#22874=ORIENTED_EDGE('',*,*,#16189,.T.);
#22875=ORIENTED_EDGE('',*,*,#16185,.T.);
#22876=ORIENTED_EDGE('',*,*,#16190,.F.);
#22877=ORIENTED_EDGE('',*,*,#16191,.F.);
#22878=ORIENTED_EDGE('',*,*,#16192,.T.);
#22879=ORIENTED_EDGE('',*,*,#16188,.T.);
#22880=ORIENTED_EDGE('',*,*,#16193,.F.);
#22881=ORIENTED_EDGE('',*,*,#16194,.F.);
#22882=ORIENTED_EDGE('',*,*,#16195,.T.);
#22883=ORIENTED_EDGE('',*,*,#16191,.T.);
#22884=ORIENTED_EDGE('',*,*,#16196,.F.);
#22885=ORIENTED_EDGE('',*,*,#16197,.F.);
#22886=ORIENTED_EDGE('',*,*,#16198,.T.);
#22887=ORIENTED_EDGE('',*,*,#16194,.T.);
#22888=ORIENTED_EDGE('',*,*,#16199,.F.);
#22889=ORIENTED_EDGE('',*,*,#16200,.F.);
#22890=ORIENTED_EDGE('',*,*,#16201,.T.);
#22891=ORIENTED_EDGE('',*,*,#16197,.T.);
#22892=ORIENTED_EDGE('',*,*,#16202,.F.);
#22893=ORIENTED_EDGE('',*,*,#16203,.F.);
#22894=ORIENTED_EDGE('',*,*,#16204,.T.);
#22895=ORIENTED_EDGE('',*,*,#16200,.T.);
#22896=ORIENTED_EDGE('',*,*,#16205,.F.);
#22897=ORIENTED_EDGE('',*,*,#16206,.F.);
#22898=ORIENTED_EDGE('',*,*,#16207,.T.);
#22899=ORIENTED_EDGE('',*,*,#16203,.T.);
#22900=ORIENTED_EDGE('',*,*,#16208,.F.);
#22901=ORIENTED_EDGE('',*,*,#16209,.F.);
#22902=ORIENTED_EDGE('',*,*,#16210,.T.);
#22903=ORIENTED_EDGE('',*,*,#16206,.T.);
#22904=ORIENTED_EDGE('',*,*,#16211,.F.);
#22905=ORIENTED_EDGE('',*,*,#16212,.F.);
#22906=ORIENTED_EDGE('',*,*,#16213,.T.);
#22907=ORIENTED_EDGE('',*,*,#16209,.T.);
#22908=ORIENTED_EDGE('',*,*,#16214,.F.);
#22909=ORIENTED_EDGE('',*,*,#16215,.F.);
#22910=ORIENTED_EDGE('',*,*,#16216,.T.);
#22911=ORIENTED_EDGE('',*,*,#16212,.T.);
#22912=ORIENTED_EDGE('',*,*,#16217,.F.);
#22913=ORIENTED_EDGE('',*,*,#16218,.F.);
#22914=ORIENTED_EDGE('',*,*,#16219,.T.);
#22915=ORIENTED_EDGE('',*,*,#16215,.T.);
#22916=ORIENTED_EDGE('',*,*,#16220,.F.);
#22917=ORIENTED_EDGE('',*,*,#16221,.F.);
#22918=ORIENTED_EDGE('',*,*,#16222,.T.);
#22919=ORIENTED_EDGE('',*,*,#16218,.T.);
#22920=ORIENTED_EDGE('',*,*,#16223,.F.);
#22921=ORIENTED_EDGE('',*,*,#16224,.F.);
#22922=ORIENTED_EDGE('',*,*,#16225,.T.);
#22923=ORIENTED_EDGE('',*,*,#16221,.T.);
#22924=ORIENTED_EDGE('',*,*,#16226,.F.);
#22925=ORIENTED_EDGE('',*,*,#16227,.F.);
#22926=ORIENTED_EDGE('',*,*,#16228,.T.);
#22927=ORIENTED_EDGE('',*,*,#16224,.T.);
#22928=ORIENTED_EDGE('',*,*,#16229,.F.);
#22929=ORIENTED_EDGE('',*,*,#16230,.F.);
#22930=ORIENTED_EDGE('',*,*,#16231,.T.);
#22931=ORIENTED_EDGE('',*,*,#16227,.T.);
#22932=ORIENTED_EDGE('',*,*,#16232,.F.);
#22933=ORIENTED_EDGE('',*,*,#16233,.F.);
#22934=ORIENTED_EDGE('',*,*,#16234,.T.);
#22935=ORIENTED_EDGE('',*,*,#16230,.T.);
#22936=ORIENTED_EDGE('',*,*,#16235,.F.);
#22937=ORIENTED_EDGE('',*,*,#16236,.F.);
#22938=ORIENTED_EDGE('',*,*,#16237,.T.);
#22939=ORIENTED_EDGE('',*,*,#16233,.T.);
#22940=ORIENTED_EDGE('',*,*,#16238,.F.);
#22941=ORIENTED_EDGE('',*,*,#16239,.F.);
#22942=ORIENTED_EDGE('',*,*,#16240,.T.);
#22943=ORIENTED_EDGE('',*,*,#16236,.T.);
#22944=ORIENTED_EDGE('',*,*,#16241,.F.);
#22945=ORIENTED_EDGE('',*,*,#16242,.F.);
#22946=ORIENTED_EDGE('',*,*,#16243,.T.);
#22947=ORIENTED_EDGE('',*,*,#16239,.T.);
#22948=ORIENTED_EDGE('',*,*,#16244,.F.);
#22949=ORIENTED_EDGE('',*,*,#16177,.T.);
#22950=ORIENTED_EDGE('',*,*,#16245,.T.);
#22951=ORIENTED_EDGE('',*,*,#16246,.F.);
#22952=ORIENTED_EDGE('',*,*,#16247,.F.);
#22953=ORIENTED_EDGE('',*,*,#16248,.T.);
#22954=ORIENTED_EDGE('',*,*,#16248,.F.);
#22955=ORIENTED_EDGE('',*,*,#16249,.F.);
#22956=ORIENTED_EDGE('',*,*,#16174,.F.);
#22957=ORIENTED_EDGE('',*,*,#16171,.F.);
#22958=ORIENTED_EDGE('',*,*,#16168,.F.);
#22959=ORIENTED_EDGE('',*,*,#16165,.F.);
#22960=ORIENTED_EDGE('',*,*,#16162,.F.);
#22961=ORIENTED_EDGE('',*,*,#16159,.F.);
#22962=ORIENTED_EDGE('',*,*,#16156,.F.);
#22963=ORIENTED_EDGE('',*,*,#16153,.F.);
#22964=ORIENTED_EDGE('',*,*,#16150,.F.);
#22965=ORIENTED_EDGE('',*,*,#16147,.F.);
#22966=ORIENTED_EDGE('',*,*,#16144,.F.);
#22967=ORIENTED_EDGE('',*,*,#16141,.F.);
#22968=ORIENTED_EDGE('',*,*,#16138,.F.);
#22969=ORIENTED_EDGE('',*,*,#16135,.F.);
#22970=ORIENTED_EDGE('',*,*,#16132,.F.);
#22971=ORIENTED_EDGE('',*,*,#16129,.F.);
#22972=ORIENTED_EDGE('',*,*,#16126,.F.);
#22973=ORIENTED_EDGE('',*,*,#16123,.F.);
#22974=ORIENTED_EDGE('',*,*,#16120,.F.);
#22975=ORIENTED_EDGE('',*,*,#16117,.F.);
#22976=ORIENTED_EDGE('',*,*,#16114,.F.);
#22977=ORIENTED_EDGE('',*,*,#16111,.F.);
#22978=ORIENTED_EDGE('',*,*,#16108,.F.);
#22979=ORIENTED_EDGE('',*,*,#16250,.F.);
#22980=ORIENTED_EDGE('',*,*,#16251,.T.);
#22981=ORIENTED_EDGE('',*,*,#16244,.T.);
#22982=ORIENTED_EDGE('',*,*,#16241,.T.);
#22983=ORIENTED_EDGE('',*,*,#16238,.T.);
#22984=ORIENTED_EDGE('',*,*,#16235,.T.);
#22985=ORIENTED_EDGE('',*,*,#16232,.T.);
#22986=ORIENTED_EDGE('',*,*,#16229,.T.);
#22987=ORIENTED_EDGE('',*,*,#16226,.T.);
#22988=ORIENTED_EDGE('',*,*,#16223,.T.);
#22989=ORIENTED_EDGE('',*,*,#16220,.T.);
#22990=ORIENTED_EDGE('',*,*,#16217,.T.);
#22991=ORIENTED_EDGE('',*,*,#16214,.T.);
#22992=ORIENTED_EDGE('',*,*,#16211,.T.);
#22993=ORIENTED_EDGE('',*,*,#16208,.T.);
#22994=ORIENTED_EDGE('',*,*,#16205,.T.);
#22995=ORIENTED_EDGE('',*,*,#16202,.T.);
#22996=ORIENTED_EDGE('',*,*,#16199,.T.);
#22997=ORIENTED_EDGE('',*,*,#16196,.T.);
#22998=ORIENTED_EDGE('',*,*,#16193,.T.);
#22999=ORIENTED_EDGE('',*,*,#16190,.T.);
#23000=ORIENTED_EDGE('',*,*,#16187,.T.);
#23001=ORIENTED_EDGE('',*,*,#16184,.T.);
#23002=ORIENTED_EDGE('',*,*,#16181,.T.);
#23003=ORIENTED_EDGE('',*,*,#16178,.T.);
#23004=ORIENTED_EDGE('',*,*,#16252,.T.);
#23005=ORIENTED_EDGE('',*,*,#16253,.T.);
#23006=ORIENTED_EDGE('',*,*,#16254,.T.);
#23007=ORIENTED_EDGE('',*,*,#16255,.T.);
#23008=ORIENTED_EDGE('',*,*,#16250,.T.);
#23009=ORIENTED_EDGE('',*,*,#16242,.T.);
#23010=ORIENTED_EDGE('',*,*,#16251,.F.);
#23011=ORIENTED_EDGE('',*,*,#16255,.F.);
#23012=ORIENTED_EDGE('',*,*,#16256,.T.);
#23013=ORIENTED_EDGE('',*,*,#16245,.F.);
#23014=ORIENTED_EDGE('',*,*,#16176,.F.);
#23015=ORIENTED_EDGE('',*,*,#16180,.F.);
#23016=ORIENTED_EDGE('',*,*,#16183,.F.);
#23017=ORIENTED_EDGE('',*,*,#16186,.F.);
#23018=ORIENTED_EDGE('',*,*,#16189,.F.);
#23019=ORIENTED_EDGE('',*,*,#16192,.F.);
#23020=ORIENTED_EDGE('',*,*,#16195,.F.);
#23021=ORIENTED_EDGE('',*,*,#16198,.F.);
#23022=ORIENTED_EDGE('',*,*,#16201,.F.);
#23023=ORIENTED_EDGE('',*,*,#16204,.F.);
#23024=ORIENTED_EDGE('',*,*,#16207,.F.);
#23025=ORIENTED_EDGE('',*,*,#16210,.F.);
#23026=ORIENTED_EDGE('',*,*,#16213,.F.);
#23027=ORIENTED_EDGE('',*,*,#16216,.F.);
#23028=ORIENTED_EDGE('',*,*,#16219,.F.);
#23029=ORIENTED_EDGE('',*,*,#16222,.F.);
#23030=ORIENTED_EDGE('',*,*,#16225,.F.);
#23031=ORIENTED_EDGE('',*,*,#16228,.F.);
#23032=ORIENTED_EDGE('',*,*,#16231,.F.);
#23033=ORIENTED_EDGE('',*,*,#16234,.F.);
#23034=ORIENTED_EDGE('',*,*,#16237,.F.);
#23035=ORIENTED_EDGE('',*,*,#16240,.F.);
#23036=ORIENTED_EDGE('',*,*,#16243,.F.);
#23037=ORIENTED_EDGE('',*,*,#16256,.F.);
#23038=ORIENTED_EDGE('',*,*,#16254,.F.);
#23039=ORIENTED_EDGE('',*,*,#16106,.F.);
#23040=ORIENTED_EDGE('',*,*,#16110,.F.);
#23041=ORIENTED_EDGE('',*,*,#16113,.F.);
#23042=ORIENTED_EDGE('',*,*,#16116,.F.);
#23043=ORIENTED_EDGE('',*,*,#16119,.F.);
#23044=ORIENTED_EDGE('',*,*,#16122,.F.);
#23045=ORIENTED_EDGE('',*,*,#16125,.F.);
#23046=ORIENTED_EDGE('',*,*,#16128,.F.);
#23047=ORIENTED_EDGE('',*,*,#16131,.F.);
#23048=ORIENTED_EDGE('',*,*,#16134,.F.);
#23049=ORIENTED_EDGE('',*,*,#16137,.F.);
#23050=ORIENTED_EDGE('',*,*,#16140,.F.);
#23051=ORIENTED_EDGE('',*,*,#16143,.F.);
#23052=ORIENTED_EDGE('',*,*,#16146,.F.);
#23053=ORIENTED_EDGE('',*,*,#16149,.F.);
#23054=ORIENTED_EDGE('',*,*,#16152,.F.);
#23055=ORIENTED_EDGE('',*,*,#16155,.F.);
#23056=ORIENTED_EDGE('',*,*,#16158,.F.);
#23057=ORIENTED_EDGE('',*,*,#16161,.F.);
#23058=ORIENTED_EDGE('',*,*,#16164,.F.);
#23059=ORIENTED_EDGE('',*,*,#16167,.F.);
#23060=ORIENTED_EDGE('',*,*,#16170,.F.);
#23061=ORIENTED_EDGE('',*,*,#16173,.F.);
#23062=ORIENTED_EDGE('',*,*,#16257,.F.);
#23063=ORIENTED_EDGE('',*,*,#16247,.T.);
#23064=ORIENTED_EDGE('',*,*,#16258,.T.);
#23065=ORIENTED_EDGE('',*,*,#16259,.T.);
#23066=ORIENTED_EDGE('',*,*,#16258,.F.);
#23067=ORIENTED_EDGE('',*,*,#16246,.T.);
#23068=ORIENTED_EDGE('',*,*,#16260,.T.);
#23069=ORIENTED_EDGE('',*,*,#16172,.T.);
#23070=ORIENTED_EDGE('',*,*,#16249,.T.);
#23071=ORIENTED_EDGE('',*,*,#16260,.F.);
#23072=ORIENTED_EDGE('',*,*,#16257,.T.);
#23073=ORIENTED_EDGE('',*,*,#16261,.F.);
#23074=ORIENTED_EDGE('',*,*,#16259,.F.);
#23075=ORIENTED_EDGE('',*,*,#16262,.F.);
#23076=ORIENTED_EDGE('',*,*,#16263,.F.);
#23077=ORIENTED_EDGE('',*,*,#16264,.F.);
#23078=ORIENTED_EDGE('',*,*,#16265,.F.);
#23079=ORIENTED_EDGE('',*,*,#16266,.F.);
#23080=ORIENTED_EDGE('',*,*,#16267,.F.);
#23081=ORIENTED_EDGE('',*,*,#16268,.F.);
#23082=ORIENTED_EDGE('',*,*,#16269,.F.);
#23083=ORIENTED_EDGE('',*,*,#16270,.F.);
#23084=ORIENTED_EDGE('',*,*,#16271,.F.);
#23085=ORIENTED_EDGE('',*,*,#16272,.F.);
#23086=ORIENTED_EDGE('',*,*,#16273,.F.);
#23087=ORIENTED_EDGE('',*,*,#16274,.T.);
#23088=ORIENTED_EDGE('',*,*,#16269,.T.);
#23089=ORIENTED_EDGE('',*,*,#16267,.T.);
#23090=ORIENTED_EDGE('',*,*,#16265,.T.);
#23091=ORIENTED_EDGE('',*,*,#16263,.T.);
#23092=ORIENTED_EDGE('',*,*,#16273,.T.);
#23093=ORIENTED_EDGE('',*,*,#16271,.T.);
#23094=ORIENTED_EDGE('',*,*,#16274,.F.);
#23095=ORIENTED_EDGE('',*,*,#16275,.F.);
#23096=ORIENTED_EDGE('',*,*,#16276,.T.);
#23097=ORIENTED_EDGE('',*,*,#16262,.T.);
#23098=ORIENTED_EDGE('',*,*,#16277,.F.);
#23099=ORIENTED_EDGE('',*,*,#16278,.F.);
#23100=ORIENTED_EDGE('',*,*,#16279,.T.);
#23101=ORIENTED_EDGE('',*,*,#16272,.T.);
#23102=ORIENTED_EDGE('',*,*,#16276,.F.);
#23103=ORIENTED_EDGE('',*,*,#16280,.F.);
#23104=ORIENTED_EDGE('',*,*,#16281,.T.);
#23105=ORIENTED_EDGE('',*,*,#16270,.T.);
#23106=ORIENTED_EDGE('',*,*,#16279,.F.);
#23107=ORIENTED_EDGE('',*,*,#16282,.F.);
#23108=ORIENTED_EDGE('',*,*,#16283,.T.);
#23109=ORIENTED_EDGE('',*,*,#16268,.T.);
#23110=ORIENTED_EDGE('',*,*,#16281,.F.);
#23111=ORIENTED_EDGE('',*,*,#16284,.F.);
#23112=ORIENTED_EDGE('',*,*,#16285,.T.);
#23113=ORIENTED_EDGE('',*,*,#16266,.T.);
#23114=ORIENTED_EDGE('',*,*,#16283,.F.);
#23115=ORIENTED_EDGE('',*,*,#16286,.F.);
#23116=ORIENTED_EDGE('',*,*,#16277,.T.);
#23117=ORIENTED_EDGE('',*,*,#16264,.T.);
#23118=ORIENTED_EDGE('',*,*,#16285,.F.);
#23119=ORIENTED_EDGE('',*,*,#16287,.F.);
#23120=ORIENTED_EDGE('',*,*,#16288,.T.);
#23121=ORIENTED_EDGE('',*,*,#16289,.F.);
#23122=ORIENTED_EDGE('',*,*,#16290,.F.);
#23123=ORIENTED_EDGE('',*,*,#16291,.F.);
#23124=ORIENTED_EDGE('',*,*,#16290,.T.);
#23125=ORIENTED_EDGE('',*,*,#16292,.T.);
#23126=ORIENTED_EDGE('',*,*,#16293,.F.);
#23127=ORIENTED_EDGE('',*,*,#16292,.F.);
#23128=ORIENTED_EDGE('',*,*,#16289,.T.);
#23129=ORIENTED_EDGE('',*,*,#16294,.T.);
#23130=ORIENTED_EDGE('',*,*,#16295,.F.);
#23131=ORIENTED_EDGE('',*,*,#16294,.F.);
#23132=ORIENTED_EDGE('',*,*,#16288,.F.);
#23133=ORIENTED_EDGE('',*,*,#16296,.F.);
#23134=ORIENTED_EDGE('',*,*,#16297,.T.);
#23135=ORIENTED_EDGE('',*,*,#16298,.F.);
#23136=ORIENTED_EDGE('',*,*,#16299,.F.);
#23137=ORIENTED_EDGE('',*,*,#16300,.F.);
#23138=ORIENTED_EDGE('',*,*,#16299,.T.);
#23139=ORIENTED_EDGE('',*,*,#16301,.T.);
#23140=ORIENTED_EDGE('',*,*,#16302,.F.);
#23141=ORIENTED_EDGE('',*,*,#16301,.F.);
#23142=ORIENTED_EDGE('',*,*,#16298,.T.);
#23143=ORIENTED_EDGE('',*,*,#16303,.T.);
#23144=ORIENTED_EDGE('',*,*,#16304,.F.);
#23145=ORIENTED_EDGE('',*,*,#16303,.F.);
#23146=ORIENTED_EDGE('',*,*,#16297,.F.);
#23147=ORIENTED_EDGE('',*,*,#16305,.F.);
#23148=ORIENTED_EDGE('',*,*,#16306,.T.);
#23149=ORIENTED_EDGE('',*,*,#16307,.F.);
#23150=ORIENTED_EDGE('',*,*,#16308,.F.);
#23151=ORIENTED_EDGE('',*,*,#16309,.F.);
#23152=ORIENTED_EDGE('',*,*,#16308,.T.);
#23153=ORIENTED_EDGE('',*,*,#16310,.T.);
#23154=ORIENTED_EDGE('',*,*,#16311,.F.);
#23155=ORIENTED_EDGE('',*,*,#16310,.F.);
#23156=ORIENTED_EDGE('',*,*,#16307,.T.);
#23157=ORIENTED_EDGE('',*,*,#16312,.T.);
#23158=ORIENTED_EDGE('',*,*,#16313,.F.);
#23159=ORIENTED_EDGE('',*,*,#16312,.F.);
#23160=ORIENTED_EDGE('',*,*,#16306,.F.);
#23161=ORIENTED_EDGE('',*,*,#16314,.F.);
#23162=ORIENTED_EDGE('',*,*,#16315,.T.);
#23163=ORIENTED_EDGE('',*,*,#16316,.F.);
#23164=ORIENTED_EDGE('',*,*,#16317,.F.);
#23165=ORIENTED_EDGE('',*,*,#16318,.F.);
#23166=ORIENTED_EDGE('',*,*,#16317,.T.);
#23167=ORIENTED_EDGE('',*,*,#16319,.T.);
#23168=ORIENTED_EDGE('',*,*,#16320,.F.);
#23169=ORIENTED_EDGE('',*,*,#16319,.F.);
#23170=ORIENTED_EDGE('',*,*,#16316,.T.);
#23171=ORIENTED_EDGE('',*,*,#16321,.T.);
#23172=ORIENTED_EDGE('',*,*,#16322,.F.);
#23173=ORIENTED_EDGE('',*,*,#16321,.F.);
#23174=ORIENTED_EDGE('',*,*,#16315,.F.);
#23175=ORIENTED_EDGE('',*,*,#16323,.F.);
#23176=ORIENTED_EDGE('',*,*,#16324,.T.);
#23177=ORIENTED_EDGE('',*,*,#16325,.F.);
#23178=ORIENTED_EDGE('',*,*,#16326,.F.);
#23179=ORIENTED_EDGE('',*,*,#16327,.F.);
#23180=ORIENTED_EDGE('',*,*,#16326,.T.);
#23181=ORIENTED_EDGE('',*,*,#16328,.T.);
#23182=ORIENTED_EDGE('',*,*,#16329,.F.);
#23183=ORIENTED_EDGE('',*,*,#16328,.F.);
#23184=ORIENTED_EDGE('',*,*,#16325,.T.);
#23185=ORIENTED_EDGE('',*,*,#16330,.T.);
#23186=ORIENTED_EDGE('',*,*,#16331,.F.);
#23187=ORIENTED_EDGE('',*,*,#16330,.F.);
#23188=ORIENTED_EDGE('',*,*,#16324,.F.);
#23189=ORIENTED_EDGE('',*,*,#16332,.F.);
#23190=ORIENTED_EDGE('',*,*,#16333,.T.);
#23191=ORIENTED_EDGE('',*,*,#16334,.F.);
#23192=ORIENTED_EDGE('',*,*,#16335,.F.);
#23193=ORIENTED_EDGE('',*,*,#16336,.F.);
#23194=ORIENTED_EDGE('',*,*,#16335,.T.);
#23195=ORIENTED_EDGE('',*,*,#16337,.T.);
#23196=ORIENTED_EDGE('',*,*,#16338,.F.);
#23197=ORIENTED_EDGE('',*,*,#16337,.F.);
#23198=ORIENTED_EDGE('',*,*,#16334,.T.);
#23199=ORIENTED_EDGE('',*,*,#16339,.T.);
#23200=ORIENTED_EDGE('',*,*,#16340,.F.);
#23201=ORIENTED_EDGE('',*,*,#16339,.F.);
#23202=ORIENTED_EDGE('',*,*,#16333,.F.);
#23203=ORIENTED_EDGE('',*,*,#16341,.F.);
#23204=ORIENTED_EDGE('',*,*,#16342,.T.);
#23205=ORIENTED_EDGE('',*,*,#16343,.F.);
#23206=ORIENTED_EDGE('',*,*,#16344,.F.);
#23207=ORIENTED_EDGE('',*,*,#16345,.F.);
#23208=ORIENTED_EDGE('',*,*,#16344,.T.);
#23209=ORIENTED_EDGE('',*,*,#16346,.T.);
#23210=ORIENTED_EDGE('',*,*,#16347,.F.);
#23211=ORIENTED_EDGE('',*,*,#16346,.F.);
#23212=ORIENTED_EDGE('',*,*,#16343,.T.);
#23213=ORIENTED_EDGE('',*,*,#16348,.T.);
#23214=ORIENTED_EDGE('',*,*,#16349,.F.);
#23215=ORIENTED_EDGE('',*,*,#16348,.F.);
#23216=ORIENTED_EDGE('',*,*,#16342,.F.);
#23217=ORIENTED_EDGE('',*,*,#16350,.F.);
#23218=ORIENTED_EDGE('',*,*,#16351,.T.);
#23219=ORIENTED_EDGE('',*,*,#16352,.F.);
#23220=ORIENTED_EDGE('',*,*,#16353,.F.);
#23221=ORIENTED_EDGE('',*,*,#16354,.F.);
#23222=ORIENTED_EDGE('',*,*,#16353,.T.);
#23223=ORIENTED_EDGE('',*,*,#16355,.T.);
#23224=ORIENTED_EDGE('',*,*,#16356,.F.);
#23225=ORIENTED_EDGE('',*,*,#16355,.F.);
#23226=ORIENTED_EDGE('',*,*,#16352,.T.);
#23227=ORIENTED_EDGE('',*,*,#16357,.T.);
#23228=ORIENTED_EDGE('',*,*,#16358,.F.);
#23229=ORIENTED_EDGE('',*,*,#16357,.F.);
#23230=ORIENTED_EDGE('',*,*,#16351,.F.);
#23231=ORIENTED_EDGE('',*,*,#16359,.F.);
#23232=ORIENTED_EDGE('',*,*,#16360,.T.);
#23233=ORIENTED_EDGE('',*,*,#16361,.F.);
#23234=ORIENTED_EDGE('',*,*,#16362,.F.);
#23235=ORIENTED_EDGE('',*,*,#16363,.F.);
#23236=ORIENTED_EDGE('',*,*,#16362,.T.);
#23237=ORIENTED_EDGE('',*,*,#16364,.T.);
#23238=ORIENTED_EDGE('',*,*,#16365,.F.);
#23239=ORIENTED_EDGE('',*,*,#16366,.F.);
#23240=ORIENTED_EDGE('',*,*,#16364,.F.);
#23241=ORIENTED_EDGE('',*,*,#16361,.T.);
#23242=ORIENTED_EDGE('',*,*,#16367,.T.);
#23243=ORIENTED_EDGE('',*,*,#16368,.F.);
#23244=ORIENTED_EDGE('',*,*,#16367,.F.);
#23245=ORIENTED_EDGE('',*,*,#16360,.F.);
#23246=ORIENTED_EDGE('',*,*,#16369,.F.);
#23247=ORIENTED_EDGE('',*,*,#16370,.F.);
#23248=ORIENTED_EDGE('',*,*,#16371,.T.);
#23249=ORIENTED_EDGE('',*,*,#16372,.F.);
#23250=ORIENTED_EDGE('',*,*,#16373,.F.);
#23251=ORIENTED_EDGE('',*,*,#16374,.F.);
#23252=ORIENTED_EDGE('',*,*,#16373,.T.);
#23253=ORIENTED_EDGE('',*,*,#16375,.T.);
#23254=ORIENTED_EDGE('',*,*,#16376,.F.);
#23255=ORIENTED_EDGE('',*,*,#16375,.F.);
#23256=ORIENTED_EDGE('',*,*,#16372,.T.);
#23257=ORIENTED_EDGE('',*,*,#16377,.T.);
#23258=ORIENTED_EDGE('',*,*,#16378,.F.);
#23259=ORIENTED_EDGE('',*,*,#16377,.F.);
#23260=ORIENTED_EDGE('',*,*,#16371,.F.);
#23261=ORIENTED_EDGE('',*,*,#16379,.F.);
#23262=ORIENTED_EDGE('',*,*,#16380,.T.);
#23263=ORIENTED_EDGE('',*,*,#16381,.F.);
#23264=ORIENTED_EDGE('',*,*,#16382,.F.);
#23265=ORIENTED_EDGE('',*,*,#16383,.F.);
#23266=ORIENTED_EDGE('',*,*,#16382,.T.);
#23267=ORIENTED_EDGE('',*,*,#16384,.T.);
#23268=ORIENTED_EDGE('',*,*,#16385,.F.);
#23269=ORIENTED_EDGE('',*,*,#16384,.F.);
#23270=ORIENTED_EDGE('',*,*,#16381,.T.);
#23271=ORIENTED_EDGE('',*,*,#16386,.T.);
#23272=ORIENTED_EDGE('',*,*,#16387,.F.);
#23273=ORIENTED_EDGE('',*,*,#16386,.F.);
#23274=ORIENTED_EDGE('',*,*,#16380,.F.);
#23275=ORIENTED_EDGE('',*,*,#16388,.F.);
#23276=ORIENTED_EDGE('',*,*,#16389,.T.);
#23277=ORIENTED_EDGE('',*,*,#16390,.F.);
#23278=ORIENTED_EDGE('',*,*,#16391,.F.);
#23279=ORIENTED_EDGE('',*,*,#16392,.F.);
#23280=ORIENTED_EDGE('',*,*,#16391,.T.);
#23281=ORIENTED_EDGE('',*,*,#16393,.T.);
#23282=ORIENTED_EDGE('',*,*,#16394,.F.);
#23283=ORIENTED_EDGE('',*,*,#16393,.F.);
#23284=ORIENTED_EDGE('',*,*,#16390,.T.);
#23285=ORIENTED_EDGE('',*,*,#16395,.T.);
#23286=ORIENTED_EDGE('',*,*,#16396,.F.);
#23287=ORIENTED_EDGE('',*,*,#16395,.F.);
#23288=ORIENTED_EDGE('',*,*,#16389,.F.);
#23289=ORIENTED_EDGE('',*,*,#16397,.F.);
#23290=ORIENTED_EDGE('',*,*,#16398,.T.);
#23291=ORIENTED_EDGE('',*,*,#16399,.F.);
#23292=ORIENTED_EDGE('',*,*,#16400,.F.);
#23293=ORIENTED_EDGE('',*,*,#16401,.F.);
#23294=ORIENTED_EDGE('',*,*,#16400,.T.);
#23295=ORIENTED_EDGE('',*,*,#16402,.T.);
#23296=ORIENTED_EDGE('',*,*,#16403,.F.);
#23297=ORIENTED_EDGE('',*,*,#16402,.F.);
#23298=ORIENTED_EDGE('',*,*,#16399,.T.);
#23299=ORIENTED_EDGE('',*,*,#16404,.T.);
#23300=ORIENTED_EDGE('',*,*,#16405,.F.);
#23301=ORIENTED_EDGE('',*,*,#16404,.F.);
#23302=ORIENTED_EDGE('',*,*,#16398,.F.);
#23303=ORIENTED_EDGE('',*,*,#16406,.F.);
#23304=ORIENTED_EDGE('',*,*,#16407,.T.);
#23305=ORIENTED_EDGE('',*,*,#16408,.F.);
#23306=ORIENTED_EDGE('',*,*,#16409,.F.);
#23307=ORIENTED_EDGE('',*,*,#16410,.F.);
#23308=ORIENTED_EDGE('',*,*,#16409,.T.);
#23309=ORIENTED_EDGE('',*,*,#16411,.T.);
#23310=ORIENTED_EDGE('',*,*,#16412,.F.);
#23311=ORIENTED_EDGE('',*,*,#16411,.F.);
#23312=ORIENTED_EDGE('',*,*,#16408,.T.);
#23313=ORIENTED_EDGE('',*,*,#16413,.T.);
#23314=ORIENTED_EDGE('',*,*,#16414,.F.);
#23315=ORIENTED_EDGE('',*,*,#16413,.F.);
#23316=ORIENTED_EDGE('',*,*,#16407,.F.);
#23317=ORIENTED_EDGE('',*,*,#16415,.F.);
#23318=ORIENTED_EDGE('',*,*,#16416,.T.);
#23319=ORIENTED_EDGE('',*,*,#16417,.F.);
#23320=ORIENTED_EDGE('',*,*,#16418,.F.);
#23321=ORIENTED_EDGE('',*,*,#16419,.F.);
#23322=ORIENTED_EDGE('',*,*,#16418,.T.);
#23323=ORIENTED_EDGE('',*,*,#16420,.T.);
#23324=ORIENTED_EDGE('',*,*,#16421,.F.);
#23325=ORIENTED_EDGE('',*,*,#16420,.F.);
#23326=ORIENTED_EDGE('',*,*,#16417,.T.);
#23327=ORIENTED_EDGE('',*,*,#16422,.T.);
#23328=ORIENTED_EDGE('',*,*,#16423,.F.);
#23329=ORIENTED_EDGE('',*,*,#16422,.F.);
#23330=ORIENTED_EDGE('',*,*,#16416,.F.);
#23331=ORIENTED_EDGE('',*,*,#16424,.F.);
#23332=ORIENTED_EDGE('',*,*,#16425,.T.);
#23333=ORIENTED_EDGE('',*,*,#16426,.F.);
#23334=ORIENTED_EDGE('',*,*,#16427,.F.);
#23335=ORIENTED_EDGE('',*,*,#16428,.F.);
#23336=ORIENTED_EDGE('',*,*,#16427,.T.);
#23337=ORIENTED_EDGE('',*,*,#16429,.T.);
#23338=ORIENTED_EDGE('',*,*,#16430,.F.);
#23339=ORIENTED_EDGE('',*,*,#16429,.F.);
#23340=ORIENTED_EDGE('',*,*,#16426,.T.);
#23341=ORIENTED_EDGE('',*,*,#16431,.T.);
#23342=ORIENTED_EDGE('',*,*,#16432,.F.);
#23343=ORIENTED_EDGE('',*,*,#16431,.F.);
#23344=ORIENTED_EDGE('',*,*,#16425,.F.);
#23345=ORIENTED_EDGE('',*,*,#16433,.F.);
#23346=ORIENTED_EDGE('',*,*,#16434,.T.);
#23347=ORIENTED_EDGE('',*,*,#16435,.F.);
#23348=ORIENTED_EDGE('',*,*,#16436,.F.);
#23349=ORIENTED_EDGE('',*,*,#16437,.F.);
#23350=ORIENTED_EDGE('',*,*,#16436,.T.);
#23351=ORIENTED_EDGE('',*,*,#16438,.T.);
#23352=ORIENTED_EDGE('',*,*,#16439,.F.);
#23353=ORIENTED_EDGE('',*,*,#16438,.F.);
#23354=ORIENTED_EDGE('',*,*,#16435,.T.);
#23355=ORIENTED_EDGE('',*,*,#16440,.T.);
#23356=ORIENTED_EDGE('',*,*,#16441,.F.);
#23357=ORIENTED_EDGE('',*,*,#16440,.F.);
#23358=ORIENTED_EDGE('',*,*,#16434,.F.);
#23359=ORIENTED_EDGE('',*,*,#16442,.F.);
#23360=ORIENTED_EDGE('',*,*,#16443,.T.);
#23361=ORIENTED_EDGE('',*,*,#16444,.F.);
#23362=ORIENTED_EDGE('',*,*,#16445,.F.);
#23363=ORIENTED_EDGE('',*,*,#16446,.F.);
#23364=ORIENTED_EDGE('',*,*,#16445,.T.);
#23365=ORIENTED_EDGE('',*,*,#16447,.T.);
#23366=ORIENTED_EDGE('',*,*,#16448,.F.);
#23367=ORIENTED_EDGE('',*,*,#16447,.F.);
#23368=ORIENTED_EDGE('',*,*,#16444,.T.);
#23369=ORIENTED_EDGE('',*,*,#16449,.T.);
#23370=ORIENTED_EDGE('',*,*,#16450,.F.);
#23371=ORIENTED_EDGE('',*,*,#16449,.F.);
#23372=ORIENTED_EDGE('',*,*,#16443,.F.);
#23373=ORIENTED_EDGE('',*,*,#16451,.F.);
#23374=ORIENTED_EDGE('',*,*,#16452,.T.);
#23375=ORIENTED_EDGE('',*,*,#16453,.F.);
#23376=ORIENTED_EDGE('',*,*,#16454,.F.);
#23377=ORIENTED_EDGE('',*,*,#16455,.F.);
#23378=ORIENTED_EDGE('',*,*,#16454,.T.);
#23379=ORIENTED_EDGE('',*,*,#16456,.T.);
#23380=ORIENTED_EDGE('',*,*,#16457,.F.);
#23381=ORIENTED_EDGE('',*,*,#16456,.F.);
#23382=ORIENTED_EDGE('',*,*,#16453,.T.);
#23383=ORIENTED_EDGE('',*,*,#16458,.T.);
#23384=ORIENTED_EDGE('',*,*,#16459,.F.);
#23385=ORIENTED_EDGE('',*,*,#16458,.F.);
#23386=ORIENTED_EDGE('',*,*,#16452,.F.);
#23387=ORIENTED_EDGE('',*,*,#16460,.F.);
#23388=ORIENTED_EDGE('',*,*,#16461,.T.);
#23389=ORIENTED_EDGE('',*,*,#16462,.F.);
#23390=ORIENTED_EDGE('',*,*,#16463,.F.);
#23391=ORIENTED_EDGE('',*,*,#16464,.F.);
#23392=ORIENTED_EDGE('',*,*,#16463,.T.);
#23393=ORIENTED_EDGE('',*,*,#16465,.T.);
#23394=ORIENTED_EDGE('',*,*,#16466,.F.);
#23395=ORIENTED_EDGE('',*,*,#16465,.F.);
#23396=ORIENTED_EDGE('',*,*,#16462,.T.);
#23397=ORIENTED_EDGE('',*,*,#16467,.T.);
#23398=ORIENTED_EDGE('',*,*,#16468,.F.);
#23399=ORIENTED_EDGE('',*,*,#16467,.F.);
#23400=ORIENTED_EDGE('',*,*,#16461,.F.);
#23401=ORIENTED_EDGE('',*,*,#16469,.F.);
#23402=ORIENTED_EDGE('',*,*,#16470,.T.);
#23403=ORIENTED_EDGE('',*,*,#16471,.F.);
#23404=ORIENTED_EDGE('',*,*,#16472,.F.);
#23405=ORIENTED_EDGE('',*,*,#16473,.F.);
#23406=ORIENTED_EDGE('',*,*,#16472,.T.);
#23407=ORIENTED_EDGE('',*,*,#16474,.T.);
#23408=ORIENTED_EDGE('',*,*,#16475,.F.);
#23409=ORIENTED_EDGE('',*,*,#16474,.F.);
#23410=ORIENTED_EDGE('',*,*,#16471,.T.);
#23411=ORIENTED_EDGE('',*,*,#16476,.T.);
#23412=ORIENTED_EDGE('',*,*,#16477,.F.);
#23413=ORIENTED_EDGE('',*,*,#16476,.F.);
#23414=ORIENTED_EDGE('',*,*,#16470,.F.);
#23415=ORIENTED_EDGE('',*,*,#16478,.F.);
#23416=ORIENTED_EDGE('',*,*,#16479,.T.);
#23417=ORIENTED_EDGE('',*,*,#16480,.F.);
#23418=ORIENTED_EDGE('',*,*,#16481,.F.);
#23419=ORIENTED_EDGE('',*,*,#16482,.F.);
#23420=ORIENTED_EDGE('',*,*,#16481,.T.);
#23421=ORIENTED_EDGE('',*,*,#16483,.T.);
#23422=ORIENTED_EDGE('',*,*,#16484,.F.);
#23423=ORIENTED_EDGE('',*,*,#16483,.F.);
#23424=ORIENTED_EDGE('',*,*,#16480,.T.);
#23425=ORIENTED_EDGE('',*,*,#16485,.T.);
#23426=ORIENTED_EDGE('',*,*,#16486,.F.);
#23427=ORIENTED_EDGE('',*,*,#16485,.F.);
#23428=ORIENTED_EDGE('',*,*,#16479,.F.);
#23429=ORIENTED_EDGE('',*,*,#16487,.F.);
#23430=ORIENTED_EDGE('',*,*,#16488,.T.);
#23431=ORIENTED_EDGE('',*,*,#16489,.F.);
#23432=ORIENTED_EDGE('',*,*,#16490,.F.);
#23433=ORIENTED_EDGE('',*,*,#16491,.F.);
#23434=ORIENTED_EDGE('',*,*,#16490,.T.);
#23435=ORIENTED_EDGE('',*,*,#16492,.T.);
#23436=ORIENTED_EDGE('',*,*,#16493,.F.);
#23437=ORIENTED_EDGE('',*,*,#16492,.F.);
#23438=ORIENTED_EDGE('',*,*,#16489,.T.);
#23439=ORIENTED_EDGE('',*,*,#16494,.T.);
#23440=ORIENTED_EDGE('',*,*,#16495,.F.);
#23441=ORIENTED_EDGE('',*,*,#16494,.F.);
#23442=ORIENTED_EDGE('',*,*,#16488,.F.);
#23443=ORIENTED_EDGE('',*,*,#16496,.F.);
#23444=ORIENTED_EDGE('',*,*,#16497,.T.);
#23445=ORIENTED_EDGE('',*,*,#16498,.F.);
#23446=ORIENTED_EDGE('',*,*,#16499,.F.);
#23447=ORIENTED_EDGE('',*,*,#16500,.F.);
#23448=ORIENTED_EDGE('',*,*,#16499,.T.);
#23449=ORIENTED_EDGE('',*,*,#16501,.T.);
#23450=ORIENTED_EDGE('',*,*,#16502,.F.);
#23451=ORIENTED_EDGE('',*,*,#16501,.F.);
#23452=ORIENTED_EDGE('',*,*,#16498,.T.);
#23453=ORIENTED_EDGE('',*,*,#16503,.T.);
#23454=ORIENTED_EDGE('',*,*,#16504,.F.);
#23455=ORIENTED_EDGE('',*,*,#16503,.F.);
#23456=ORIENTED_EDGE('',*,*,#16497,.F.);
#23457=ORIENTED_EDGE('',*,*,#16505,.F.);
#23458=ORIENTED_EDGE('',*,*,#16506,.T.);
#23459=ORIENTED_EDGE('',*,*,#16507,.F.);
#23460=ORIENTED_EDGE('',*,*,#16508,.F.);
#23461=ORIENTED_EDGE('',*,*,#16509,.F.);
#23462=ORIENTED_EDGE('',*,*,#16508,.T.);
#23463=ORIENTED_EDGE('',*,*,#16510,.T.);
#23464=ORIENTED_EDGE('',*,*,#16511,.F.);
#23465=ORIENTED_EDGE('',*,*,#16510,.F.);
#23466=ORIENTED_EDGE('',*,*,#16507,.T.);
#23467=ORIENTED_EDGE('',*,*,#16512,.T.);
#23468=ORIENTED_EDGE('',*,*,#16513,.F.);
#23469=ORIENTED_EDGE('',*,*,#16512,.F.);
#23470=ORIENTED_EDGE('',*,*,#16506,.F.);
#23471=ORIENTED_EDGE('',*,*,#16514,.F.);
#23472=ORIENTED_EDGE('',*,*,#16515,.T.);
#23473=ORIENTED_EDGE('',*,*,#16516,.F.);
#23474=ORIENTED_EDGE('',*,*,#16517,.F.);
#23475=ORIENTED_EDGE('',*,*,#16518,.F.);
#23476=ORIENTED_EDGE('',*,*,#16517,.T.);
#23477=ORIENTED_EDGE('',*,*,#16519,.T.);
#23478=ORIENTED_EDGE('',*,*,#16520,.F.);
#23479=ORIENTED_EDGE('',*,*,#16519,.F.);
#23480=ORIENTED_EDGE('',*,*,#16516,.T.);
#23481=ORIENTED_EDGE('',*,*,#16521,.T.);
#23482=ORIENTED_EDGE('',*,*,#16522,.F.);
#23483=ORIENTED_EDGE('',*,*,#16521,.F.);
#23484=ORIENTED_EDGE('',*,*,#16515,.F.);
#23485=ORIENTED_EDGE('',*,*,#16523,.F.);
#23486=ORIENTED_EDGE('',*,*,#16524,.T.);
#23487=ORIENTED_EDGE('',*,*,#16525,.T.);
#23488=ORIENTED_EDGE('',*,*,#16526,.F.);
#23489=ORIENTED_EDGE('',*,*,#16527,.T.);
#23490=ORIENTED_EDGE('',*,*,#16528,.F.);
#23491=ORIENTED_EDGE('',*,*,#16524,.F.);
#23492=ORIENTED_EDGE('',*,*,#16529,.F.);
#23493=ORIENTED_EDGE('',*,*,#16525,.F.);
#23494=ORIENTED_EDGE('',*,*,#16528,.T.);
#23495=ORIENTED_EDGE('',*,*,#16530,.T.);
#23496=ORIENTED_EDGE('',*,*,#16531,.F.);
#23497=ORIENTED_EDGE('',*,*,#16530,.F.);
#23498=ORIENTED_EDGE('',*,*,#16527,.F.);
#23499=ORIENTED_EDGE('',*,*,#16532,.F.);
#23500=ORIENTED_EDGE('',*,*,#16533,.T.);
#23501=ORIENTED_EDGE('',*,*,#16534,.F.);
#23502=ORIENTED_EDGE('',*,*,#16535,.F.);
#23503=ORIENTED_EDGE('',*,*,#16536,.F.);
#23504=ORIENTED_EDGE('',*,*,#16535,.T.);
#23505=ORIENTED_EDGE('',*,*,#16537,.T.);
#23506=ORIENTED_EDGE('',*,*,#16538,.F.);
#23507=ORIENTED_EDGE('',*,*,#16537,.F.);
#23508=ORIENTED_EDGE('',*,*,#16534,.T.);
#23509=ORIENTED_EDGE('',*,*,#16539,.T.);
#23510=ORIENTED_EDGE('',*,*,#16540,.F.);
#23511=ORIENTED_EDGE('',*,*,#16539,.F.);
#23512=ORIENTED_EDGE('',*,*,#16533,.F.);
#23513=ORIENTED_EDGE('',*,*,#16541,.F.);
#23514=ORIENTED_EDGE('',*,*,#16542,.T.);
#23515=ORIENTED_EDGE('',*,*,#16543,.F.);
#23516=ORIENTED_EDGE('',*,*,#16544,.F.);
#23517=ORIENTED_EDGE('',*,*,#16545,.F.);
#23518=ORIENTED_EDGE('',*,*,#16544,.T.);
#23519=ORIENTED_EDGE('',*,*,#16546,.T.);
#23520=ORIENTED_EDGE('',*,*,#16547,.F.);
#23521=ORIENTED_EDGE('',*,*,#16546,.F.);
#23522=ORIENTED_EDGE('',*,*,#16543,.T.);
#23523=ORIENTED_EDGE('',*,*,#16548,.T.);
#23524=ORIENTED_EDGE('',*,*,#16549,.F.);
#23525=ORIENTED_EDGE('',*,*,#16548,.F.);
#23526=ORIENTED_EDGE('',*,*,#16542,.F.);
#23527=ORIENTED_EDGE('',*,*,#16550,.F.);
#23528=ORIENTED_EDGE('',*,*,#16551,.T.);
#23529=ORIENTED_EDGE('',*,*,#16552,.F.);
#23530=ORIENTED_EDGE('',*,*,#16553,.F.);
#23531=ORIENTED_EDGE('',*,*,#16554,.F.);
#23532=ORIENTED_EDGE('',*,*,#16553,.T.);
#23533=ORIENTED_EDGE('',*,*,#16555,.T.);
#23534=ORIENTED_EDGE('',*,*,#16556,.F.);
#23535=ORIENTED_EDGE('',*,*,#16555,.F.);
#23536=ORIENTED_EDGE('',*,*,#16552,.T.);
#23537=ORIENTED_EDGE('',*,*,#16557,.T.);
#23538=ORIENTED_EDGE('',*,*,#16558,.F.);
#23539=ORIENTED_EDGE('',*,*,#16557,.F.);
#23540=ORIENTED_EDGE('',*,*,#16551,.F.);
#23541=ORIENTED_EDGE('',*,*,#16559,.F.);
#23542=ORIENTED_EDGE('',*,*,#16560,.T.);
#23543=ORIENTED_EDGE('',*,*,#16561,.F.);
#23544=ORIENTED_EDGE('',*,*,#16562,.F.);
#23545=ORIENTED_EDGE('',*,*,#16563,.F.);
#23546=ORIENTED_EDGE('',*,*,#16562,.T.);
#23547=ORIENTED_EDGE('',*,*,#16564,.T.);
#23548=ORIENTED_EDGE('',*,*,#16565,.F.);
#23549=ORIENTED_EDGE('',*,*,#16564,.F.);
#23550=ORIENTED_EDGE('',*,*,#16561,.T.);
#23551=ORIENTED_EDGE('',*,*,#16566,.T.);
#23552=ORIENTED_EDGE('',*,*,#16567,.F.);
#23553=ORIENTED_EDGE('',*,*,#16566,.F.);
#23554=ORIENTED_EDGE('',*,*,#16560,.F.);
#23555=ORIENTED_EDGE('',*,*,#16568,.F.);
#23556=ORIENTED_EDGE('',*,*,#16569,.T.);
#23557=ORIENTED_EDGE('',*,*,#16570,.F.);
#23558=ORIENTED_EDGE('',*,*,#16571,.F.);
#23559=ORIENTED_EDGE('',*,*,#16572,.F.);
#23560=ORIENTED_EDGE('',*,*,#16571,.T.);
#23561=ORIENTED_EDGE('',*,*,#16573,.T.);
#23562=ORIENTED_EDGE('',*,*,#16574,.F.);
#23563=ORIENTED_EDGE('',*,*,#16573,.F.);
#23564=ORIENTED_EDGE('',*,*,#16570,.T.);
#23565=ORIENTED_EDGE('',*,*,#16575,.T.);
#23566=ORIENTED_EDGE('',*,*,#16576,.F.);
#23567=ORIENTED_EDGE('',*,*,#16575,.F.);
#23568=ORIENTED_EDGE('',*,*,#16569,.F.);
#23569=ORIENTED_EDGE('',*,*,#16577,.F.);
#23570=ORIENTED_EDGE('',*,*,#16578,.T.);
#23571=ORIENTED_EDGE('',*,*,#16579,.F.);
#23572=ORIENTED_EDGE('',*,*,#16580,.F.);
#23573=ORIENTED_EDGE('',*,*,#16581,.F.);
#23574=ORIENTED_EDGE('',*,*,#16580,.T.);
#23575=ORIENTED_EDGE('',*,*,#16582,.T.);
#23576=ORIENTED_EDGE('',*,*,#16583,.F.);
#23577=ORIENTED_EDGE('',*,*,#16582,.F.);
#23578=ORIENTED_EDGE('',*,*,#16579,.T.);
#23579=ORIENTED_EDGE('',*,*,#16584,.T.);
#23580=ORIENTED_EDGE('',*,*,#16585,.F.);
#23581=ORIENTED_EDGE('',*,*,#16584,.F.);
#23582=ORIENTED_EDGE('',*,*,#16578,.F.);
#23583=ORIENTED_EDGE('',*,*,#16586,.F.);
#23584=ORIENTED_EDGE('',*,*,#16587,.T.);
#23585=ORIENTED_EDGE('',*,*,#16588,.F.);
#23586=ORIENTED_EDGE('',*,*,#16589,.F.);
#23587=ORIENTED_EDGE('',*,*,#16590,.F.);
#23588=ORIENTED_EDGE('',*,*,#16589,.T.);
#23589=ORIENTED_EDGE('',*,*,#16591,.T.);
#23590=ORIENTED_EDGE('',*,*,#16592,.F.);
#23591=ORIENTED_EDGE('',*,*,#16591,.F.);
#23592=ORIENTED_EDGE('',*,*,#16588,.T.);
#23593=ORIENTED_EDGE('',*,*,#16593,.T.);
#23594=ORIENTED_EDGE('',*,*,#16594,.F.);
#23595=ORIENTED_EDGE('',*,*,#16593,.F.);
#23596=ORIENTED_EDGE('',*,*,#16587,.F.);
#23597=ORIENTED_EDGE('',*,*,#16595,.F.);
#23598=ORIENTED_EDGE('',*,*,#16596,.T.);
#23599=ORIENTED_EDGE('',*,*,#16597,.F.);
#23600=ORIENTED_EDGE('',*,*,#16598,.F.);
#23601=ORIENTED_EDGE('',*,*,#16599,.F.);
#23602=ORIENTED_EDGE('',*,*,#16598,.T.);
#23603=ORIENTED_EDGE('',*,*,#16600,.T.);
#23604=ORIENTED_EDGE('',*,*,#16601,.F.);
#23605=ORIENTED_EDGE('',*,*,#16600,.F.);
#23606=ORIENTED_EDGE('',*,*,#16597,.T.);
#23607=ORIENTED_EDGE('',*,*,#16602,.T.);
#23608=ORIENTED_EDGE('',*,*,#16603,.F.);
#23609=ORIENTED_EDGE('',*,*,#16602,.F.);
#23610=ORIENTED_EDGE('',*,*,#16596,.F.);
#23611=ORIENTED_EDGE('',*,*,#16604,.F.);
#23612=ORIENTED_EDGE('',*,*,#16605,.T.);
#23613=ORIENTED_EDGE('',*,*,#16606,.F.);
#23614=ORIENTED_EDGE('',*,*,#16607,.F.);
#23615=ORIENTED_EDGE('',*,*,#16608,.F.);
#23616=ORIENTED_EDGE('',*,*,#16607,.T.);
#23617=ORIENTED_EDGE('',*,*,#16609,.T.);
#23618=ORIENTED_EDGE('',*,*,#16610,.F.);
#23619=ORIENTED_EDGE('',*,*,#16609,.F.);
#23620=ORIENTED_EDGE('',*,*,#16606,.T.);
#23621=ORIENTED_EDGE('',*,*,#16611,.T.);
#23622=ORIENTED_EDGE('',*,*,#16612,.F.);
#23623=ORIENTED_EDGE('',*,*,#16611,.F.);
#23624=ORIENTED_EDGE('',*,*,#16605,.F.);
#23625=ORIENTED_EDGE('',*,*,#16613,.F.);
#23626=ORIENTED_EDGE('',*,*,#16252,.F.);
#23627=ORIENTED_EDGE('',*,*,#16107,.F.);
#23628=ORIENTED_EDGE('',*,*,#16253,.F.);
#23629=ORIENTED_EDGE('',*,*,#16614,.T.);
#23630=ORIENTED_EDGE('',*,*,#16613,.T.);
#23631=ORIENTED_EDGE('',*,*,#16614,.F.);
#23632=ORIENTED_EDGE('',*,*,#16615,.F.);
#23633=ORIENTED_EDGE('',*,*,#16616,.T.);
#23634=ORIENTED_EDGE('',*,*,#16261,.T.);
#23635=ORIENTED_EDGE('',*,*,#16616,.F.);
#23636=ORIENTED_EDGE('',*,*,#16287,.T.);
#23637=ORIENTED_EDGE('',*,*,#16617,.F.);
#23638=ORIENTED_EDGE('',*,*,#16601,.T.);
#23639=ORIENTED_EDGE('',*,*,#16603,.T.);
#23640=ORIENTED_EDGE('',*,*,#16595,.T.);
#23641=ORIENTED_EDGE('',*,*,#16618,.F.);
#23642=ORIENTED_EDGE('',*,*,#16302,.T.);
#23643=ORIENTED_EDGE('',*,*,#16304,.T.);
#23644=ORIENTED_EDGE('',*,*,#16296,.T.);
#23645=ORIENTED_EDGE('',*,*,#16619,.F.);
#23646=ORIENTED_EDGE('',*,*,#16592,.T.);
#23647=ORIENTED_EDGE('',*,*,#16594,.T.);
#23648=ORIENTED_EDGE('',*,*,#16586,.T.);
#23649=ORIENTED_EDGE('',*,*,#16620,.F.);
#23650=ORIENTED_EDGE('',*,*,#16311,.T.);
#23651=ORIENTED_EDGE('',*,*,#16313,.T.);
#23652=ORIENTED_EDGE('',*,*,#16305,.T.);
#23653=ORIENTED_EDGE('',*,*,#16621,.F.);
#23654=ORIENTED_EDGE('',*,*,#16583,.T.);
#23655=ORIENTED_EDGE('',*,*,#16585,.T.);
#23656=ORIENTED_EDGE('',*,*,#16577,.T.);
#23657=ORIENTED_EDGE('',*,*,#16622,.F.);
#23658=ORIENTED_EDGE('',*,*,#16320,.T.);
#23659=ORIENTED_EDGE('',*,*,#16322,.T.);
#23660=ORIENTED_EDGE('',*,*,#16314,.T.);
#23661=ORIENTED_EDGE('',*,*,#16623,.F.);
#23662=ORIENTED_EDGE('',*,*,#16574,.T.);
#23663=ORIENTED_EDGE('',*,*,#16576,.T.);
#23664=ORIENTED_EDGE('',*,*,#16568,.T.);
#23665=ORIENTED_EDGE('',*,*,#16624,.F.);
#23666=ORIENTED_EDGE('',*,*,#16329,.T.);
#23667=ORIENTED_EDGE('',*,*,#16331,.T.);
#23668=ORIENTED_EDGE('',*,*,#16323,.T.);
#23669=ORIENTED_EDGE('',*,*,#16625,.F.);
#23670=ORIENTED_EDGE('',*,*,#16565,.T.);
#23671=ORIENTED_EDGE('',*,*,#16567,.T.);
#23672=ORIENTED_EDGE('',*,*,#16559,.T.);
#23673=ORIENTED_EDGE('',*,*,#16626,.F.);
#23674=ORIENTED_EDGE('',*,*,#16338,.T.);
#23675=ORIENTED_EDGE('',*,*,#16340,.T.);
#23676=ORIENTED_EDGE('',*,*,#16332,.T.);
#23677=ORIENTED_EDGE('',*,*,#16627,.F.);
#23678=ORIENTED_EDGE('',*,*,#16556,.T.);
#23679=ORIENTED_EDGE('',*,*,#16558,.T.);
#23680=ORIENTED_EDGE('',*,*,#16550,.T.);
#23681=ORIENTED_EDGE('',*,*,#16628,.F.);
#23682=ORIENTED_EDGE('',*,*,#16347,.T.);
#23683=ORIENTED_EDGE('',*,*,#16349,.T.);
#23684=ORIENTED_EDGE('',*,*,#16341,.T.);
#23685=ORIENTED_EDGE('',*,*,#16629,.F.);
#23686=ORIENTED_EDGE('',*,*,#16547,.T.);
#23687=ORIENTED_EDGE('',*,*,#16549,.T.);
#23688=ORIENTED_EDGE('',*,*,#16541,.T.);
#23689=ORIENTED_EDGE('',*,*,#16630,.F.);
#23690=ORIENTED_EDGE('',*,*,#16356,.T.);
#23691=ORIENTED_EDGE('',*,*,#16358,.T.);
#23692=ORIENTED_EDGE('',*,*,#16350,.T.);
#23693=ORIENTED_EDGE('',*,*,#16631,.F.);
#23694=ORIENTED_EDGE('',*,*,#16538,.T.);
#23695=ORIENTED_EDGE('',*,*,#16540,.T.);
#23696=ORIENTED_EDGE('',*,*,#16532,.T.);
#23697=ORIENTED_EDGE('',*,*,#16632,.F.);
#23698=ORIENTED_EDGE('',*,*,#16366,.T.);
#23699=ORIENTED_EDGE('',*,*,#16368,.T.);
#23700=ORIENTED_EDGE('',*,*,#16633,.T.);
#23701=ORIENTED_EDGE('',*,*,#16615,.T.);
#23702=ORIENTED_EDGE('',*,*,#16633,.F.);
#23703=ORIENTED_EDGE('',*,*,#16369,.T.);
#23704=ORIENTED_EDGE('',*,*,#16359,.T.);
#23705=ORIENTED_EDGE('',*,*,#16634,.F.);
#23706=ORIENTED_EDGE('',*,*,#16376,.T.);
#23707=ORIENTED_EDGE('',*,*,#16378,.T.);
#23708=ORIENTED_EDGE('',*,*,#16370,.T.);
#23709=ORIENTED_EDGE('',*,*,#16635,.F.);
#23710=ORIENTED_EDGE('',*,*,#16520,.T.);
#23711=ORIENTED_EDGE('',*,*,#16522,.T.);
#23712=ORIENTED_EDGE('',*,*,#16514,.T.);
#23713=ORIENTED_EDGE('',*,*,#16636,.F.);
#23714=ORIENTED_EDGE('',*,*,#16385,.T.);
#23715=ORIENTED_EDGE('',*,*,#16387,.T.);
#23716=ORIENTED_EDGE('',*,*,#16379,.T.);
#23717=ORIENTED_EDGE('',*,*,#16637,.F.);
#23718=ORIENTED_EDGE('',*,*,#16511,.T.);
#23719=ORIENTED_EDGE('',*,*,#16513,.T.);
#23720=ORIENTED_EDGE('',*,*,#16505,.T.);
#23721=ORIENTED_EDGE('',*,*,#16638,.F.);
#23722=ORIENTED_EDGE('',*,*,#16394,.T.);
#23723=ORIENTED_EDGE('',*,*,#16396,.T.);
#23724=ORIENTED_EDGE('',*,*,#16388,.T.);
#23725=ORIENTED_EDGE('',*,*,#16639,.F.);
#23726=ORIENTED_EDGE('',*,*,#16502,.T.);
#23727=ORIENTED_EDGE('',*,*,#16504,.T.);
#23728=ORIENTED_EDGE('',*,*,#16496,.T.);
#23729=ORIENTED_EDGE('',*,*,#16640,.F.);
#23730=ORIENTED_EDGE('',*,*,#16403,.T.);
#23731=ORIENTED_EDGE('',*,*,#16405,.T.);
#23732=ORIENTED_EDGE('',*,*,#16397,.T.);
#23733=ORIENTED_EDGE('',*,*,#16641,.F.);
#23734=ORIENTED_EDGE('',*,*,#16493,.T.);
#23735=ORIENTED_EDGE('',*,*,#16495,.T.);
#23736=ORIENTED_EDGE('',*,*,#16487,.T.);
#23737=ORIENTED_EDGE('',*,*,#16642,.F.);
#23738=ORIENTED_EDGE('',*,*,#16412,.T.);
#23739=ORIENTED_EDGE('',*,*,#16414,.T.);
#23740=ORIENTED_EDGE('',*,*,#16406,.T.);
#23741=ORIENTED_EDGE('',*,*,#16643,.F.);
#23742=ORIENTED_EDGE('',*,*,#16484,.T.);
#23743=ORIENTED_EDGE('',*,*,#16486,.T.);
#23744=ORIENTED_EDGE('',*,*,#16478,.T.);
#23745=ORIENTED_EDGE('',*,*,#16644,.F.);
#23746=ORIENTED_EDGE('',*,*,#16421,.T.);
#23747=ORIENTED_EDGE('',*,*,#16423,.T.);
#23748=ORIENTED_EDGE('',*,*,#16415,.T.);
#23749=ORIENTED_EDGE('',*,*,#16645,.F.);
#23750=ORIENTED_EDGE('',*,*,#16475,.T.);
#23751=ORIENTED_EDGE('',*,*,#16477,.T.);
#23752=ORIENTED_EDGE('',*,*,#16469,.T.);
#23753=ORIENTED_EDGE('',*,*,#16646,.F.);
#23754=ORIENTED_EDGE('',*,*,#16430,.T.);
#23755=ORIENTED_EDGE('',*,*,#16432,.T.);
#23756=ORIENTED_EDGE('',*,*,#16424,.T.);
#23757=ORIENTED_EDGE('',*,*,#16647,.F.);
#23758=ORIENTED_EDGE('',*,*,#16466,.T.);
#23759=ORIENTED_EDGE('',*,*,#16468,.T.);
#23760=ORIENTED_EDGE('',*,*,#16460,.T.);
#23761=ORIENTED_EDGE('',*,*,#16648,.F.);
#23762=ORIENTED_EDGE('',*,*,#16439,.T.);
#23763=ORIENTED_EDGE('',*,*,#16441,.T.);
#23764=ORIENTED_EDGE('',*,*,#16433,.T.);
#23765=ORIENTED_EDGE('',*,*,#16649,.F.);
#23766=ORIENTED_EDGE('',*,*,#16457,.T.);
#23767=ORIENTED_EDGE('',*,*,#16459,.T.);
#23768=ORIENTED_EDGE('',*,*,#16451,.T.);
#23769=ORIENTED_EDGE('',*,*,#16650,.F.);
#23770=ORIENTED_EDGE('',*,*,#16448,.T.);
#23771=ORIENTED_EDGE('',*,*,#16450,.T.);
#23772=ORIENTED_EDGE('',*,*,#16442,.T.);
#23773=ORIENTED_EDGE('',*,*,#16651,.F.);
#23774=ORIENTED_EDGE('',*,*,#16529,.T.);
#23775=ORIENTED_EDGE('',*,*,#16531,.T.);
#23776=ORIENTED_EDGE('',*,*,#16526,.T.);
#23777=ORIENTED_EDGE('',*,*,#16652,.F.);
#23778=ORIENTED_EDGE('',*,*,#16610,.T.);
#23779=ORIENTED_EDGE('',*,*,#16612,.T.);
#23780=ORIENTED_EDGE('',*,*,#16604,.T.);
#23781=ORIENTED_EDGE('',*,*,#16653,.F.);
#23782=ORIENTED_EDGE('',*,*,#16293,.T.);
#23783=ORIENTED_EDGE('',*,*,#16295,.T.);
#23784=ORIENTED_EDGE('',*,*,#16654,.F.);
#23785=ORIENTED_EDGE('',*,*,#16655,.T.);
#23786=ORIENTED_EDGE('',*,*,#16365,.T.);
#23787=ORIENTED_EDGE('',*,*,#16632,.T.);
#23788=ORIENTED_EDGE('',*,*,#16536,.T.);
#23789=ORIENTED_EDGE('',*,*,#16631,.T.);
#23790=ORIENTED_EDGE('',*,*,#16354,.T.);
#23791=ORIENTED_EDGE('',*,*,#16630,.T.);
#23792=ORIENTED_EDGE('',*,*,#16545,.T.);
#23793=ORIENTED_EDGE('',*,*,#16629,.T.);
#23794=ORIENTED_EDGE('',*,*,#16345,.T.);
#23795=ORIENTED_EDGE('',*,*,#16628,.T.);
#23796=ORIENTED_EDGE('',*,*,#16554,.T.);
#23797=ORIENTED_EDGE('',*,*,#16627,.T.);
#23798=ORIENTED_EDGE('',*,*,#16336,.T.);
#23799=ORIENTED_EDGE('',*,*,#16626,.T.);
#23800=ORIENTED_EDGE('',*,*,#16563,.T.);
#23801=ORIENTED_EDGE('',*,*,#16625,.T.);
#23802=ORIENTED_EDGE('',*,*,#16327,.T.);
#23803=ORIENTED_EDGE('',*,*,#16624,.T.);
#23804=ORIENTED_EDGE('',*,*,#16572,.T.);
#23805=ORIENTED_EDGE('',*,*,#16623,.T.);
#23806=ORIENTED_EDGE('',*,*,#16318,.T.);
#23807=ORIENTED_EDGE('',*,*,#16622,.T.);
#23808=ORIENTED_EDGE('',*,*,#16581,.T.);
#23809=ORIENTED_EDGE('',*,*,#16621,.T.);
#23810=ORIENTED_EDGE('',*,*,#16309,.T.);
#23811=ORIENTED_EDGE('',*,*,#16620,.T.);
#23812=ORIENTED_EDGE('',*,*,#16590,.T.);
#23813=ORIENTED_EDGE('',*,*,#16619,.T.);
#23814=ORIENTED_EDGE('',*,*,#16300,.T.);
#23815=ORIENTED_EDGE('',*,*,#16618,.T.);
#23816=ORIENTED_EDGE('',*,*,#16599,.T.);
#23817=ORIENTED_EDGE('',*,*,#16617,.T.);
#23818=ORIENTED_EDGE('',*,*,#16291,.T.);
#23819=ORIENTED_EDGE('',*,*,#16653,.T.);
#23820=ORIENTED_EDGE('',*,*,#16608,.T.);
#23821=ORIENTED_EDGE('',*,*,#16652,.T.);
#23822=ORIENTED_EDGE('',*,*,#16523,.T.);
#23823=ORIENTED_EDGE('',*,*,#16651,.T.);
#23824=ORIENTED_EDGE('',*,*,#16446,.T.);
#23825=ORIENTED_EDGE('',*,*,#16650,.T.);
#23826=ORIENTED_EDGE('',*,*,#16455,.T.);
#23827=ORIENTED_EDGE('',*,*,#16649,.T.);
#23828=ORIENTED_EDGE('',*,*,#16437,.T.);
#23829=ORIENTED_EDGE('',*,*,#16648,.T.);
#23830=ORIENTED_EDGE('',*,*,#16464,.T.);
#23831=ORIENTED_EDGE('',*,*,#16647,.T.);
#23832=ORIENTED_EDGE('',*,*,#16428,.T.);
#23833=ORIENTED_EDGE('',*,*,#16646,.T.);
#23834=ORIENTED_EDGE('',*,*,#16473,.T.);
#23835=ORIENTED_EDGE('',*,*,#16645,.T.);
#23836=ORIENTED_EDGE('',*,*,#16419,.T.);
#23837=ORIENTED_EDGE('',*,*,#16644,.T.);
#23838=ORIENTED_EDGE('',*,*,#16482,.T.);
#23839=ORIENTED_EDGE('',*,*,#16643,.T.);
#23840=ORIENTED_EDGE('',*,*,#16410,.T.);
#23841=ORIENTED_EDGE('',*,*,#16642,.T.);
#23842=ORIENTED_EDGE('',*,*,#16491,.T.);
#23843=ORIENTED_EDGE('',*,*,#16641,.T.);
#23844=ORIENTED_EDGE('',*,*,#16401,.T.);
#23845=ORIENTED_EDGE('',*,*,#16640,.T.);
#23846=ORIENTED_EDGE('',*,*,#16500,.T.);
#23847=ORIENTED_EDGE('',*,*,#16639,.T.);
#23848=ORIENTED_EDGE('',*,*,#16392,.T.);
#23849=ORIENTED_EDGE('',*,*,#16638,.T.);
#23850=ORIENTED_EDGE('',*,*,#16509,.T.);
#23851=ORIENTED_EDGE('',*,*,#16637,.T.);
#23852=ORIENTED_EDGE('',*,*,#16383,.T.);
#23853=ORIENTED_EDGE('',*,*,#16636,.T.);
#23854=ORIENTED_EDGE('',*,*,#16518,.T.);
#23855=ORIENTED_EDGE('',*,*,#16635,.T.);
#23856=ORIENTED_EDGE('',*,*,#16374,.T.);
#23857=ORIENTED_EDGE('',*,*,#16634,.T.);
#23858=ORIENTED_EDGE('',*,*,#16363,.T.);
#23859=ORIENTED_EDGE('',*,*,#16655,.F.);
#23860=ORIENTED_EDGE('',*,*,#16654,.T.);
#23861=ORIENTED_EDGE('',*,*,#16275,.T.);
#23862=ORIENTED_EDGE('',*,*,#16286,.T.);
#23863=ORIENTED_EDGE('',*,*,#16284,.T.);
#23864=ORIENTED_EDGE('',*,*,#16282,.T.);
#23865=ORIENTED_EDGE('',*,*,#16280,.T.);
#23866=ORIENTED_EDGE('',*,*,#16278,.T.);
#25104=CONICAL_SURFACE('',#28708,0.23094010767585,1.03037682652431);
#25105=CONICAL_SURFACE('',#28935,0.475,0.78539816339745);
#25106=CONICAL_SURFACE('',#28936,0.785,0.785398163397449);
#25107=CONICAL_SURFACE('',#28975,0.775,0.785398163397448);
#26237=ADVANCED_FACE('',(#3649),#1462,.T.);
#26238=ADVANCED_FACE('',(#3650),#1463,.T.);
#26239=ADVANCED_FACE('',(#3651),#1464,.T.);
#26240=ADVANCED_FACE('',(#3652),#1465,.T.);
#26241=ADVANCED_FACE('',(#3653),#1466,.T.);
#26242=ADVANCED_FACE('',(#3654),#1467,.T.);
#26243=ADVANCED_FACE('',(#3655),#1468,.T.);
#26244=ADVANCED_FACE('',(#3656),#1469,.T.);
#26245=ADVANCED_FACE('',(#3657),#1470,.T.);
#26246=ADVANCED_FACE('',(#3658),#1471,.T.);
#26247=ADVANCED_FACE('',(#3659),#1472,.T.);
#26248=ADVANCED_FACE('',(#3660),#1473,.T.);
#26249=ADVANCED_FACE('',(#3661),#1474,.T.);
#26250=ADVANCED_FACE('',(#3662),#1475,.T.);
#26251=ADVANCED_FACE('',(#3663),#1476,.T.);
#26252=ADVANCED_FACE('',(#3664),#1477,.T.);
#26253=ADVANCED_FACE('',(#3665),#1478,.T.);
#26254=ADVANCED_FACE('',(#3666),#1479,.T.);
#26255=ADVANCED_FACE('',(#3667),#1480,.T.);
#26256=ADVANCED_FACE('',(#3668),#1481,.T.);
#26257=ADVANCED_FACE('',(#3669),#1482,.T.);
#26258=ADVANCED_FACE('',(#3670),#1483,.T.);
#26259=ADVANCED_FACE('',(#3671),#1484,.T.);
#26260=ADVANCED_FACE('',(#3672),#1485,.T.);
#26261=ADVANCED_FACE('',(#3673),#1486,.T.);
#26262=ADVANCED_FACE('',(#3674),#1487,.T.);
#26263=ADVANCED_FACE('',(#3675),#1488,.T.);
#26264=ADVANCED_FACE('',(#3676),#1489,.T.);
#26265=ADVANCED_FACE('',(#3677),#1490,.T.);
#26266=ADVANCED_FACE('',(#3678),#1491,.T.);
#26267=ADVANCED_FACE('',(#3679),#1492,.T.);
#26268=ADVANCED_FACE('',(#3680),#1493,.T.);
#26269=ADVANCED_FACE('',(#3681),#1494,.T.);
#26270=ADVANCED_FACE('',(#3682),#1495,.T.);
#26271=ADVANCED_FACE('',(#3683),#1496,.T.);
#26272=ADVANCED_FACE('',(#3684),#1497,.T.);
#26273=ADVANCED_FACE('',(#3685),#1498,.T.);
#26274=ADVANCED_FACE('',(#3686),#1499,.T.);
#26275=ADVANCED_FACE('',(#3687),#1500,.T.);
#26276=ADVANCED_FACE('',(#3688),#1501,.T.);
#26277=ADVANCED_FACE('',(#3689),#1502,.T.);
#26278=ADVANCED_FACE('',(#3690),#1503,.T.);
#26279=ADVANCED_FACE('',(#3691),#1504,.T.);
#26280=ADVANCED_FACE('',(#3692),#1505,.T.);
#26281=ADVANCED_FACE('',(#3693),#1506,.T.);
#26282=ADVANCED_FACE('',(#3694),#1507,.T.);
#26283=ADVANCED_FACE('',(#3695),#2202,.F.);
#26284=ADVANCED_FACE('',(#3696),#170,.F.);
#26285=ADVANCED_FACE('',(#3697),#2203,.T.);
#26286=ADVANCED_FACE('',(#3698),#1508,.T.);
#26287=ADVANCED_FACE('',(#3699),#171,.F.);
#26288=ADVANCED_FACE('',(#3700),#1087,.F.);
#26289=ADVANCED_FACE('',(#3701),#1509,.T.);
#26290=ADVANCED_FACE('',(#3702,#1652),#2204,.T.);
#26291=ADVANCED_FACE('',(#3703),#2205,.F.);
#26292=ADVANCED_FACE('',(#3704),#2206,.F.);
#26293=ADVANCED_FACE('',(#3705),#2207,.F.);
#26294=ADVANCED_FACE('',(#3706),#2208,.F.);
#26295=ADVANCED_FACE('',(#3707),#2209,.F.);
#26296=ADVANCED_FACE('',(#3708),#2210,.F.);
#26297=ADVANCED_FACE('',(#3709),#25104,.F.);
#26298=ADVANCED_FACE('',(#3710),#2211,.F.);
#26299=ADVANCED_FACE('',(#3711),#2212,.F.);
#26300=ADVANCED_FACE('',(#3712),#2213,.F.);
#26301=ADVANCED_FACE('',(#3713),#2214,.F.);
#26302=ADVANCED_FACE('',(#3714),#2215,.F.);
#26303=ADVANCED_FACE('',(#3715),#2216,.F.);
#26304=ADVANCED_FACE('',(#3716),#2217,.F.);
#26305=ADVANCED_FACE('',(#3717),#2218,.F.);
#26306=ADVANCED_FACE('',(#3718),#2219,.F.);
#26307=ADVANCED_FACE('',(#3719),#2220,.F.);
#26308=ADVANCED_FACE('',(#3720),#2221,.F.);
#26309=ADVANCED_FACE('',(#3721),#2222,.F.);
#26310=ADVANCED_FACE('',(#3722),#2223,.F.);
#26311=ADVANCED_FACE('',(#3723),#2224,.F.);
#26312=ADVANCED_FACE('',(#3724),#2225,.F.);
#26313=ADVANCED_FACE('',(#3725),#2226,.F.);
#26314=ADVANCED_FACE('',(#3726),#2227,.F.);
#26315=ADVANCED_FACE('',(#3727),#2228,.F.);
#26316=ADVANCED_FACE('',(#3728),#2229,.F.);
#26317=ADVANCED_FACE('',(#3729),#2230,.F.);
#26318=ADVANCED_FACE('',(#3730),#2231,.F.);
#26319=ADVANCED_FACE('',(#3731),#2232,.F.);
#26320=ADVANCED_FACE('',(#3732),#2233,.F.);
#26321=ADVANCED_FACE('',(#3733),#2234,.F.);
#26322=ADVANCED_FACE('',(#3734),#2235,.F.);
#26323=ADVANCED_FACE('',(#3735),#2236,.F.);
#26324=ADVANCED_FACE('',(#3736),#2237,.F.);
#26325=ADVANCED_FACE('',(#3737),#2238,.F.);
#26326=ADVANCED_FACE('',(#3738),#2239,.F.);
#26327=ADVANCED_FACE('',(#3739),#2240,.F.);
#26328=ADVANCED_FACE('',(#3740),#2241,.F.);
#26329=ADVANCED_FACE('',(#3741),#2242,.F.);
#26330=ADVANCED_FACE('',(#3742),#2243,.F.);
#26331=ADVANCED_FACE('',(#3743),#2244,.F.);
#26332=ADVANCED_FACE('',(#3744),#2245,.F.);
#26333=ADVANCED_FACE('',(#3745),#2246,.F.);
#26334=ADVANCED_FACE('',(#3746),#2247,.F.);
#26335=ADVANCED_FACE('',(#3747),#2248,.F.);
#26336=ADVANCED_FACE('',(#3748),#2249,.F.);
#26337=ADVANCED_FACE('',(#3749),#2250,.F.);
#26338=ADVANCED_FACE('',(#3750),#2251,.F.);
#26339=ADVANCED_FACE('',(#3751),#2252,.F.);
#26340=ADVANCED_FACE('',(#3752),#2253,.F.);
#26341=ADVANCED_FACE('',(#3753),#2254,.F.);
#26342=ADVANCED_FACE('',(#3754),#2255,.F.);
#26343=ADVANCED_FACE('',(#3755),#2256,.F.);
#26344=ADVANCED_FACE('',(#3756),#2257,.F.);
#26345=ADVANCED_FACE('',(#3757),#2258,.F.);
#26346=ADVANCED_FACE('',(#3758),#2259,.F.);
#26347=ADVANCED_FACE('',(#3759),#2260,.F.);
#26348=ADVANCED_FACE('',(#3760),#2261,.F.);
#26349=ADVANCED_FACE('',(#3761),#2262,.F.);
#26350=ADVANCED_FACE('',(#3762),#2263,.F.);
#26351=ADVANCED_FACE('',(#3763),#2264,.F.);
#26352=ADVANCED_FACE('',(#3764),#2265,.F.);
#26353=ADVANCED_FACE('',(#3765),#2266,.F.);
#26354=ADVANCED_FACE('',(#3766),#2267,.F.);
#26355=ADVANCED_FACE('',(#3767),#2268,.F.);
#26356=ADVANCED_FACE('',(#3768),#2269,.F.);
#26357=ADVANCED_FACE('',(#3769),#2270,.F.);
#26358=ADVANCED_FACE('',(#3770),#2271,.F.);
#26359=ADVANCED_FACE('',(#3771),#2272,.F.);
#26360=ADVANCED_FACE('',(#3772),#2273,.F.);
#26361=ADVANCED_FACE('',(#3773),#2274,.F.);
#26362=ADVANCED_FACE('',(#3774),#2275,.F.);
#26363=ADVANCED_FACE('',(#3775),#2276,.F.);
#26364=ADVANCED_FACE('',(#3776),#2277,.F.);
#26365=ADVANCED_FACE('',(#3777),#2278,.F.);
#26366=ADVANCED_FACE('',(#3778),#2279,.F.);
#26367=ADVANCED_FACE('',(#3779),#2280,.F.);
#26368=ADVANCED_FACE('',(#3780),#2281,.F.);
#26369=ADVANCED_FACE('',(#3781),#2282,.F.);
#26370=ADVANCED_FACE('',(#3782),#2283,.F.);
#26371=ADVANCED_FACE('',(#3783),#2284,.F.);
#26372=ADVANCED_FACE('',(#3784),#2285,.F.);
#26373=ADVANCED_FACE('',(#3785),#2286,.F.);
#26374=ADVANCED_FACE('',(#3786),#2287,.F.);
#26375=ADVANCED_FACE('',(#3787),#2288,.F.);
#26376=ADVANCED_FACE('',(#3788),#2289,.F.);
#26377=ADVANCED_FACE('',(#3789),#2290,.F.);
#26378=ADVANCED_FACE('',(#3790),#2291,.F.);
#26379=ADVANCED_FACE('',(#3791),#2292,.F.);
#26380=ADVANCED_FACE('',(#3792),#2293,.F.);
#26381=ADVANCED_FACE('',(#3793),#2294,.F.);
#26382=ADVANCED_FACE('',(#3794),#2295,.F.);
#26383=ADVANCED_FACE('',(#3795),#2296,.F.);
#26384=ADVANCED_FACE('',(#3796),#2297,.F.);
#26385=ADVANCED_FACE('',(#3797),#2298,.F.);
#26386=ADVANCED_FACE('',(#3798),#2299,.F.);
#26387=ADVANCED_FACE('',(#3799),#2300,.F.);
#26388=ADVANCED_FACE('',(#3800),#2301,.F.);
#26389=ADVANCED_FACE('',(#3801),#2302,.F.);
#26390=ADVANCED_FACE('',(#3802),#2303,.F.);
#26391=ADVANCED_FACE('',(#3803),#2304,.F.);
#26392=ADVANCED_FACE('',(#3804),#2305,.F.);
#26393=ADVANCED_FACE('',(#3805),#2306,.F.);
#26394=ADVANCED_FACE('',(#3806),#2307,.F.);
#26395=ADVANCED_FACE('',(#3807),#2308,.F.);
#26396=ADVANCED_FACE('',(#3808),#2309,.F.);
#26397=ADVANCED_FACE('',(#3809),#2310,.F.);
#26398=ADVANCED_FACE('',(#3810),#2311,.F.);
#26399=ADVANCED_FACE('',(#3811),#2312,.F.);
#26400=ADVANCED_FACE('',(#3812),#2313,.F.);
#26401=ADVANCED_FACE('',(#3813),#2314,.F.);
#26402=ADVANCED_FACE('',(#3814),#2315,.F.);
#26403=ADVANCED_FACE('',(#3815),#2316,.F.);
#26404=ADVANCED_FACE('',(#3816),#2317,.F.);
#26405=ADVANCED_FACE('',(#3817),#2318,.F.);
#26406=ADVANCED_FACE('',(#3818),#2319,.F.);
#26407=ADVANCED_FACE('',(#3819),#2320,.F.);
#26408=ADVANCED_FACE('',(#3820),#2321,.F.);
#26409=ADVANCED_FACE('',(#3821),#2322,.F.);
#26410=ADVANCED_FACE('',(#3822),#2323,.F.);
#26411=ADVANCED_FACE('',(#3823),#2324,.F.);
#26412=ADVANCED_FACE('',(#3824),#2325,.F.);
#26413=ADVANCED_FACE('',(#3825),#2326,.F.);
#26414=ADVANCED_FACE('',(#3826),#2327,.F.);
#26415=ADVANCED_FACE('',(#3827),#2328,.F.);
#26416=ADVANCED_FACE('',(#3828),#2329,.F.);
#26417=ADVANCED_FACE('',(#3829),#2330,.F.);
#26418=ADVANCED_FACE('',(#3830),#2331,.F.);
#26419=ADVANCED_FACE('',(#3831),#2332,.F.);
#26420=ADVANCED_FACE('',(#3832),#2333,.F.);
#26421=ADVANCED_FACE('',(#3833),#2334,.F.);
#26422=ADVANCED_FACE('',(#3834),#2335,.F.);
#26423=ADVANCED_FACE('',(#3835),#2336,.F.);
#26424=ADVANCED_FACE('',(#3836),#2337,.F.);
#26425=ADVANCED_FACE('',(#3837),#2338,.F.);
#26426=ADVANCED_FACE('',(#3838),#2339,.F.);
#26427=ADVANCED_FACE('',(#3839),#2340,.F.);
#26428=ADVANCED_FACE('',(#3840),#2341,.F.);
#26429=ADVANCED_FACE('',(#3841),#2342,.F.);
#26430=ADVANCED_FACE('',(#3842),#2343,.F.);
#26431=ADVANCED_FACE('',(#3843),#2344,.F.);
#26432=ADVANCED_FACE('',(#3844),#2345,.F.);
#26433=ADVANCED_FACE('',(#3845),#2346,.F.);
#26434=ADVANCED_FACE('',(#3846),#2347,.F.);
#26435=ADVANCED_FACE('',(#3847),#2348,.F.);
#26436=ADVANCED_FACE('',(#3848),#2349,.F.);
#26437=ADVANCED_FACE('',(#3849),#2350,.F.);
#26438=ADVANCED_FACE('',(#3850),#2351,.F.);
#26439=ADVANCED_FACE('',(#3851),#2352,.F.);
#26440=ADVANCED_FACE('',(#3852),#2353,.F.);
#26441=ADVANCED_FACE('',(#3853),#2354,.F.);
#26442=ADVANCED_FACE('',(#3854),#2355,.F.);
#26443=ADVANCED_FACE('',(#3855),#2356,.F.);
#26444=ADVANCED_FACE('',(#3856),#2357,.F.);
#26445=ADVANCED_FACE('',(#3857),#2358,.F.);
#26446=ADVANCED_FACE('',(#3858),#2359,.F.);
#26447=ADVANCED_FACE('',(#3859),#2360,.F.);
#26448=ADVANCED_FACE('',(#3860),#2361,.T.);
#26449=ADVANCED_FACE('',(#3861),#25105,.T.);
#26450=ADVANCED_FACE('',(#3862),#25106,.T.);
#26451=ADVANCED_FACE('',(#3863),#1510,.T.);
#26452=ADVANCED_FACE('',(#3864),#25107,.T.);
#26453=ADVANCED_FACE('',(#3865,#1653),#2362,.T.);
#26682=CLOSED_SHELL('',(#26237,#26238,#26239,#26240,#26241,#26242,#26243,
#26244,#26245,#26246,#26247,#26248,#26249,#26250,#26251,#26252,#26253,#26254,
#26255,#26256,#26257,#26258,#26259,#26260,#26261,#26262,#26263,#26264,#26265,
#26266,#26267,#26268,#26269,#26270,#26271,#26272,#26273,#26274,#26275,#26276,
#26277,#26278,#26279,#26280,#26281,#26282,#26283,#26284,#26285,#26286,#26287,
#26288,#26289,#26290,#26291,#26292,#26293,#26294,#26295,#26296,#26297,#26298,
#26299,#26300,#26301,#26302,#26303,#26304,#26305,#26306,#26307,#26308,#26309,
#26310,#26311,#26312,#26313,#26314,#26315,#26316,#26317,#26318,#26319,#26320,
#26321,#26322,#26323,#26324,#26325,#26326,#26327,#26328,#26329,#26330,#26331,
#26332,#26333,#26334,#26335,#26336,#26337,#26338,#26339,#26340,#26341,#26342,
#26343,#26344,#26345,#26346,#26347,#26348,#26349,#26350,#26351,#26352,#26353,
#26354,#26355,#26356,#26357,#26358,#26359,#26360,#26361,#26362,#26363,#26364,
#26365,#26366,#26367,#26368,#26369,#26370,#26371,#26372,#26373,#26374,#26375,
#26376,#26377,#26378,#26379,#26380,#26381,#26382,#26383,#26384,#26385,#26386,
#26387,#26388,#26389,#26390,#26391,#26392,#26393,#26394,#26395,#26396,#26397,
#26398,#26399,#26400,#26401,#26402,#26403,#26404,#26405,#26406,#26407,#26408,
#26409,#26410,#26411,#26412,#26413,#26414,#26415,#26416,#26417,#26418,#26419,
#26420,#26421,#26422,#26423,#26424,#26425,#26426,#26427,#26428,#26429,#26430,
#26431,#26432,#26433,#26434,#26435,#26436,#26437,#26438,#26439,#26440,#26441,
#26442,#26443,#26444,#26445,#26446,#26447,#26448,#26449,#26450,#26451,#26452,
#26453));
#28632=AXIS2_PLACEMENT_3D('',#69065,#34320,#34321);
#28633=AXIS2_PLACEMENT_3D('',#69066,#34322,#34323);
#28634=AXIS2_PLACEMENT_3D('',#69082,#34325,#34326);
#28635=AXIS2_PLACEMENT_3D('',#69093,#34327,#34328);
#28636=AXIS2_PLACEMENT_3D('',#69141,#34330,#34331);
#28637=AXIS2_PLACEMENT_3D('',#69189,#34333,#34334);
#28638=AXIS2_PLACEMENT_3D('',#69237,#34336,#34337);
#28639=AXIS2_PLACEMENT_3D('',#69291,#34339,#34340);
#28640=AXIS2_PLACEMENT_3D('',#69339,#34342,#34343);
#28641=AXIS2_PLACEMENT_3D('',#69387,#34345,#34346);
#28642=AXIS2_PLACEMENT_3D('',#69441,#34348,#34349);
#28643=AXIS2_PLACEMENT_3D('',#69489,#34351,#34352);
#28644=AXIS2_PLACEMENT_3D('',#69537,#34354,#34355);
#28645=AXIS2_PLACEMENT_3D('',#69588,#34357,#34358);
#28646=AXIS2_PLACEMENT_3D('',#69639,#34360,#34361);
#28647=AXIS2_PLACEMENT_3D('',#69687,#34363,#34364);
#28648=AXIS2_PLACEMENT_3D('',#69735,#34366,#34367);
#28649=AXIS2_PLACEMENT_3D('',#69789,#34369,#34370);
#28650=AXIS2_PLACEMENT_3D('',#69837,#34372,#34373);
#28651=AXIS2_PLACEMENT_3D('',#69885,#34375,#34376);
#28652=AXIS2_PLACEMENT_3D('',#69939,#34378,#34379);
#28653=AXIS2_PLACEMENT_3D('',#69987,#34381,#34382);
#28654=AXIS2_PLACEMENT_3D('',#70035,#34384,#34385);
#28655=AXIS2_PLACEMENT_3D('',#70083,#34387,#34388);
#28656=AXIS2_PLACEMENT_3D('',#70137,#34390,#34391);
#28657=AXIS2_PLACEMENT_3D('',#70185,#34393,#34394);
#28658=AXIS2_PLACEMENT_3D('',#70196,#34396,#34397);
#28659=AXIS2_PLACEMENT_3D('',#70201,#34398,#34399);
#28660=AXIS2_PLACEMENT_3D('',#70226,#34401,#34402);
#28661=AXIS2_PLACEMENT_3D('',#70251,#34404,#34405);
#28662=AXIS2_PLACEMENT_3D('',#70276,#34407,#34408);
#28663=AXIS2_PLACEMENT_3D('',#70300,#34410,#34411);
#28664=AXIS2_PLACEMENT_3D('',#70324,#34413,#34414);
#28665=AXIS2_PLACEMENT_3D('',#70349,#34416,#34417);
#28666=AXIS2_PLACEMENT_3D('',#70374,#34419,#34420);
#28667=AXIS2_PLACEMENT_3D('',#70398,#34422,#34423);
#28668=AXIS2_PLACEMENT_3D('',#70423,#34425,#34426);
#28669=AXIS2_PLACEMENT_3D('',#70448,#34428,#34429);
#28670=AXIS2_PLACEMENT_3D('',#70472,#34431,#34432);
#28671=AXIS2_PLACEMENT_3D('',#70497,#34434,#34435);
#28672=AXIS2_PLACEMENT_3D('',#70521,#34437,#34438);
#28673=AXIS2_PLACEMENT_3D('',#70546,#34440,#34441);
#28674=AXIS2_PLACEMENT_3D('',#70570,#34443,#34444);
#28675=AXIS2_PLACEMENT_3D('',#70595,#34446,#34447);
#28676=AXIS2_PLACEMENT_3D('',#70620,#34449,#34450);
#28677=AXIS2_PLACEMENT_3D('',#70644,#34452,#34453);
#28678=AXIS2_PLACEMENT_3D('',#70669,#34455,#34456);
#28679=AXIS2_PLACEMENT_3D('',#70694,#34458,#34459);
#28680=AXIS2_PLACEMENT_3D('',#70718,#34461,#34462);
#28681=AXIS2_PLACEMENT_3D('',#70742,#34464,#34465);
#28682=AXIS2_PLACEMENT_3D('',#70812,#34466,#34467);
#28683=AXIS2_PLACEMENT_3D('',#70814,#34468,#34469);
#28684=AXIS2_PLACEMENT_3D('',#71579,#34470,#34471);
#28685=AXIS2_PLACEMENT_3D('',#71581,#34472,#34473);
#28686=AXIS2_PLACEMENT_3D('',#71582,#34474,#34475);
#28687=AXIS2_PLACEMENT_3D('',#71651,#34476,#34477);
#28688=AXIS2_PLACEMENT_3D('',#71652,#34478,#34479);
#28689=AXIS2_PLACEMENT_3D('',#72282,#34480,#34481);
#28690=AXIS2_PLACEMENT_3D('',#72284,#34482,#34483);
#28691=AXIS2_PLACEMENT_3D('',#72285,#34484,#34485);
#28692=AXIS2_PLACEMENT_3D('',#72286,#34486,#34487);
#28693=AXIS2_PLACEMENT_3D('',#72287,#34488,#34489);
#28694=AXIS2_PLACEMENT_3D('',#72288,#34490,#34491);
#28695=AXIS2_PLACEMENT_3D('',#72290,#34492,#34493);
#28696=AXIS2_PLACEMENT_3D('',#72291,#34494,#34495);
#28697=AXIS2_PLACEMENT_3D('',#72295,#34497,#34498);
#28698=AXIS2_PLACEMENT_3D('',#72296,#34499,#34500);
#28699=AXIS2_PLACEMENT_3D('',#72299,#34502,#34503);
#28700=AXIS2_PLACEMENT_3D('',#72300,#34504,#34505);
#28701=AXIS2_PLACEMENT_3D('',#72303,#34507,#34508);
#28702=AXIS2_PLACEMENT_3D('',#72304,#34509,#34510);
#28703=AXIS2_PLACEMENT_3D('',#72307,#34512,#34513);
#28704=AXIS2_PLACEMENT_3D('',#72308,#34514,#34515);
#28705=AXIS2_PLACEMENT_3D('',#72311,#34517,#34518);
#28706=AXIS2_PLACEMENT_3D('',#72312,#34519,#34520);
#28707=AXIS2_PLACEMENT_3D('',#72314,#34522,#34523);
#28708=AXIS2_PLACEMENT_3D('',#72315,#34524,#34525);
#28709=AXIS2_PLACEMENT_3D('',#72318,#34527,#34528);
#28710=AXIS2_PLACEMENT_3D('',#72324,#34532,#34533);
#28711=AXIS2_PLACEMENT_3D('',#72328,#34536,#34537);
#28712=AXIS2_PLACEMENT_3D('',#72332,#34540,#34541);
#28713=AXIS2_PLACEMENT_3D('',#72336,#34544,#34545);
#28714=AXIS2_PLACEMENT_3D('',#72340,#34548,#34549);
#28715=AXIS2_PLACEMENT_3D('',#72342,#34551,#34552);
#28716=AXIS2_PLACEMENT_3D('',#72351,#34557,#34558);
#28717=AXIS2_PLACEMENT_3D('',#72353,#34559,#34560);
#28718=AXIS2_PLACEMENT_3D('',#72355,#34562,#34563);
#28719=AXIS2_PLACEMENT_3D('',#72359,#34566,#34567);
#28720=AXIS2_PLACEMENT_3D('',#72360,#34568,#34569);
#28721=AXIS2_PLACEMENT_3D('',#72361,#34570,#34571);
#28722=AXIS2_PLACEMENT_3D('',#72370,#34576,#34577);
#28723=AXIS2_PLACEMENT_3D('',#72372,#34578,#34579);
#28724=AXIS2_PLACEMENT_3D('',#72374,#34581,#34582);
#28725=AXIS2_PLACEMENT_3D('',#72378,#34585,#34586);
#28726=AXIS2_PLACEMENT_3D('',#72379,#34587,#34588);
#28727=AXIS2_PLACEMENT_3D('',#72380,#34589,#34590);
#28728=AXIS2_PLACEMENT_3D('',#72389,#34595,#34596);
#28729=AXIS2_PLACEMENT_3D('',#72391,#34597,#34598);
#28730=AXIS2_PLACEMENT_3D('',#72393,#34600,#34601);
#28731=AXIS2_PLACEMENT_3D('',#72397,#34604,#34605);
#28732=AXIS2_PLACEMENT_3D('',#72398,#34606,#34607);
#28733=AXIS2_PLACEMENT_3D('',#72399,#34608,#34609);
#28734=AXIS2_PLACEMENT_3D('',#72408,#34614,#34615);
#28735=AXIS2_PLACEMENT_3D('',#72410,#34616,#34617);
#28736=AXIS2_PLACEMENT_3D('',#72412,#34619,#34620);
#28737=AXIS2_PLACEMENT_3D('',#72416,#34623,#34624);
#28738=AXIS2_PLACEMENT_3D('',#72417,#34625,#34626);
#28739=AXIS2_PLACEMENT_3D('',#72418,#34627,#34628);
#28740=AXIS2_PLACEMENT_3D('',#72427,#34633,#34634);
#28741=AXIS2_PLACEMENT_3D('',#72429,#34635,#34636);
#28742=AXIS2_PLACEMENT_3D('',#72431,#34638,#34639);
#28743=AXIS2_PLACEMENT_3D('',#72435,#34642,#34643);
#28744=AXIS2_PLACEMENT_3D('',#72436,#34644,#34645);
#28745=AXIS2_PLACEMENT_3D('',#72437,#34646,#34647);
#28746=AXIS2_PLACEMENT_3D('',#72446,#34652,#34653);
#28747=AXIS2_PLACEMENT_3D('',#72448,#34654,#34655);
#28748=AXIS2_PLACEMENT_3D('',#72450,#34657,#34658);
#28749=AXIS2_PLACEMENT_3D('',#72454,#34661,#34662);
#28750=AXIS2_PLACEMENT_3D('',#72455,#34663,#34664);
#28751=AXIS2_PLACEMENT_3D('',#72456,#34665,#34666);
#28752=AXIS2_PLACEMENT_3D('',#72465,#34671,#34672);
#28753=AXIS2_PLACEMENT_3D('',#72467,#34673,#34674);
#28754=AXIS2_PLACEMENT_3D('',#72469,#34676,#34677);
#28755=AXIS2_PLACEMENT_3D('',#72473,#34680,#34681);
#28756=AXIS2_PLACEMENT_3D('',#72474,#34682,#34683);
#28757=AXIS2_PLACEMENT_3D('',#72475,#34684,#34685);
#28758=AXIS2_PLACEMENT_3D('',#72484,#34690,#34691);
#28759=AXIS2_PLACEMENT_3D('',#72486,#34692,#34693);
#28760=AXIS2_PLACEMENT_3D('',#72488,#34695,#34696);
#28761=AXIS2_PLACEMENT_3D('',#72492,#34699,#34700);
#28762=AXIS2_PLACEMENT_3D('',#72493,#34701,#34702);
#28763=AXIS2_PLACEMENT_3D('',#72494,#34703,#34704);
#28764=AXIS2_PLACEMENT_3D('',#72503,#34709,#34710);
#28765=AXIS2_PLACEMENT_3D('',#72505,#34711,#34712);
#28766=AXIS2_PLACEMENT_3D('',#72508,#34714,#34715);
#28767=AXIS2_PLACEMENT_3D('',#72509,#34716,#34717);
#28768=AXIS2_PLACEMENT_3D('',#72513,#34720,#34721);
#28769=AXIS2_PLACEMENT_3D('',#72515,#34722,#34723);
#28770=AXIS2_PLACEMENT_3D('',#72516,#34724,#34725);
#28771=AXIS2_PLACEMENT_3D('',#72517,#34726,#34727);
#28772=AXIS2_PLACEMENT_3D('',#72526,#34732,#34733);
#28773=AXIS2_PLACEMENT_3D('',#72528,#34734,#34735);
#28774=AXIS2_PLACEMENT_3D('',#72530,#34737,#34738);
#28775=AXIS2_PLACEMENT_3D('',#72534,#34741,#34742);
#28776=AXIS2_PLACEMENT_3D('',#72535,#34743,#34744);
#28777=AXIS2_PLACEMENT_3D('',#72536,#34745,#34746);
#28778=AXIS2_PLACEMENT_3D('',#72545,#34751,#34752);
#28779=AXIS2_PLACEMENT_3D('',#72547,#34753,#34754);
#28780=AXIS2_PLACEMENT_3D('',#72549,#34756,#34757);
#28781=AXIS2_PLACEMENT_3D('',#72553,#34760,#34761);
#28782=AXIS2_PLACEMENT_3D('',#72554,#34762,#34763);
#28783=AXIS2_PLACEMENT_3D('',#72555,#34764,#34765);
#28784=AXIS2_PLACEMENT_3D('',#72564,#34770,#34771);
#28785=AXIS2_PLACEMENT_3D('',#72566,#34772,#34773);
#28786=AXIS2_PLACEMENT_3D('',#72568,#34775,#34776);
#28787=AXIS2_PLACEMENT_3D('',#72572,#34779,#34780);
#28788=AXIS2_PLACEMENT_3D('',#72573,#34781,#34782);
#28789=AXIS2_PLACEMENT_3D('',#72574,#34783,#34784);
#28790=AXIS2_PLACEMENT_3D('',#72583,#34789,#34790);
#28791=AXIS2_PLACEMENT_3D('',#72585,#34791,#34792);
#28792=AXIS2_PLACEMENT_3D('',#72587,#34794,#34795);
#28793=AXIS2_PLACEMENT_3D('',#72591,#34798,#34799);
#28794=AXIS2_PLACEMENT_3D('',#72592,#34800,#34801);
#28795=AXIS2_PLACEMENT_3D('',#72593,#34802,#34803);
#28796=AXIS2_PLACEMENT_3D('',#72602,#34808,#34809);
#28797=AXIS2_PLACEMENT_3D('',#72604,#34810,#34811);
#28798=AXIS2_PLACEMENT_3D('',#72606,#34813,#34814);
#28799=AXIS2_PLACEMENT_3D('',#72610,#34817,#34818);
#28800=AXIS2_PLACEMENT_3D('',#72611,#34819,#34820);
#28801=AXIS2_PLACEMENT_3D('',#72612,#34821,#34822);
#28802=AXIS2_PLACEMENT_3D('',#72621,#34827,#34828);
#28803=AXIS2_PLACEMENT_3D('',#72623,#34829,#34830);
#28804=AXIS2_PLACEMENT_3D('',#72625,#34832,#34833);
#28805=AXIS2_PLACEMENT_3D('',#72629,#34836,#34837);
#28806=AXIS2_PLACEMENT_3D('',#72630,#34838,#34839);
#28807=AXIS2_PLACEMENT_3D('',#72631,#34840,#34841);
#28808=AXIS2_PLACEMENT_3D('',#72640,#34846,#34847);
#28809=AXIS2_PLACEMENT_3D('',#72642,#34848,#34849);
#28810=AXIS2_PLACEMENT_3D('',#72644,#34851,#34852);
#28811=AXIS2_PLACEMENT_3D('',#72648,#34855,#34856);
#28812=AXIS2_PLACEMENT_3D('',#72649,#34857,#34858);
#28813=AXIS2_PLACEMENT_3D('',#72650,#34859,#34860);
#28814=AXIS2_PLACEMENT_3D('',#72659,#34865,#34866);
#28815=AXIS2_PLACEMENT_3D('',#72661,#34867,#34868);
#28816=AXIS2_PLACEMENT_3D('',#72663,#34870,#34871);
#28817=AXIS2_PLACEMENT_3D('',#72667,#34874,#34875);
#28818=AXIS2_PLACEMENT_3D('',#72668,#34876,#34877);
#28819=AXIS2_PLACEMENT_3D('',#72669,#34878,#34879);
#28820=AXIS2_PLACEMENT_3D('',#72678,#34884,#34885);
#28821=AXIS2_PLACEMENT_3D('',#72680,#34886,#34887);
#28822=AXIS2_PLACEMENT_3D('',#72682,#34889,#34890);
#28823=AXIS2_PLACEMENT_3D('',#72686,#34893,#34894);
#28824=AXIS2_PLACEMENT_3D('',#72687,#34895,#34896);
#28825=AXIS2_PLACEMENT_3D('',#72688,#34897,#34898);
#28826=AXIS2_PLACEMENT_3D('',#72697,#34903,#34904);
#28827=AXIS2_PLACEMENT_3D('',#72699,#34905,#34906);
#28828=AXIS2_PLACEMENT_3D('',#72701,#34908,#34909);
#28829=AXIS2_PLACEMENT_3D('',#72705,#34912,#34913);
#28830=AXIS2_PLACEMENT_3D('',#72706,#34914,#34915);
#28831=AXIS2_PLACEMENT_3D('',#72707,#34916,#34917);
#28832=AXIS2_PLACEMENT_3D('',#72716,#34922,#34923);
#28833=AXIS2_PLACEMENT_3D('',#72718,#34924,#34925);
#28834=AXIS2_PLACEMENT_3D('',#72720,#34927,#34928);
#28835=AXIS2_PLACEMENT_3D('',#72724,#34931,#34932);
#28836=AXIS2_PLACEMENT_3D('',#72725,#34933,#34934);
#28837=AXIS2_PLACEMENT_3D('',#72726,#34935,#34936);
#28838=AXIS2_PLACEMENT_3D('',#72735,#34941,#34942);
#28839=AXIS2_PLACEMENT_3D('',#72737,#34943,#34944);
#28840=AXIS2_PLACEMENT_3D('',#72739,#34946,#34947);
#28841=AXIS2_PLACEMENT_3D('',#72743,#34950,#34951);
#28842=AXIS2_PLACEMENT_3D('',#72744,#34952,#34953);
#28843=AXIS2_PLACEMENT_3D('',#72745,#34954,#34955);
#28844=AXIS2_PLACEMENT_3D('',#72754,#34960,#34961);
#28845=AXIS2_PLACEMENT_3D('',#72756,#34962,#34963);
#28846=AXIS2_PLACEMENT_3D('',#72758,#34965,#34966);
#28847=AXIS2_PLACEMENT_3D('',#72762,#34969,#34970);
#28848=AXIS2_PLACEMENT_3D('',#72763,#34971,#34972);
#28849=AXIS2_PLACEMENT_3D('',#72764,#34973,#34974);
#28850=AXIS2_PLACEMENT_3D('',#72773,#34979,#34980);
#28851=AXIS2_PLACEMENT_3D('',#72775,#34981,#34982);
#28852=AXIS2_PLACEMENT_3D('',#72777,#34984,#34985);
#28853=AXIS2_PLACEMENT_3D('',#72781,#34988,#34989);
#28854=AXIS2_PLACEMENT_3D('',#72782,#34990,#34991);
#28855=AXIS2_PLACEMENT_3D('',#72783,#34992,#34993);
#28856=AXIS2_PLACEMENT_3D('',#72792,#34998,#34999);
#28857=AXIS2_PLACEMENT_3D('',#72794,#35000,#35001);
#28858=AXIS2_PLACEMENT_3D('',#72796,#35003,#35004);
#28859=AXIS2_PLACEMENT_3D('',#72800,#35007,#35008);
#28860=AXIS2_PLACEMENT_3D('',#72801,#35009,#35010);
#28861=AXIS2_PLACEMENT_3D('',#72802,#35011,#35012);
#28862=AXIS2_PLACEMENT_3D('',#72811,#35017,#35018);
#28863=AXIS2_PLACEMENT_3D('',#72813,#35019,#35020);
#28864=AXIS2_PLACEMENT_3D('',#72815,#35022,#35023);
#28865=AXIS2_PLACEMENT_3D('',#72819,#35026,#35027);
#28866=AXIS2_PLACEMENT_3D('',#72820,#35028,#35029);
#28867=AXIS2_PLACEMENT_3D('',#72821,#35030,#35031);
#28868=AXIS2_PLACEMENT_3D('',#72830,#35036,#35037);
#28869=AXIS2_PLACEMENT_3D('',#72832,#35038,#35039);
#28870=AXIS2_PLACEMENT_3D('',#72834,#35041,#35042);
#28871=AXIS2_PLACEMENT_3D('',#72838,#35045,#35046);
#28872=AXIS2_PLACEMENT_3D('',#72839,#35047,#35048);
#28873=AXIS2_PLACEMENT_3D('',#72840,#35049,#35050);
#28874=AXIS2_PLACEMENT_3D('',#72843,#35051,#35052);
#28875=AXIS2_PLACEMENT_3D('',#72847,#35055,#35056);
#28876=AXIS2_PLACEMENT_3D('',#72853,#35060,#35061);
#28877=AXIS2_PLACEMENT_3D('',#72857,#35064,#35065);
#28878=AXIS2_PLACEMENT_3D('',#72858,#35066,#35067);
#28879=AXIS2_PLACEMENT_3D('',#72859,#35068,#35069);
#28880=AXIS2_PLACEMENT_3D('',#72868,#35074,#35075);
#28881=AXIS2_PLACEMENT_3D('',#72870,#35076,#35077);
#28882=AXIS2_PLACEMENT_3D('',#72872,#35079,#35080);
#28883=AXIS2_PLACEMENT_3D('',#72876,#35083,#35084);
#28884=AXIS2_PLACEMENT_3D('',#72877,#35085,#35086);
#28885=AXIS2_PLACEMENT_3D('',#72878,#35087,#35088);
#28886=AXIS2_PLACEMENT_3D('',#72887,#35093,#35094);
#28887=AXIS2_PLACEMENT_3D('',#72889,#35095,#35096);
#28888=AXIS2_PLACEMENT_3D('',#72891,#35098,#35099);
#28889=AXIS2_PLACEMENT_3D('',#72895,#35102,#35103);
#28890=AXIS2_PLACEMENT_3D('',#72896,#35104,#35105);
#28891=AXIS2_PLACEMENT_3D('',#72897,#35106,#35107);
#28892=AXIS2_PLACEMENT_3D('',#72906,#35112,#35113);
#28893=AXIS2_PLACEMENT_3D('',#72908,#35114,#35115);
#28894=AXIS2_PLACEMENT_3D('',#72910,#35117,#35118);
#28895=AXIS2_PLACEMENT_3D('',#72914,#35121,#35122);
#28896=AXIS2_PLACEMENT_3D('',#72915,#35123,#35124);
#28897=AXIS2_PLACEMENT_3D('',#72916,#35125,#35126);
#28898=AXIS2_PLACEMENT_3D('',#72925,#35131,#35132);
#28899=AXIS2_PLACEMENT_3D('',#72927,#35133,#35134);
#28900=AXIS2_PLACEMENT_3D('',#72929,#35136,#35137);
#28901=AXIS2_PLACEMENT_3D('',#72933,#35140,#35141);
#28902=AXIS2_PLACEMENT_3D('',#72934,#35142,#35143);
#28903=AXIS2_PLACEMENT_3D('',#72935,#35144,#35145);
#28904=AXIS2_PLACEMENT_3D('',#72944,#35150,#35151);
#28905=AXIS2_PLACEMENT_3D('',#72946,#35152,#35153);
#28906=AXIS2_PLACEMENT_3D('',#72948,#35155,#35156);
#28907=AXIS2_PLACEMENT_3D('',#72952,#35159,#35160);
#28908=AXIS2_PLACEMENT_3D('',#72953,#35161,#35162);
#28909=AXIS2_PLACEMENT_3D('',#72954,#35163,#35164);
#28910=AXIS2_PLACEMENT_3D('',#72963,#35169,#35170);
#28911=AXIS2_PLACEMENT_3D('',#72965,#35171,#35172);
#28912=AXIS2_PLACEMENT_3D('',#72967,#35174,#35175);
#28913=AXIS2_PLACEMENT_3D('',#72971,#35178,#35179);
#28914=AXIS2_PLACEMENT_3D('',#72972,#35180,#35181);
#28915=AXIS2_PLACEMENT_3D('',#72973,#35182,#35183);
#28916=AXIS2_PLACEMENT_3D('',#72982,#35188,#35189);
#28917=AXIS2_PLACEMENT_3D('',#72984,#35190,#35191);
#28918=AXIS2_PLACEMENT_3D('',#72986,#35193,#35194);
#28919=AXIS2_PLACEMENT_3D('',#72990,#35197,#35198);
#28920=AXIS2_PLACEMENT_3D('',#72991,#35199,#35200);
#28921=AXIS2_PLACEMENT_3D('',#72992,#35201,#35202);
#28922=AXIS2_PLACEMENT_3D('',#73001,#35207,#35208);
#28923=AXIS2_PLACEMENT_3D('',#73003,#35209,#35210);
#28924=AXIS2_PLACEMENT_3D('',#73005,#35212,#35213);
#28925=AXIS2_PLACEMENT_3D('',#73009,#35216,#35217);
#28926=AXIS2_PLACEMENT_3D('',#73010,#35218,#35219);
#28927=AXIS2_PLACEMENT_3D('',#73011,#35220,#35221);
#28928=AXIS2_PLACEMENT_3D('',#73020,#35226,#35227);
#28929=AXIS2_PLACEMENT_3D('',#73022,#35228,#35229);
#28930=AXIS2_PLACEMENT_3D('',#73024,#35231,#35232);
#28931=AXIS2_PLACEMENT_3D('',#73028,#35235,#35236);
#28932=AXIS2_PLACEMENT_3D('',#73029,#35237,#35238);
#28933=AXIS2_PLACEMENT_3D('',#73030,#35239,#35240);
#28934=AXIS2_PLACEMENT_3D('',#73032,#35241,#35242);
#28935=AXIS2_PLACEMENT_3D('',#73033,#35243,#35244);
#28936=AXIS2_PLACEMENT_3D('',#73035,#35246,#35247);
#28937=AXIS2_PLACEMENT_3D('',#73037,#35248,#35249);
#28938=AXIS2_PLACEMENT_3D('',#73039,#35251,#35252);
#28939=AXIS2_PLACEMENT_3D('',#73040,#35253,#35254);
#28940=AXIS2_PLACEMENT_3D('',#73041,#35255,#35256);
#28941=AXIS2_PLACEMENT_3D('',#73042,#35257,#35258);
#28942=AXIS2_PLACEMENT_3D('',#73043,#35259,#35260);
#28943=AXIS2_PLACEMENT_3D('',#73044,#35261,#35262);
#28944=AXIS2_PLACEMENT_3D('',#73045,#35263,#35264);
#28945=AXIS2_PLACEMENT_3D('',#73046,#35265,#35266);
#28946=AXIS2_PLACEMENT_3D('',#73047,#35267,#35268);
#28947=AXIS2_PLACEMENT_3D('',#73048,#35269,#35270);
#28948=AXIS2_PLACEMENT_3D('',#73049,#35271,#35272);
#28949=AXIS2_PLACEMENT_3D('',#73050,#35273,#35274);
#28950=AXIS2_PLACEMENT_3D('',#73051,#35275,#35276);
#28951=AXIS2_PLACEMENT_3D('',#73052,#35277,#35278);
#28952=AXIS2_PLACEMENT_3D('',#73053,#35279,#35280);
#28953=AXIS2_PLACEMENT_3D('',#73054,#35281,#35282);
#28954=AXIS2_PLACEMENT_3D('',#73055,#35283,#35284);
#28955=AXIS2_PLACEMENT_3D('',#73057,#35286,#35287);
#28956=AXIS2_PLACEMENT_3D('',#73058,#35288,#35289);
#28957=AXIS2_PLACEMENT_3D('',#73059,#35290,#35291);
#28958=AXIS2_PLACEMENT_3D('',#73060,#35292,#35293);
#28959=AXIS2_PLACEMENT_3D('',#73061,#35294,#35295);
#28960=AXIS2_PLACEMENT_3D('',#73062,#35296,#35297);
#28961=AXIS2_PLACEMENT_3D('',#73063,#35298,#35299);
#28962=AXIS2_PLACEMENT_3D('',#73064,#35300,#35301);
#28963=AXIS2_PLACEMENT_3D('',#73065,#35302,#35303);
#28964=AXIS2_PLACEMENT_3D('',#73066,#35304,#35305);
#28965=AXIS2_PLACEMENT_3D('',#73067,#35306,#35307);
#28966=AXIS2_PLACEMENT_3D('',#73068,#35308,#35309);
#28967=AXIS2_PLACEMENT_3D('',#73069,#35310,#35311);
#28968=AXIS2_PLACEMENT_3D('',#73070,#35312,#35313);
#28969=AXIS2_PLACEMENT_3D('',#73071,#35314,#35315);
#28970=AXIS2_PLACEMENT_3D('',#73072,#35316,#35317);
#28971=AXIS2_PLACEMENT_3D('',#73073,#35318,#35319);
#28972=AXIS2_PLACEMENT_3D('',#73074,#35320,#35321);
#28973=AXIS2_PLACEMENT_3D('',#73075,#35322,#35323);
#28974=AXIS2_PLACEMENT_3D('',#73076,#35324,#35325);
#28975=AXIS2_PLACEMENT_3D('',#73077,#35326,#35327);
#28976=AXIS2_PLACEMENT_3D('',#73079,#35328,#35329);
#28977=AXIS2_PLACEMENT_3D('',#73081,#35331,#35332);
#34320=DIRECTION('axis',(0.,0.,1.));
#34321=DIRECTION('refdir',(1.,0.,0.));
#34322=DIRECTION('center_axis',(0.,0.,1.));
#34323=DIRECTION('ref_axis',(1.,0.,0.));
#34324=DIRECTION('',(0.,0.,-1.));
#34325=DIRECTION('center_axis',(0.,0.,1.));
#34326=DIRECTION('ref_axis',(1.,0.,0.));
#34327=DIRECTION('center_axis',(0.,0.,1.));
#34328=DIRECTION('ref_axis',(1.,0.,0.));
#34329=DIRECTION('',(0.,0.,-1.));
#34330=DIRECTION('center_axis',(0.,0.,1.));
#34331=DIRECTION('ref_axis',(1.,0.,0.));
#34332=DIRECTION('',(0.,0.,-1.));
#34333=DIRECTION('center_axis',(0.,0.,1.));
#34334=DIRECTION('ref_axis',(1.,0.,0.));
#34335=DIRECTION('',(0.,0.,-1.));
#34336=DIRECTION('center_axis',(0.,0.,1.));
#34337=DIRECTION('ref_axis',(1.,0.,0.));
#34338=DIRECTION('',(0.,0.,-1.));
#34339=DIRECTION('center_axis',(0.,0.,1.));
#34340=DIRECTION('ref_axis',(1.,0.,0.));
#34341=DIRECTION('',(0.,0.,-1.));
#34342=DIRECTION('center_axis',(0.,0.,1.));
#34343=DIRECTION('ref_axis',(1.,0.,0.));
#34344=DIRECTION('',(0.,0.,-1.));
#34345=DIRECTION('center_axis',(0.,0.,1.));
#34346=DIRECTION('ref_axis',(1.,0.,0.));
#34347=DIRECTION('',(0.,0.,-1.));
#34348=DIRECTION('center_axis',(0.,0.,1.));
#34349=DIRECTION('ref_axis',(1.,0.,0.));
#34350=DIRECTION('',(0.,0.,-1.));
#34351=DIRECTION('center_axis',(0.,0.,1.));
#34352=DIRECTION('ref_axis',(1.,0.,0.));
#34353=DIRECTION('',(0.,0.,-1.));
#34354=DIRECTION('center_axis',(0.,0.,1.));
#34355=DIRECTION('ref_axis',(1.,0.,0.));
#34356=DIRECTION('',(0.,0.,-1.));
#34357=DIRECTION('center_axis',(0.,0.,1.));
#34358=DIRECTION('ref_axis',(1.,0.,0.));
#34359=DIRECTION('',(0.,0.,-1.));
#34360=DIRECTION('center_axis',(0.,0.,1.));
#34361=DIRECTION('ref_axis',(1.,0.,0.));
#34362=DIRECTION('',(0.,0.,-1.));
#34363=DIRECTION('center_axis',(0.,0.,1.));
#34364=DIRECTION('ref_axis',(1.,0.,0.));
#34365=DIRECTION('',(0.,0.,-1.));
#34366=DIRECTION('center_axis',(0.,0.,1.));
#34367=DIRECTION('ref_axis',(1.,0.,0.));
#34368=DIRECTION('',(0.,0.,-1.));
#34369=DIRECTION('center_axis',(0.,0.,1.));
#34370=DIRECTION('ref_axis',(1.,0.,0.));
#34371=DIRECTION('',(0.,0.,-1.));
#34372=DIRECTION('center_axis',(0.,0.,1.));
#34373=DIRECTION('ref_axis',(1.,0.,0.));
#34374=DIRECTION('',(0.,0.,-1.));
#34375=DIRECTION('center_axis',(0.,0.,1.));
#34376=DIRECTION('ref_axis',(1.,0.,0.));
#34377=DIRECTION('',(0.,0.,-1.));
#34378=DIRECTION('center_axis',(0.,0.,1.));
#34379=DIRECTION('ref_axis',(1.,0.,0.));
#34380=DIRECTION('',(0.,0.,-1.));
#34381=DIRECTION('center_axis',(0.,0.,1.));
#34382=DIRECTION('ref_axis',(1.,0.,0.));
#34383=DIRECTION('',(0.,0.,-1.));
#34384=DIRECTION('center_axis',(0.,0.,1.));
#34385=DIRECTION('ref_axis',(1.,0.,0.));
#34386=DIRECTION('',(0.,0.,-1.));
#34387=DIRECTION('center_axis',(0.,0.,1.));
#34388=DIRECTION('ref_axis',(1.,0.,0.));
#34389=DIRECTION('',(0.,0.,-1.));
#34390=DIRECTION('center_axis',(0.,0.,1.));
#34391=DIRECTION('ref_axis',(1.,0.,0.));
#34392=DIRECTION('',(0.,0.,-1.));
#34393=DIRECTION('center_axis',(0.,0.,1.));
#34394=DIRECTION('ref_axis',(-0.745989836172204,-0.665957329209438,0.));
#34395=DIRECTION('',(0.,0.,1.));
#34396=DIRECTION('center_axis',(0.,0.,1.));
#34397=DIRECTION('ref_axis',(1.,2.60874502654993E-14,0.));
#34398=DIRECTION('center_axis',(0.,0.,1.));
#34399=DIRECTION('ref_axis',(1.,2.60874502654993E-14,0.));
#34400=DIRECTION('',(0.,0.,1.));
#34401=DIRECTION('center_axis',(0.,0.,1.));
#34402=DIRECTION('ref_axis',(1.,2.60874502654993E-14,0.));
#34403=DIRECTION('',(0.,0.,1.));
#34404=DIRECTION('center_axis',(0.,0.,1.));
#34405=DIRECTION('ref_axis',(1.,2.60874502654993E-14,0.));
#34406=DIRECTION('',(0.,0.,1.));
#34407=DIRECTION('center_axis',(0.,0.,1.));
#34408=DIRECTION('ref_axis',(1.,2.60874502654993E-14,0.));
#34409=DIRECTION('',(0.,0.,1.));
#34410=DIRECTION('center_axis',(0.,0.,1.));
#34411=DIRECTION('ref_axis',(1.,2.60874502654993E-14,0.));
#34412=DIRECTION('',(0.,0.,1.));
#34413=DIRECTION('center_axis',(0.,0.,1.));
#34414=DIRECTION('ref_axis',(1.,2.60874502654993E-14,0.));
#34415=DIRECTION('',(0.,0.,1.));
#34416=DIRECTION('center_axis',(0.,0.,1.));
#34417=DIRECTION('ref_axis',(1.,2.60874502654993E-14,0.));
#34418=DIRECTION('',(0.,0.,1.));
#34419=DIRECTION('center_axis',(0.,0.,1.));
#34420=DIRECTION('ref_axis',(1.,2.60874502654993E-14,0.));
#34421=DIRECTION('',(0.,0.,1.));
#34422=DIRECTION('center_axis',(0.,0.,1.));
#34423=DIRECTION('ref_axis',(1.,2.60874502654993E-14,0.));
#34424=DIRECTION('',(0.,0.,1.));
#34425=DIRECTION('center_axis',(0.,0.,1.));
#34426=DIRECTION('ref_axis',(1.,2.60874502654993E-14,0.));
#34427=DIRECTION('',(0.,0.,1.));
#34428=DIRECTION('center_axis',(0.,0.,1.));
#34429=DIRECTION('ref_axis',(1.,2.60874502654993E-14,0.));
#34430=DIRECTION('',(0.,0.,1.));
#34431=DIRECTION('center_axis',(0.,0.,1.));
#34432=DIRECTION('ref_axis',(1.,2.60874502654993E-14,0.));
#34433=DIRECTION('',(0.,0.,1.));
#34434=DIRECTION('center_axis',(0.,0.,1.));
#34435=DIRECTION('ref_axis',(1.,2.60874502654993E-14,0.));
#34436=DIRECTION('',(0.,0.,1.));
#34437=DIRECTION('center_axis',(0.,0.,1.));
#34438=DIRECTION('ref_axis',(1.,2.60874502654993E-14,0.));
#34439=DIRECTION('',(0.,0.,1.));
#34440=DIRECTION('center_axis',(0.,0.,1.));
#34441=DIRECTION('ref_axis',(1.,2.60874502654993E-14,0.));
#34442=DIRECTION('',(0.,0.,1.));
#34443=DIRECTION('center_axis',(0.,0.,1.));
#34444=DIRECTION('ref_axis',(1.,2.60874502654993E-14,0.));
#34445=DIRECTION('',(0.,0.,1.));
#34446=DIRECTION('center_axis',(0.,0.,1.));
#34447=DIRECTION('ref_axis',(1.,2.60874502654993E-14,0.));
#34448=DIRECTION('',(0.,0.,1.));
#34449=DIRECTION('center_axis',(0.,0.,1.));
#34450=DIRECTION('ref_axis',(1.,2.60874502654993E-14,0.));
#34451=DIRECTION('',(0.,0.,1.));
#34452=DIRECTION('center_axis',(0.,0.,1.));
#34453=DIRECTION('ref_axis',(1.,2.60874502654993E-14,0.));
#34454=DIRECTION('',(0.,0.,1.));
#34455=DIRECTION('center_axis',(0.,0.,1.));
#34456=DIRECTION('ref_axis',(1.,2.60874502654993E-14,0.));
#34457=DIRECTION('',(0.,0.,1.));
#34458=DIRECTION('center_axis',(0.,0.,1.));
#34459=DIRECTION('ref_axis',(1.,2.60874502654993E-14,0.));
#34460=DIRECTION('',(0.,0.,1.));
#34461=DIRECTION('center_axis',(0.,0.,1.));
#34462=DIRECTION('ref_axis',(1.,2.60874502654993E-14,0.));
#34463=DIRECTION('',(0.,0.,1.));
#34464=DIRECTION('center_axis',(0.,0.,1.));
#34465=DIRECTION('ref_axis',(1.,0.,0.));
#34466=DIRECTION('center_axis',(0.,0.,1.));
#34467=DIRECTION('ref_axis',(1.,0.,0.));
#34468=DIRECTION('center_axis',(0.,0.,1.));
#34469=DIRECTION('ref_axis',(1.,0.,0.));
#34470=DIRECTION('center_axis',(0.,0.,1.));
#34471=DIRECTION('ref_axis',(1.,0.,0.));
#34472=DIRECTION('center_axis',(0.,0.,1.));
#34473=DIRECTION('ref_axis',(1.,0.,0.));
#34474=DIRECTION('center_axis',(0.,0.,1.));
#34475=DIRECTION('ref_axis',(1.,0.,0.));
#34476=DIRECTION('center_axis',(0.,0.,-1.));
#34477=DIRECTION('ref_axis',(1.,2.60874502654993E-14,0.));
#34478=DIRECTION('center_axis',(0.,0.,1.));
#34479=DIRECTION('ref_axis',(1.,2.60874502654993E-14,0.));
#34480=DIRECTION('center_axis',(0.,0.,1.));
#34481=DIRECTION('ref_axis',(1.,0.,0.));
#34482=DIRECTION('center_axis',(1.22464679914735E-16,-1.,0.));
#34483=DIRECTION('ref_axis',(-1.,-1.22464679914735E-16,0.));
#34484=DIRECTION('center_axis',(0.,0.,-1.));
#34485=DIRECTION('ref_axis',(1.,0.,0.));
#34486=DIRECTION('center_axis',(0.,0.,1.));
#34487=DIRECTION('ref_axis',(1.,0.,0.));
#34488=DIRECTION('center_axis',(0.,0.,1.));
#34489=DIRECTION('ref_axis',(0.602919366379948,-0.797802129380463,0.));
#34490=DIRECTION('center_axis',(0.,0.,-1.));
#34491=DIRECTION('ref_axis',(-1.,0.,0.));
#34492=DIRECTION('center_axis',(0.,0.,1.));
#34493=DIRECTION('ref_axis',(1.,0.,0.));
#34494=DIRECTION('center_axis',(0.,0.,1.));
#34495=DIRECTION('ref_axis',(1.,0.,0.));
#34496=DIRECTION('',(0.5,-0.866025403784439,0.));
#34497=DIRECTION('center_axis',(0.,0.,1.));
#34498=DIRECTION('ref_axis',(1.,0.,0.));
#34499=DIRECTION('center_axis',(0.,0.,1.));
#34500=DIRECTION('ref_axis',(1.,0.,0.));
#34501=DIRECTION('',(-0.5,-0.866025403784439,0.));
#34502=DIRECTION('center_axis',(0.,0.,1.));
#34503=DIRECTION('ref_axis',(1.,0.,0.));
#34504=DIRECTION('center_axis',(0.,0.,1.));
#34505=DIRECTION('ref_axis',(1.,0.,0.));
#34506=DIRECTION('',(-1.,2.40370335797945E-16,0.));
#34507=DIRECTION('center_axis',(0.,0.,1.));
#34508=DIRECTION('ref_axis',(1.,0.,0.));
#34509=DIRECTION('center_axis',(0.,0.,1.));
#34510=DIRECTION('ref_axis',(1.,0.,0.));
#34511=DIRECTION('',(-0.5,0.866025403784439,0.));
#34512=DIRECTION('center_axis',(0.,0.,1.));
#34513=DIRECTION('ref_axis',(1.,0.,0.));
#34514=DIRECTION('center_axis',(0.,0.,1.));
#34515=DIRECTION('ref_axis',(1.,0.,0.));
#34516=DIRECTION('',(0.5,0.866025403784439,0.));
#34517=DIRECTION('center_axis',(0.,0.,1.));
#34518=DIRECTION('ref_axis',(1.,0.,0.));
#34519=DIRECTION('center_axis',(0.,0.,1.));
#34520=DIRECTION('ref_axis',(1.,0.,0.));
#34521=DIRECTION('',(1.,-1.20185167898973E-16,0.));
#34522=DIRECTION('center_axis',(0.,0.,1.));
#34523=DIRECTION('ref_axis',(1.,0.,0.));
#34524=DIRECTION('center_axis',(0.,0.,1.));
#34525=DIRECTION('ref_axis',(1.,0.,0.));
#34526=DIRECTION('',(-0.857492925712544,-1.05012596676537E-16,0.514495755427527));
#34527=DIRECTION('center_axis',(0.866025403784439,0.5,0.));
#34528=DIRECTION('ref_axis',(0.5,-0.866025403784439,0.));
#34529=DIRECTION('',(0.5,-0.866025403784439,0.));
#34530=DIRECTION('',(0.,0.,-1.));
#34531=DIRECTION('',(0.,0.,-1.));
#34532=DIRECTION('center_axis',(1.20185167898973E-16,1.,0.));
#34533=DIRECTION('ref_axis',(1.,-1.20185167898973E-16,0.));
#34534=DIRECTION('',(1.,-1.20185167898973E-16,0.));
#34535=DIRECTION('',(0.,0.,-1.));
#34536=DIRECTION('center_axis',(-0.866025403784439,0.5,0.));
#34537=DIRECTION('ref_axis',(0.5,0.866025403784439,0.));
#34538=DIRECTION('',(0.5,0.866025403784439,0.));
#34539=DIRECTION('',(0.,0.,-1.));
#34540=DIRECTION('center_axis',(-0.866025403784439,-0.5,0.));
#34541=DIRECTION('ref_axis',(-0.5,0.866025403784439,0.));
#34542=DIRECTION('',(-0.5,0.866025403784439,0.));
#34543=DIRECTION('',(0.,0.,-1.));
#34544=DIRECTION('center_axis',(-2.40370335797945E-16,-1.,0.));
#34545=DIRECTION('ref_axis',(-1.,2.40370335797945E-16,0.));
#34546=DIRECTION('',(-1.,2.40370335797945E-16,0.));
#34547=DIRECTION('',(0.,0.,-1.));
#34548=DIRECTION('center_axis',(0.866025403784439,-0.5,0.));
#34549=DIRECTION('ref_axis',(-0.5,-0.866025403784439,0.));
#34550=DIRECTION('',(-0.5,-0.866025403784439,0.));
#34551=DIRECTION('center_axis',(-0.836392077301054,-0.548131638411821,0.));
#34552=DIRECTION('ref_axis',(-0.548131638411821,0.836392077301054,0.));
#34553=DIRECTION('',(0.,0.,1.));
#34554=DIRECTION('',(-0.548131638411821,0.836392077301054,0.));
#34555=DIRECTION('',(0.,0.,-1.));
#34556=DIRECTION('',(-0.548131638411821,0.836392077301054,0.));
#34557=DIRECTION('center_axis',(0.,0.,1.));
#34558=DIRECTION('ref_axis',(1.,0.,0.));
#34559=DIRECTION('center_axis',(0.,0.,1.));
#34560=DIRECTION('ref_axis',(1.,0.,0.));
#34561=DIRECTION('',(0.957515659832182,0.288381277436904,0.));
#34562=DIRECTION('center_axis',(-0.288381277436904,0.957515659832182,0.));
#34563=DIRECTION('ref_axis',(0.957515659832182,0.288381277436904,0.));
#34564=DIRECTION('',(0.,0.,-1.));
#34565=DIRECTION('',(0.957515659832182,0.288381277436904,0.));
#34566=DIRECTION('center_axis',(0.,0.,-1.));
#34567=DIRECTION('ref_axis',(-1.,0.,0.));
#34568=DIRECTION('center_axis',(0.,0.,-1.));
#34569=DIRECTION('ref_axis',(1.,0.,0.));
#34570=DIRECTION('center_axis',(-0.973423524654541,-0.229012317679924,0.));
#34571=DIRECTION('ref_axis',(-0.229012317679924,0.973423524654541,0.));
#34572=DIRECTION('',(0.,0.,1.));
#34573=DIRECTION('',(-0.229012317679924,0.973423524654541,0.));
#34574=DIRECTION('',(0.,0.,-1.));
#34575=DIRECTION('',(-0.229012317679924,0.973423524654541,0.));
#34576=DIRECTION('center_axis',(0.,0.,1.));
#34577=DIRECTION('ref_axis',(1.,0.,0.));
#34578=DIRECTION('center_axis',(0.,0.,1.));
#34579=DIRECTION('ref_axis',(1.,0.,0.));
#34580=DIRECTION('',(0.998402605672661,-0.0564998848320951,0.));
#34581=DIRECTION('center_axis',(0.0564998848320951,0.998402605672661,0.));
#34582=DIRECTION('ref_axis',(0.998402605672661,-0.0564998848320951,0.));
#34583=DIRECTION('',(0.,0.,-1.));
#34584=DIRECTION('',(0.998402605672661,-0.0564998848320951,0.));
#34585=DIRECTION('center_axis',(0.,0.,-1.));
#34586=DIRECTION('ref_axis',(-1.,0.,0.));
#34587=DIRECTION('center_axis',(0.,0.,-1.));
#34588=DIRECTION('ref_axis',(1.,0.,0.));
#34589=DIRECTION('center_axis',(-0.993045728733512,0.117729268426028,0.));
#34590=DIRECTION('ref_axis',(0.117729268426028,0.993045728733512,0.));
#34591=DIRECTION('',(0.,0.,1.));
#34592=DIRECTION('',(0.117729268426028,0.993045728733512,0.));
#34593=DIRECTION('',(0.,0.,-1.));
#34594=DIRECTION('',(0.117729268426028,0.993045728733512,0.));
#34595=DIRECTION('center_axis',(0.,0.,1.));
#34596=DIRECTION('ref_axis',(1.,0.,0.));
#34597=DIRECTION('center_axis',(0.,0.,1.));
#34598=DIRECTION('ref_axis',(1.,0.,0.));
#34599=DIRECTION('',(0.918867462415862,-0.394566327140867,0.));
#34600=DIRECTION('center_axis',(0.394566327140867,0.918867462415862,0.));
#34601=DIRECTION('ref_axis',(0.918867462415862,-0.394566327140867,0.));
#34602=DIRECTION('',(0.,0.,-1.));
#34603=DIRECTION('',(0.918867462415862,-0.394566327140867,0.));
#34604=DIRECTION('center_axis',(0.,0.,-1.));
#34605=DIRECTION('ref_axis',(-1.,0.,0.));
#34606=DIRECTION('center_axis',(0.,0.,-1.));
#34607=DIRECTION('ref_axis',(1.,0.,0.));
#34608=DIRECTION('center_axis',(-0.892891962133153,0.450270967260834,0.));
#34609=DIRECTION('ref_axis',(0.450270967260834,0.892891962133153,0.));
#34610=DIRECTION('',(0.,0.,1.));
#34611=DIRECTION('',(0.450270967260834,0.892891962133153,0.));
#34612=DIRECTION('',(0.,0.,-1.));
#34613=DIRECTION('',(0.450270967260834,0.892891962133153,0.));
#34614=DIRECTION('center_axis',(0.,0.,1.));
#34615=DIRECTION('ref_axis',(1.,0.,0.));
#34616=DIRECTION('center_axis',(0.,0.,1.));
#34617=DIRECTION('ref_axis',(1.,0.,0.));
#34618=DIRECTION('',(0.728503342152264,-0.685042247217631,0.));
#34619=DIRECTION('center_axis',(0.685042247217631,0.728503342152264,0.));
#34620=DIRECTION('ref_axis',(0.728503342152264,-0.685042247217631,0.));
#34621=DIRECTION('',(0.,0.,-1.));
#34622=DIRECTION('',(0.728503342152264,-0.685042247217631,0.));
#34623=DIRECTION('center_axis',(0.,0.,-1.));
#34624=DIRECTION('ref_axis',(-1.,0.,0.));
#34625=DIRECTION('center_axis',(0.,0.,-1.));
#34626=DIRECTION('ref_axis',(1.,0.,0.));
#34627=DIRECTION('center_axis',(-0.685042247217632,0.728503342152263,0.));
#34628=DIRECTION('ref_axis',(0.728503342152263,0.685042247217632,0.));
#34629=DIRECTION('',(0.,0.,1.));
#34630=DIRECTION('',(0.728503342152263,0.685042247217632,0.));
#34631=DIRECTION('',(0.,0.,-1.));
#34632=DIRECTION('',(0.728503342152263,0.685042247217632,0.));
#34633=DIRECTION('center_axis',(0.,0.,1.));
#34634=DIRECTION('ref_axis',(1.,0.,0.));
#34635=DIRECTION('center_axis',(0.,0.,1.));
#34636=DIRECTION('ref_axis',(1.,0.,0.));
#34637=DIRECTION('',(0.450270967260841,-0.89289196213315,0.));
#34638=DIRECTION('center_axis',(0.89289196213315,0.450270967260841,0.));
#34639=DIRECTION('ref_axis',(0.450270967260841,-0.89289196213315,0.));
#34640=DIRECTION('',(0.,0.,-1.));
#34641=DIRECTION('',(0.450270967260841,-0.89289196213315,0.));
#34642=DIRECTION('center_axis',(0.,0.,-1.));
#34643=DIRECTION('ref_axis',(-1.,0.,0.));
#34644=DIRECTION('center_axis',(0.,0.,-1.));
#34645=DIRECTION('ref_axis',(1.,0.,0.));
#34646=DIRECTION('center_axis',(-0.394566327140866,0.918867462415863,0.));
#34647=DIRECTION('ref_axis',(0.918867462415863,0.394566327140866,0.));
#34648=DIRECTION('',(0.,0.,1.));
#34649=DIRECTION('',(0.918867462415863,0.394566327140866,0.));
#34650=DIRECTION('',(0.,0.,-1.));
#34651=DIRECTION('',(0.918867462415863,0.394566327140866,0.));
#34652=DIRECTION('center_axis',(0.,0.,1.));
#34653=DIRECTION('ref_axis',(1.,0.,0.));
#34654=DIRECTION('center_axis',(0.,0.,1.));
#34655=DIRECTION('ref_axis',(1.,0.,0.));
#34656=DIRECTION('',(0.117729268426029,-0.993045728733512,0.));
#34657=DIRECTION('center_axis',(0.993045728733512,0.117729268426029,0.));
#34658=DIRECTION('ref_axis',(0.117729268426029,-0.993045728733512,0.));
#34659=DIRECTION('',(0.,0.,-1.));
#34660=DIRECTION('',(0.117729268426029,-0.993045728733512,0.));
#34661=DIRECTION('center_axis',(0.,0.,-1.));
#34662=DIRECTION('ref_axis',(-1.,0.,0.));
#34663=DIRECTION('center_axis',(0.,0.,-1.));
#34664=DIRECTION('ref_axis',(1.,0.,0.));
#34665=DIRECTION('center_axis',(-0.0564998848320997,0.998402605672661,0.));
#34666=DIRECTION('ref_axis',(0.998402605672661,0.0564998848320997,0.));
#34667=DIRECTION('',(0.,0.,1.));
#34668=DIRECTION('',(0.998402605672661,0.0564998848320997,0.));
#34669=DIRECTION('',(0.,0.,-1.));
#34670=DIRECTION('',(0.998402605672661,0.0564998848320997,0.));
#34671=DIRECTION('center_axis',(0.,0.,1.));
#34672=DIRECTION('ref_axis',(1.,0.,0.));
#34673=DIRECTION('center_axis',(0.,0.,1.));
#34674=DIRECTION('ref_axis',(1.,0.,0.));
#34675=DIRECTION('',(-0.229012317679922,-0.973423524654541,0.));
#34676=DIRECTION('center_axis',(0.973423524654541,-0.229012317679922,0.));
#34677=DIRECTION('ref_axis',(-0.229012317679922,-0.973423524654541,0.));
#34678=DIRECTION('',(0.,0.,-1.));
#34679=DIRECTION('',(-0.229012317679922,-0.973423524654541,0.));
#34680=DIRECTION('center_axis',(0.,0.,-1.));
#34681=DIRECTION('ref_axis',(-1.,0.,0.));
#34682=DIRECTION('center_axis',(0.,0.,-1.));
#34683=DIRECTION('ref_axis',(1.,0.,0.));
#34684=DIRECTION('center_axis',(0.288381277436907,0.957515659832181,0.));
#34685=DIRECTION('ref_axis',(0.957515659832181,-0.288381277436907,0.));
#34686=DIRECTION('',(0.,0.,1.));
#34687=DIRECTION('',(0.957515659832181,-0.288381277436907,0.));
#34688=DIRECTION('',(0.,0.,-1.));
#34689=DIRECTION('',(0.957515659832181,-0.288381277436907,0.));
#34690=DIRECTION('center_axis',(0.,0.,1.));
#34691=DIRECTION('ref_axis',(1.,0.,0.));
#34692=DIRECTION('center_axis',(0.,0.,1.));
#34693=DIRECTION('ref_axis',(1.,0.,0.));
#34694=DIRECTION('',(-0.548131638411824,-0.836392077301052,0.));
#34695=DIRECTION('center_axis',(0.836392077301052,-0.548131638411824,0.));
#34696=DIRECTION('ref_axis',(-0.548131638411824,-0.836392077301052,0.));
#34697=DIRECTION('',(0.,0.,-1.));
#34698=DIRECTION('',(-0.548131638411824,-0.836392077301052,0.));
#34699=DIRECTION('center_axis',(0.,0.,-1.));
#34700=DIRECTION('ref_axis',(-1.,0.,0.));
#34701=DIRECTION('center_axis',(0.,0.,-1.));
#34702=DIRECTION('ref_axis',(1.,0.,0.));
#34703=DIRECTION('center_axis',(0.598479401592652,0.801138193989839,0.));
#34704=DIRECTION('ref_axis',(0.801138193989839,-0.598479401592652,0.));
#34705=DIRECTION('',(0.,0.,1.));
#34706=DIRECTION('',(0.801138193989839,-0.598479401592652,0.));
#34707=DIRECTION('',(0.,0.,-1.));
#34708=DIRECTION('',(0.801138193989839,-0.598479401592652,0.));
#34709=DIRECTION('center_axis',(0.,0.,1.));
#34710=DIRECTION('ref_axis',(1.,0.,0.));
#34711=DIRECTION('center_axis',(0.,0.,1.));
#34712=DIRECTION('ref_axis',(1.,0.,0.));
#34713=DIRECTION('',(-0.801138193989839,-0.598479401592652,0.));
#34714=DIRECTION('center_axis',(0.,0.,1.));
#34715=DIRECTION('ref_axis',(1.,0.,0.));
#34716=DIRECTION('center_axis',(0.598479401592652,-0.801138193989839,0.));
#34717=DIRECTION('ref_axis',(-0.801138193989839,-0.598479401592652,0.));
#34718=DIRECTION('',(0.,0.,-1.));
#34719=DIRECTION('',(-0.801138193989839,-0.598479401592652,0.));
#34720=DIRECTION('center_axis',(0.,0.,-1.));
#34721=DIRECTION('ref_axis',(-1.,0.,0.));
#34722=DIRECTION('center_axis',(0.,0.,-1.));
#34723=DIRECTION('ref_axis',(1.,0.,0.));
#34724=DIRECTION('center_axis',(0.,0.,-1.));
#34725=DIRECTION('ref_axis',(1.,0.,0.));
#34726=DIRECTION('center_axis',(0.728503342152263,0.685042247217632,0.));
#34727=DIRECTION('ref_axis',(0.685042247217632,-0.728503342152263,0.));
#34728=DIRECTION('',(0.,0.,1.));
#34729=DIRECTION('',(0.685042247217632,-0.728503342152263,0.));
#34730=DIRECTION('',(0.,0.,-1.));
#34731=DIRECTION('',(0.685042247217632,-0.728503342152263,0.));
#34732=DIRECTION('center_axis',(0.,0.,1.));
#34733=DIRECTION('ref_axis',(1.,0.,0.));
#34734=DIRECTION('center_axis',(0.,0.,1.));
#34735=DIRECTION('ref_axis',(1.,0.,0.));
#34736=DIRECTION('',(-0.892891962133152,-0.450270967260837,0.));
#34737=DIRECTION('center_axis',(0.450270967260837,-0.892891962133152,0.));
#34738=DIRECTION('ref_axis',(-0.892891962133152,-0.450270967260837,0.));
#34739=DIRECTION('',(0.,0.,-1.));
#34740=DIRECTION('',(-0.892891962133152,-0.450270967260837,0.));
#34741=DIRECTION('center_axis',(0.,0.,-1.));
#34742=DIRECTION('ref_axis',(-1.,0.,0.));
#34743=DIRECTION('center_axis',(0.,0.,-1.));
#34744=DIRECTION('ref_axis',(1.,0.,0.));
#34745=DIRECTION('center_axis',(0.918867462415866,0.394566327140858,0.));
#34746=DIRECTION('ref_axis',(0.394566327140858,-0.918867462415866,0.));
#34747=DIRECTION('',(0.,0.,1.));
#34748=DIRECTION('',(0.394566327140858,-0.918867462415866,0.));
#34749=DIRECTION('',(0.,0.,-1.));
#34750=DIRECTION('',(0.394566327140858,-0.918867462415866,0.));
#34751=DIRECTION('center_axis',(0.,0.,1.));
#34752=DIRECTION('ref_axis',(1.,0.,0.));
#34753=DIRECTION('center_axis',(0.,0.,1.));
#34754=DIRECTION('ref_axis',(1.,0.,0.));
#34755=DIRECTION('',(-0.993045728733513,-0.117729268426025,0.));
#34756=DIRECTION('center_axis',(0.117729268426025,-0.993045728733513,0.));
#34757=DIRECTION('ref_axis',(-0.993045728733513,-0.117729268426025,0.));
#34758=DIRECTION('',(0.,0.,-1.));
#34759=DIRECTION('',(-0.993045728733513,-0.117729268426025,0.));
#34760=DIRECTION('center_axis',(0.,0.,-1.));
#34761=DIRECTION('ref_axis',(-1.,0.,0.));
#34762=DIRECTION('center_axis',(0.,0.,-1.));
#34763=DIRECTION('ref_axis',(1.,0.,0.));
#34764=DIRECTION('center_axis',(0.998402605672661,0.0564998848320982,0.));
#34765=DIRECTION('ref_axis',(0.0564998848320982,-0.998402605672661,0.));
#34766=DIRECTION('',(0.,0.,1.));
#34767=DIRECTION('',(0.0564998848320982,-0.998402605672661,0.));
#34768=DIRECTION('',(0.,0.,-1.));
#34769=DIRECTION('',(0.0564998848320982,-0.998402605672661,0.));
#34770=DIRECTION('center_axis',(0.,0.,1.));
#34771=DIRECTION('ref_axis',(1.,0.,0.));
#34772=DIRECTION('center_axis',(0.,0.,1.));
#34773=DIRECTION('ref_axis',(1.,0.,0.));
#34774=DIRECTION('',(-0.973423524654541,0.229012317679922,0.));
#34775=DIRECTION('center_axis',(-0.229012317679922,-0.973423524654541,0.));
#34776=DIRECTION('ref_axis',(-0.973423524654541,0.229012317679922,0.));
#34777=DIRECTION('',(0.,0.,-1.));
#34778=DIRECTION('',(-0.973423524654541,0.229012317679922,0.));
#34779=DIRECTION('center_axis',(0.,0.,-1.));
#34780=DIRECTION('ref_axis',(-1.,0.,0.));
#34781=DIRECTION('center_axis',(0.,0.,-1.));
#34782=DIRECTION('ref_axis',(1.,0.,0.));
#34783=DIRECTION('center_axis',(0.957515659832181,-0.288381277436909,0.));
#34784=DIRECTION('ref_axis',(-0.288381277436909,-0.957515659832181,0.));
#34785=DIRECTION('',(0.,0.,1.));
#34786=DIRECTION('',(-0.288381277436909,-0.957515659832181,0.));
#34787=DIRECTION('',(0.,0.,-1.));
#34788=DIRECTION('',(-0.288381277436909,-0.957515659832181,0.));
#34789=DIRECTION('center_axis',(0.,0.,1.));
#34790=DIRECTION('ref_axis',(1.,0.,0.));
#34791=DIRECTION('center_axis',(0.,0.,1.));
#34792=DIRECTION('ref_axis',(1.,0.,0.));
#34793=DIRECTION('',(-0.836392077301054,0.548131638411822,0.));
#34794=DIRECTION('center_axis',(-0.548131638411822,-0.836392077301054,0.));
#34795=DIRECTION('ref_axis',(-0.836392077301054,0.548131638411822,0.));
#34796=DIRECTION('',(0.,0.,-1.));
#34797=DIRECTION('',(-0.836392077301054,0.548131638411822,0.));
#34798=DIRECTION('center_axis',(0.,0.,-1.));
#34799=DIRECTION('ref_axis',(-1.,0.,0.));
#34800=DIRECTION('center_axis',(0.,0.,-1.));
#34801=DIRECTION('ref_axis',(1.,0.,0.));
#34802=DIRECTION('center_axis',(0.801138193989838,-0.598479401592653,0.));
#34803=DIRECTION('ref_axis',(-0.598479401592653,-0.801138193989838,0.));
#34804=DIRECTION('',(0.,0.,1.));
#34805=DIRECTION('',(-0.598479401592653,-0.801138193989838,0.));
#34806=DIRECTION('',(0.,0.,-1.));
#34807=DIRECTION('',(-0.598479401592653,-0.801138193989838,0.));
#34808=DIRECTION('center_axis',(0.,0.,1.));
#34809=DIRECTION('ref_axis',(1.,0.,0.));
#34810=DIRECTION('center_axis',(0.,0.,1.));
#34811=DIRECTION('ref_axis',(1.,0.,0.));
#34812=DIRECTION('',(-0.598479401592653,0.801138193989838,0.));
#34813=DIRECTION('center_axis',(-0.801138193989838,-0.598479401592653,0.));
#34814=DIRECTION('ref_axis',(-0.598479401592653,0.801138193989838,0.));
#34815=DIRECTION('',(0.,0.,-1.));
#34816=DIRECTION('',(-0.598479401592653,0.801138193989838,0.));
#34817=DIRECTION('center_axis',(0.,0.,-1.));
#34818=DIRECTION('ref_axis',(-1.,0.,0.));
#34819=DIRECTION('center_axis',(0.,0.,-1.));
#34820=DIRECTION('ref_axis',(1.,0.,0.));
#34821=DIRECTION('center_axis',(0.548131638411824,-0.836392077301052,0.));
#34822=DIRECTION('ref_axis',(-0.836392077301052,-0.548131638411824,0.));
#34823=DIRECTION('',(0.,0.,1.));
#34824=DIRECTION('',(-0.836392077301052,-0.548131638411824,0.));
#34825=DIRECTION('',(0.,0.,-1.));
#34826=DIRECTION('',(-0.836392077301052,-0.548131638411824,0.));
#34827=DIRECTION('center_axis',(0.,0.,1.));
#34828=DIRECTION('ref_axis',(1.,0.,0.));
#34829=DIRECTION('center_axis',(0.,0.,1.));
#34830=DIRECTION('ref_axis',(1.,0.,0.));
#34831=DIRECTION('',(-0.288381277436909,0.957515659832181,0.));
#34832=DIRECTION('center_axis',(-0.957515659832181,-0.288381277436909,0.));
#34833=DIRECTION('ref_axis',(-0.288381277436909,0.957515659832181,0.));
#34834=DIRECTION('',(0.,0.,-1.));
#34835=DIRECTION('',(-0.288381277436909,0.957515659832181,0.));
#34836=DIRECTION('center_axis',(0.,0.,-1.));
#34837=DIRECTION('ref_axis',(-1.,0.,0.));
#34838=DIRECTION('center_axis',(0.,0.,-1.));
#34839=DIRECTION('ref_axis',(1.,0.,0.));
#34840=DIRECTION('center_axis',(0.229012317679921,-0.973423524654542,0.));
#34841=DIRECTION('ref_axis',(-0.973423524654542,-0.229012317679921,0.));
#34842=DIRECTION('',(0.,0.,1.));
#34843=DIRECTION('',(-0.973423524654542,-0.229012317679921,0.));
#34844=DIRECTION('',(0.,0.,-1.));
#34845=DIRECTION('',(-0.973423524654542,-0.229012317679921,0.));
#34846=DIRECTION('center_axis',(0.,0.,1.));
#34847=DIRECTION('ref_axis',(1.,0.,0.));
#34848=DIRECTION('center_axis',(0.,0.,1.));
#34849=DIRECTION('ref_axis',(1.,0.,0.));
#34850=DIRECTION('',(0.0564998848320982,0.998402605672661,0.));
#34851=DIRECTION('center_axis',(-0.998402605672661,0.0564998848320982,0.));
#34852=DIRECTION('ref_axis',(0.0564998848320982,0.998402605672661,0.));
#34853=DIRECTION('',(0.,0.,-1.));
#34854=DIRECTION('',(0.0564998848320982,0.998402605672661,0.));
#34855=DIRECTION('center_axis',(0.,0.,-1.));
#34856=DIRECTION('ref_axis',(-1.,0.,0.));
#34857=DIRECTION('center_axis',(0.,0.,-1.));
#34858=DIRECTION('ref_axis',(1.,0.,0.));
#34859=DIRECTION('center_axis',(-0.117729268426025,-0.993045728733512,0.));
#34860=DIRECTION('ref_axis',(-0.993045728733512,0.117729268426025,0.));
#34861=DIRECTION('',(0.,0.,1.));
#34862=DIRECTION('',(-0.993045728733512,0.117729268426025,0.));
#34863=DIRECTION('',(0.,0.,-1.));
#34864=DIRECTION('',(-0.993045728733512,0.117729268426025,0.));
#34865=DIRECTION('center_axis',(0.,0.,1.));
#34866=DIRECTION('ref_axis',(1.,0.,0.));
#34867=DIRECTION('center_axis',(0.,0.,1.));
#34868=DIRECTION('ref_axis',(1.,0.,0.));
#34869=DIRECTION('',(0.394566327140861,0.918867462415865,0.));
#34870=DIRECTION('center_axis',(-0.918867462415865,0.394566327140861,0.));
#34871=DIRECTION('ref_axis',(0.394566327140861,0.918867462415865,0.));
#34872=DIRECTION('',(0.,0.,-1.));
#34873=DIRECTION('',(0.394566327140861,0.918867462415865,0.));
#34874=DIRECTION('center_axis',(0.,0.,-1.));
#34875=DIRECTION('ref_axis',(-1.,0.,0.));
#34876=DIRECTION('center_axis',(0.,0.,-1.));
#34877=DIRECTION('ref_axis',(1.,0.,0.));
#34878=DIRECTION('center_axis',(-0.450270967260838,-0.892891962133151,0.));
#34879=DIRECTION('ref_axis',(-0.892891962133151,0.450270967260838,0.));
#34880=DIRECTION('',(0.,0.,1.));
#34881=DIRECTION('',(-0.892891962133151,0.450270967260838,0.));
#34882=DIRECTION('',(0.,0.,-1.));
#34883=DIRECTION('',(-0.892891962133151,0.450270967260838,0.));
#34884=DIRECTION('center_axis',(0.,0.,1.));
#34885=DIRECTION('ref_axis',(1.,0.,0.));
#34886=DIRECTION('center_axis',(0.,0.,1.));
#34887=DIRECTION('ref_axis',(1.,0.,0.));
#34888=DIRECTION('',(0.685042247217633,0.728503342152262,0.));
#34889=DIRECTION('center_axis',(-0.728503342152262,0.685042247217633,0.));
#34890=DIRECTION('ref_axis',(0.685042247217633,0.728503342152262,0.));
#34891=DIRECTION('',(0.,0.,-1.));
#34892=DIRECTION('',(0.685042247217633,0.728503342152262,0.));
#34893=DIRECTION('center_axis',(0.,0.,-1.));
#34894=DIRECTION('ref_axis',(-1.,0.,0.));
#34895=DIRECTION('center_axis',(0.,0.,-1.));
#34896=DIRECTION('ref_axis',(1.,0.,0.));
#34897=DIRECTION('center_axis',(-0.288381277436908,-0.957515659832181,0.));
#34898=DIRECTION('ref_axis',(-0.957515659832181,0.288381277436908,0.));
#34899=DIRECTION('',(0.,0.,1.));
#34900=DIRECTION('',(-0.957515659832181,0.288381277436908,0.));
#34901=DIRECTION('',(0.,0.,-1.));
#34902=DIRECTION('',(-0.957515659832181,0.288381277436908,0.));
#34903=DIRECTION('center_axis',(0.,0.,1.));
#34904=DIRECTION('ref_axis',(1.,0.,0.));
#34905=DIRECTION('center_axis',(0.,0.,1.));
#34906=DIRECTION('ref_axis',(1.,0.,0.));
#34907=DIRECTION('',(0.548131638411823,0.836392077301053,0.));
#34908=DIRECTION('center_axis',(-0.836392077301053,0.548131638411823,0.));
#34909=DIRECTION('ref_axis',(0.548131638411823,0.836392077301053,0.));
#34910=DIRECTION('',(0.,0.,-1.));
#34911=DIRECTION('',(0.548131638411823,0.836392077301053,0.));
#34912=DIRECTION('center_axis',(0.,0.,-1.));
#34913=DIRECTION('ref_axis',(-1.,0.,0.));
#34914=DIRECTION('center_axis',(0.,0.,-1.));
#34915=DIRECTION('ref_axis',(1.,0.,0.));
#34916=DIRECTION('center_axis',(0.0564998848320982,-0.998402605672661,0.));
#34917=DIRECTION('ref_axis',(-0.998402605672661,-0.0564998848320982,0.));
#34918=DIRECTION('',(0.,0.,1.));
#34919=DIRECTION('',(-0.998402605672661,-0.0564998848320982,0.));
#34920=DIRECTION('',(0.,0.,-1.));
#34921=DIRECTION('',(-0.998402605672661,-0.0564998848320982,0.));
#34922=DIRECTION('center_axis',(0.,0.,1.));
#34923=DIRECTION('ref_axis',(1.,0.,0.));
#34924=DIRECTION('center_axis',(0.,0.,1.));
#34925=DIRECTION('ref_axis',(1.,0.,0.));
#34926=DIRECTION('',(0.22901231767992,0.973423524654542,0.));
#34927=DIRECTION('center_axis',(-0.973423524654542,0.22901231767992,0.));
#34928=DIRECTION('ref_axis',(0.22901231767992,0.973423524654542,0.));
#34929=DIRECTION('',(0.,0.,-1.));
#34930=DIRECTION('',(0.22901231767992,0.973423524654542,0.));
#34931=DIRECTION('center_axis',(0.,0.,-1.));
#34932=DIRECTION('ref_axis',(-1.,0.,0.));
#34933=DIRECTION('center_axis',(0.,0.,-1.));
#34934=DIRECTION('ref_axis',(1.,0.,0.));
#34935=DIRECTION('center_axis',(0.394566327140863,-0.918867462415864,0.));
#34936=DIRECTION('ref_axis',(-0.918867462415864,-0.394566327140863,0.));
#34937=DIRECTION('',(0.,0.,1.));
#34938=DIRECTION('',(-0.918867462415864,-0.394566327140863,0.));
#34939=DIRECTION('',(0.,0.,-1.));
#34940=DIRECTION('',(-0.918867462415864,-0.394566327140863,0.));
#34941=DIRECTION('center_axis',(0.,0.,1.));
#34942=DIRECTION('ref_axis',(1.,0.,0.));
#34943=DIRECTION('center_axis',(0.,0.,1.));
#34944=DIRECTION('ref_axis',(1.,0.,0.));
#34945=DIRECTION('',(-0.117729268426026,0.993045728733512,0.));
#34946=DIRECTION('center_axis',(-0.993045728733512,-0.117729268426026,0.));
#34947=DIRECTION('ref_axis',(-0.117729268426026,0.993045728733512,0.));
#34948=DIRECTION('',(0.,0.,-1.));
#34949=DIRECTION('',(-0.117729268426026,0.993045728733512,0.));
#34950=DIRECTION('center_axis',(0.,0.,-1.));
#34951=DIRECTION('ref_axis',(-1.,0.,0.));
#34952=DIRECTION('center_axis',(0.,0.,-1.));
#34953=DIRECTION('ref_axis',(1.,0.,0.));
#34954=DIRECTION('center_axis',(0.685042247217634,-0.728503342152261,0.));
#34955=DIRECTION('ref_axis',(-0.728503342152261,-0.685042247217634,0.));
#34956=DIRECTION('',(0.,0.,1.));
#34957=DIRECTION('',(-0.728503342152261,-0.685042247217634,0.));
#34958=DIRECTION('',(0.,0.,-1.));
#34959=DIRECTION('',(-0.728503342152261,-0.685042247217634,0.));
#34960=DIRECTION('center_axis',(0.,0.,1.));
#34961=DIRECTION('ref_axis',(1.,0.,0.));
#34962=DIRECTION('center_axis',(0.,0.,1.));
#34963=DIRECTION('ref_axis',(1.,0.,0.));
#34964=DIRECTION('',(-0.450270967260839,0.892891962133151,0.));
#34965=DIRECTION('center_axis',(-0.892891962133151,-0.450270967260839,0.));
#34966=DIRECTION('ref_axis',(-0.450270967260839,0.892891962133151,0.));
#34967=DIRECTION('',(0.,0.,-1.));
#34968=DIRECTION('',(-0.450270967260839,0.892891962133151,0.));
#34969=DIRECTION('center_axis',(0.,0.,-1.));
#34970=DIRECTION('ref_axis',(-1.,0.,0.));
#34971=DIRECTION('center_axis',(0.,0.,-1.));
#34972=DIRECTION('ref_axis',(1.,0.,0.));
#34973=DIRECTION('center_axis',(0.892891962133151,-0.450270967260839,0.));
#34974=DIRECTION('ref_axis',(-0.450270967260839,-0.892891962133151,0.));
#34975=DIRECTION('',(0.,0.,1.));
#34976=DIRECTION('',(-0.450270967260839,-0.892891962133151,0.));
#34977=DIRECTION('',(0.,0.,-1.));
#34978=DIRECTION('',(-0.450270967260839,-0.892891962133151,0.));
#34979=DIRECTION('center_axis',(0.,0.,1.));
#34980=DIRECTION('ref_axis',(1.,0.,0.));
#34981=DIRECTION('center_axis',(0.,0.,1.));
#34982=DIRECTION('ref_axis',(1.,0.,0.));
#34983=DIRECTION('',(-0.728503342152262,0.685042247217633,0.));
#34984=DIRECTION('center_axis',(-0.685042247217633,-0.728503342152262,0.));
#34985=DIRECTION('ref_axis',(-0.728503342152262,0.685042247217633,0.));
#34986=DIRECTION('',(0.,0.,-1.));
#34987=DIRECTION('',(-0.728503342152262,0.685042247217633,0.));
#34988=DIRECTION('center_axis',(0.,0.,-1.));
#34989=DIRECTION('ref_axis',(-1.,0.,0.));
#34990=DIRECTION('center_axis',(0.,0.,-1.));
#34991=DIRECTION('ref_axis',(1.,0.,0.));
#34992=DIRECTION('center_axis',(0.993045728733513,-0.117729268426024,0.));
#34993=DIRECTION('ref_axis',(-0.117729268426024,-0.993045728733513,0.));
#34994=DIRECTION('',(0.,0.,1.));
#34995=DIRECTION('',(-0.117729268426024,-0.993045728733513,0.));
#34996=DIRECTION('',(0.,0.,-1.));
#34997=DIRECTION('',(-0.117729268426024,-0.993045728733513,0.));
#34998=DIRECTION('center_axis',(0.,0.,1.));
#34999=DIRECTION('ref_axis',(1.,0.,0.));
#35000=DIRECTION('center_axis',(0.,0.,1.));
#35001=DIRECTION('ref_axis',(1.,0.,0.));
#35002=DIRECTION('',(-0.918867462415865,0.39456632714086,0.));
#35003=DIRECTION('center_axis',(-0.39456632714086,-0.918867462415865,0.));
#35004=DIRECTION('ref_axis',(-0.918867462415865,0.39456632714086,0.));
#35005=DIRECTION('',(0.,0.,-1.));
#35006=DIRECTION('',(-0.918867462415865,0.39456632714086,0.));
#35007=DIRECTION('center_axis',(0.,0.,-1.));
#35008=DIRECTION('ref_axis',(-1.,0.,0.));
#35009=DIRECTION('center_axis',(0.,0.,-1.));
#35010=DIRECTION('ref_axis',(1.,0.,0.));
#35011=DIRECTION('center_axis',(0.973423524654542,0.229012317679921,0.));
#35012=DIRECTION('ref_axis',(0.229012317679921,-0.973423524654542,0.));
#35013=DIRECTION('',(0.,0.,1.));
#35014=DIRECTION('',(0.229012317679921,-0.973423524654542,0.));
#35015=DIRECTION('',(0.,0.,-1.));
#35016=DIRECTION('',(0.229012317679921,-0.973423524654542,0.));
#35017=DIRECTION('center_axis',(0.,0.,1.));
#35018=DIRECTION('ref_axis',(1.,0.,0.));
#35019=DIRECTION('center_axis',(0.,0.,1.));
#35020=DIRECTION('ref_axis',(1.,0.,0.));
#35021=DIRECTION('',(-0.998402605672661,0.0564998848320951,0.));
#35022=DIRECTION('center_axis',(-0.0564998848320951,-0.998402605672661,
0.));
#35023=DIRECTION('ref_axis',(-0.998402605672661,0.0564998848320951,0.));
#35024=DIRECTION('',(0.,0.,-1.));
#35025=DIRECTION('',(-0.998402605672661,0.0564998848320951,0.));
#35026=DIRECTION('center_axis',(0.,0.,-1.));
#35027=DIRECTION('ref_axis',(-1.,0.,0.));
#35028=DIRECTION('center_axis',(0.,0.,-1.));
#35029=DIRECTION('ref_axis',(1.,0.,0.));
#35030=DIRECTION('center_axis',(0.836392077301052,0.548131638411824,0.));
#35031=DIRECTION('ref_axis',(0.548131638411824,-0.836392077301052,0.));
#35032=DIRECTION('',(0.,0.,1.));
#35033=DIRECTION('',(0.548131638411824,-0.836392077301052,0.));
#35034=DIRECTION('',(0.,0.,-1.));
#35035=DIRECTION('',(0.548131638411824,-0.836392077301052,0.));
#35036=DIRECTION('center_axis',(0.,0.,1.));
#35037=DIRECTION('ref_axis',(1.,0.,0.));
#35038=DIRECTION('center_axis',(0.,0.,1.));
#35039=DIRECTION('ref_axis',(1.,0.,0.));
#35040=DIRECTION('',(-0.95751565983218,-0.288381277436911,0.));
#35041=DIRECTION('center_axis',(0.288381277436911,-0.95751565983218,0.));
#35042=DIRECTION('ref_axis',(-0.95751565983218,-0.288381277436911,0.));
#35043=DIRECTION('',(0.,0.,-1.));
#35044=DIRECTION('',(-0.95751565983218,-0.288381277436911,0.));
#35045=DIRECTION('center_axis',(0.,0.,-1.));
#35046=DIRECTION('ref_axis',(-1.,0.,0.));
#35047=DIRECTION('center_axis',(0.,0.,-1.));
#35048=DIRECTION('ref_axis',(1.,0.,0.));
#35049=DIRECTION('center_axis',(0.,0.,1.));
#35050=DIRECTION('ref_axis',(1.,0.,0.));
#35051=DIRECTION('center_axis',(0.,0.,1.));
#35052=DIRECTION('ref_axis',(1.,0.,0.));
#35053=DIRECTION('',(-0.801138193989839,0.598479401592653,0.));
#35054=DIRECTION('',(0.801138193989839,0.598479401592653,0.));
#35055=DIRECTION('center_axis',(-0.598479401592653,-0.801138193989839,0.));
#35056=DIRECTION('ref_axis',(-0.801138193989839,0.598479401592653,0.));
#35057=DIRECTION('',(0.,0.,1.));
#35058=DIRECTION('',(-0.801138193989839,0.598479401592653,0.));
#35059=DIRECTION('',(0.,0.,-1.));
#35060=DIRECTION('center_axis',(-0.598479401592653,0.801138193989839,0.));
#35061=DIRECTION('ref_axis',(0.801138193989839,0.598479401592653,0.));
#35062=DIRECTION('',(0.,0.,-1.));
#35063=DIRECTION('',(0.801138193989839,0.598479401592653,0.));
#35064=DIRECTION('center_axis',(0.,0.,-1.));
#35065=DIRECTION('ref_axis',(-1.,0.,0.));
#35066=DIRECTION('center_axis',(0.,0.,-1.));
#35067=DIRECTION('ref_axis',(1.,0.,0.));
#35068=DIRECTION('center_axis',(0.450270967260841,0.89289196213315,0.));
#35069=DIRECTION('ref_axis',(0.89289196213315,-0.450270967260841,0.));
#35070=DIRECTION('',(0.,0.,1.));
#35071=DIRECTION('',(0.89289196213315,-0.450270967260841,0.));
#35072=DIRECTION('',(0.,0.,-1.));
#35073=DIRECTION('',(0.89289196213315,-0.450270967260841,0.));
#35074=DIRECTION('center_axis',(0.,0.,1.));
#35075=DIRECTION('ref_axis',(1.,0.,0.));
#35076=DIRECTION('center_axis',(0.,0.,1.));
#35077=DIRECTION('ref_axis',(1.,0.,0.));
#35078=DIRECTION('',(-0.685042247217634,-0.728503342152261,0.));
#35079=DIRECTION('center_axis',(0.728503342152261,-0.685042247217634,0.));
#35080=DIRECTION('ref_axis',(-0.685042247217634,-0.728503342152261,0.));
#35081=DIRECTION('',(0.,0.,-1.));
#35082=DIRECTION('',(-0.685042247217634,-0.728503342152261,0.));
#35083=DIRECTION('center_axis',(0.,0.,-1.));
#35084=DIRECTION('ref_axis',(-1.,0.,0.));
#35085=DIRECTION('center_axis',(0.,0.,-1.));
#35086=DIRECTION('ref_axis',(1.,0.,0.));
#35087=DIRECTION('center_axis',(0.117729268426028,0.993045728733512,0.));
#35088=DIRECTION('ref_axis',(0.993045728733512,-0.117729268426028,0.));
#35089=DIRECTION('',(0.,0.,1.));
#35090=DIRECTION('',(0.993045728733512,-0.117729268426028,0.));
#35091=DIRECTION('',(0.,0.,-1.));
#35092=DIRECTION('',(0.993045728733512,-0.117729268426028,0.));
#35093=DIRECTION('center_axis',(0.,0.,1.));
#35094=DIRECTION('ref_axis',(1.,0.,0.));
#35095=DIRECTION('center_axis',(0.,0.,1.));
#35096=DIRECTION('ref_axis',(1.,0.,0.));
#35097=DIRECTION('',(-0.394566327140863,-0.918867462415864,0.));
#35098=DIRECTION('center_axis',(0.918867462415864,-0.394566327140863,0.));
#35099=DIRECTION('ref_axis',(-0.394566327140863,-0.918867462415864,0.));
#35100=DIRECTION('',(0.,0.,-1.));
#35101=DIRECTION('',(-0.394566327140863,-0.918867462415864,0.));
#35102=DIRECTION('center_axis',(0.,0.,-1.));
#35103=DIRECTION('ref_axis',(-1.,0.,0.));
#35104=DIRECTION('center_axis',(0.,0.,-1.));
#35105=DIRECTION('ref_axis',(1.,0.,0.));
#35106=DIRECTION('center_axis',(-0.22901231767992,0.973423524654542,0.));
#35107=DIRECTION('ref_axis',(0.973423524654542,0.22901231767992,0.));
#35108=DIRECTION('',(0.,0.,1.));
#35109=DIRECTION('',(0.973423524654542,0.22901231767992,0.));
#35110=DIRECTION('',(0.,0.,-1.));
#35111=DIRECTION('',(0.973423524654542,0.22901231767992,0.));
#35112=DIRECTION('center_axis',(0.,0.,1.));
#35113=DIRECTION('ref_axis',(1.,0.,0.));
#35114=DIRECTION('center_axis',(0.,0.,1.));
#35115=DIRECTION('ref_axis',(1.,0.,0.));
#35116=DIRECTION('',(-0.0564998848320967,-0.998402605672661,0.));
#35117=DIRECTION('center_axis',(0.998402605672661,-0.0564998848320967,0.));
#35118=DIRECTION('ref_axis',(-0.0564998848320967,-0.998402605672661,0.));
#35119=DIRECTION('',(0.,0.,-1.));
#35120=DIRECTION('',(-0.0564998848320967,-0.998402605672661,0.));
#35121=DIRECTION('center_axis',(0.,0.,-1.));
#35122=DIRECTION('ref_axis',(-1.,0.,0.));
#35123=DIRECTION('center_axis',(0.,0.,-1.));
#35124=DIRECTION('ref_axis',(1.,0.,0.));
#35125=DIRECTION('center_axis',(-0.548131638411821,0.836392077301054,0.));
#35126=DIRECTION('ref_axis',(0.836392077301054,0.548131638411821,0.));
#35127=DIRECTION('',(0.,0.,1.));
#35128=DIRECTION('',(0.836392077301054,0.548131638411821,0.));
#35129=DIRECTION('',(0.,0.,-1.));
#35130=DIRECTION('',(0.836392077301054,0.548131638411821,0.));
#35131=DIRECTION('center_axis',(0.,0.,1.));
#35132=DIRECTION('ref_axis',(1.,0.,0.));
#35133=DIRECTION('center_axis',(0.,0.,1.));
#35134=DIRECTION('ref_axis',(1.,0.,0.));
#35135=DIRECTION('',(0.288381277436903,-0.957515659832182,0.));
#35136=DIRECTION('center_axis',(0.957515659832182,0.288381277436903,0.));
#35137=DIRECTION('ref_axis',(0.288381277436903,-0.957515659832182,0.));
#35138=DIRECTION('',(0.,0.,-1.));
#35139=DIRECTION('',(0.288381277436903,-0.957515659832182,0.));
#35140=DIRECTION('center_axis',(0.,0.,-1.));
#35141=DIRECTION('ref_axis',(-1.,0.,0.));
#35142=DIRECTION('center_axis',(0.,0.,-1.));
#35143=DIRECTION('ref_axis',(1.,0.,0.));
#35144=DIRECTION('center_axis',(-0.801138193989837,0.598479401592655,0.));
#35145=DIRECTION('ref_axis',(0.598479401592655,0.801138193989837,0.));
#35146=DIRECTION('',(0.,0.,1.));
#35147=DIRECTION('',(0.598479401592655,0.801138193989837,0.));
#35148=DIRECTION('',(0.,0.,-1.));
#35149=DIRECTION('',(0.598479401592655,0.801138193989837,0.));
#35150=DIRECTION('center_axis',(0.,0.,1.));
#35151=DIRECTION('ref_axis',(1.,0.,0.));
#35152=DIRECTION('center_axis',(0.,0.,1.));
#35153=DIRECTION('ref_axis',(1.,0.,0.));
#35154=DIRECTION('',(0.598479401592655,-0.801138193989837,0.));
#35155=DIRECTION('center_axis',(0.801138193989837,0.598479401592655,0.));
#35156=DIRECTION('ref_axis',(0.598479401592655,-0.801138193989837,0.));
#35157=DIRECTION('',(0.,0.,-1.));
#35158=DIRECTION('',(0.598479401592655,-0.801138193989837,0.));
#35159=DIRECTION('center_axis',(0.,0.,-1.));
#35160=DIRECTION('ref_axis',(-1.,0.,0.));
#35161=DIRECTION('center_axis',(0.,0.,-1.));
#35162=DIRECTION('ref_axis',(1.,0.,0.));
#35163=DIRECTION('center_axis',(-0.95751565983218,0.288381277436912,0.));
#35164=DIRECTION('ref_axis',(0.288381277436912,0.95751565983218,0.));
#35165=DIRECTION('',(0.,0.,1.));
#35166=DIRECTION('',(0.288381277436912,0.95751565983218,0.));
#35167=DIRECTION('',(0.,0.,-1.));
#35168=DIRECTION('',(0.288381277436912,0.95751565983218,0.));
#35169=DIRECTION('center_axis',(0.,0.,1.));
#35170=DIRECTION('ref_axis',(1.,0.,0.));
#35171=DIRECTION('center_axis',(0.,0.,1.));
#35172=DIRECTION('ref_axis',(1.,0.,0.));
#35173=DIRECTION('',(0.836392077301051,-0.548131638411826,0.));
#35174=DIRECTION('center_axis',(0.548131638411826,0.836392077301051,0.));
#35175=DIRECTION('ref_axis',(0.836392077301051,-0.548131638411826,0.));
#35176=DIRECTION('',(0.,0.,-1.));
#35177=DIRECTION('',(0.836392077301051,-0.548131638411826,0.));
#35178=DIRECTION('center_axis',(0.,0.,-1.));
#35179=DIRECTION('ref_axis',(-1.,0.,0.));
#35180=DIRECTION('center_axis',(0.,0.,-1.));
#35181=DIRECTION('ref_axis',(1.,0.,0.));
#35182=DIRECTION('center_axis',(-0.998402605672661,-0.0564998848320951,
0.));
#35183=DIRECTION('ref_axis',(-0.0564998848320951,0.998402605672661,0.));
#35184=DIRECTION('',(0.,0.,1.));
#35185=DIRECTION('',(-0.0564998848320951,0.998402605672661,0.));
#35186=DIRECTION('',(0.,0.,-1.));
#35187=DIRECTION('',(-0.0564998848320951,0.998402605672661,0.));
#35188=DIRECTION('center_axis',(0.,0.,1.));
#35189=DIRECTION('ref_axis',(1.,0.,0.));
#35190=DIRECTION('center_axis',(0.,0.,1.));
#35191=DIRECTION('ref_axis',(1.,0.,0.));
#35192=DIRECTION('',(0.973423524654543,-0.229012317679917,0.));
#35193=DIRECTION('center_axis',(0.229012317679917,0.973423524654543,0.));
#35194=DIRECTION('ref_axis',(0.973423524654543,-0.229012317679917,0.));
#35195=DIRECTION('',(0.,0.,-1.));
#35196=DIRECTION('',(0.973423524654543,-0.229012317679917,0.));
#35197=DIRECTION('center_axis',(0.,0.,-1.));
#35198=DIRECTION('ref_axis',(-1.,0.,0.));
#35199=DIRECTION('center_axis',(0.,0.,-1.));
#35200=DIRECTION('ref_axis',(1.,0.,0.));
#35201=DIRECTION('center_axis',(-0.918867462415863,-0.394566327140866,0.));
#35202=DIRECTION('ref_axis',(-0.394566327140866,0.918867462415863,0.));
#35203=DIRECTION('',(0.,0.,1.));
#35204=DIRECTION('',(-0.394566327140866,0.918867462415863,0.));
#35205=DIRECTION('',(0.,0.,-1.));
#35206=DIRECTION('',(-0.394566327140866,0.918867462415863,0.));
#35207=DIRECTION('center_axis',(0.,0.,1.));
#35208=DIRECTION('ref_axis',(1.,0.,0.));
#35209=DIRECTION('center_axis',(0.,0.,1.));
#35210=DIRECTION('ref_axis',(1.,0.,0.));
#35211=DIRECTION('',(0.993045728733512,0.117729268426028,0.));
#35212=DIRECTION('center_axis',(-0.117729268426028,0.993045728733512,0.));
#35213=DIRECTION('ref_axis',(0.993045728733512,0.117729268426028,0.));
#35214=DIRECTION('',(0.,0.,-1.));
#35215=DIRECTION('',(0.993045728733512,0.117729268426028,0.));
#35216=DIRECTION('center_axis',(0.,0.,-1.));
#35217=DIRECTION('ref_axis',(-1.,0.,0.));
#35218=DIRECTION('center_axis',(0.,0.,-1.));
#35219=DIRECTION('ref_axis',(1.,0.,0.));
#35220=DIRECTION('center_axis',(-0.728503342152263,-0.685042247217632,0.));
#35221=DIRECTION('ref_axis',(-0.685042247217632,0.728503342152263,0.));
#35222=DIRECTION('',(0.,0.,1.));
#35223=DIRECTION('',(-0.685042247217632,0.728503342152263,0.));
#35224=DIRECTION('',(0.,0.,-1.));
#35225=DIRECTION('',(-0.685042247217632,0.728503342152263,0.));
#35226=DIRECTION('center_axis',(0.,0.,1.));
#35227=DIRECTION('ref_axis',(1.,0.,0.));
#35228=DIRECTION('center_axis',(0.,0.,1.));
#35229=DIRECTION('ref_axis',(1.,0.,0.));
#35230=DIRECTION('',(0.89289196213315,0.450270967260841,0.));
#35231=DIRECTION('center_axis',(-0.450270967260841,0.89289196213315,0.));
#35232=DIRECTION('ref_axis',(0.89289196213315,0.450270967260841,0.));
#35233=DIRECTION('',(0.,0.,-1.));
#35234=DIRECTION('',(0.89289196213315,0.450270967260841,0.));
#35235=DIRECTION('center_axis',(0.,0.,-1.));
#35236=DIRECTION('ref_axis',(-1.,0.,0.));
#35237=DIRECTION('center_axis',(0.,0.,-1.));
#35238=DIRECTION('ref_axis',(1.,0.,0.));
#35239=DIRECTION('center_axis',(0.,0.,-1.));
#35240=DIRECTION('ref_axis',(-1.,0.,0.));
#35241=DIRECTION('center_axis',(0.,0.,1.));
#35242=DIRECTION('ref_axis',(1.,0.,0.));
#35243=DIRECTION('center_axis',(0.,0.,1.));
#35244=DIRECTION('ref_axis',(1.,0.,0.));
#35245=DIRECTION('',(0.707106781186549,8.65956056235495E-17,-0.707106781186546));
#35246=DIRECTION('center_axis',(0.,0.,1.));
#35247=DIRECTION('ref_axis',(1.,0.,0.));
#35248=DIRECTION('center_axis',(0.,0.,1.));
#35249=DIRECTION('ref_axis',(1.,0.,0.));
#35250=DIRECTION('',(0.707106781186548,8.65956056235494E-17,-0.707106781186547));
#35251=DIRECTION('center_axis',(0.,0.,1.));
#35252=DIRECTION('ref_axis',(1.,0.,0.));
#35253=DIRECTION('center_axis',(0.,0.,1.));
#35254=DIRECTION('ref_axis',(1.,0.,0.));
#35255=DIRECTION('center_axis',(0.,0.,1.));
#35256=DIRECTION('ref_axis',(1.,0.,0.));
#35257=DIRECTION('center_axis',(0.,0.,1.));
#35258=DIRECTION('ref_axis',(1.,0.,0.));
#35259=DIRECTION('center_axis',(0.,0.,1.));
#35260=DIRECTION('ref_axis',(1.,0.,0.));
#35261=DIRECTION('center_axis',(0.,0.,1.));
#35262=DIRECTION('ref_axis',(1.,0.,0.));
#35263=DIRECTION('center_axis',(0.,0.,1.));
#35264=DIRECTION('ref_axis',(1.,0.,0.));
#35265=DIRECTION('center_axis',(0.,0.,1.));
#35266=DIRECTION('ref_axis',(1.,0.,0.));
#35267=DIRECTION('center_axis',(0.,0.,1.));
#35268=DIRECTION('ref_axis',(1.,0.,0.));
#35269=DIRECTION('center_axis',(0.,0.,1.));
#35270=DIRECTION('ref_axis',(1.,0.,0.));
#35271=DIRECTION('center_axis',(0.,0.,1.));
#35272=DIRECTION('ref_axis',(1.,0.,0.));
#35273=DIRECTION('center_axis',(0.,0.,1.));
#35274=DIRECTION('ref_axis',(1.,0.,0.));
#35275=DIRECTION('center_axis',(0.,0.,1.));
#35276=DIRECTION('ref_axis',(1.,0.,0.));
#35277=DIRECTION('center_axis',(0.,0.,1.));
#35278=DIRECTION('ref_axis',(1.,0.,0.));
#35279=DIRECTION('center_axis',(0.,0.,1.));
#35280=DIRECTION('ref_axis',(1.,0.,0.));
#35281=DIRECTION('center_axis',(0.,0.,1.));
#35282=DIRECTION('ref_axis',(1.,0.,0.));
#35283=DIRECTION('center_axis',(0.,0.,1.));
#35284=DIRECTION('ref_axis',(1.,0.,0.));
#35285=DIRECTION('',(0.,0.,-1.));
#35286=DIRECTION('center_axis',(0.,0.,1.));
#35287=DIRECTION('ref_axis',(1.,0.,0.));
#35288=DIRECTION('center_axis',(0.,0.,1.));
#35289=DIRECTION('ref_axis',(1.,0.,0.));
#35290=DIRECTION('center_axis',(0.,0.,1.));
#35291=DIRECTION('ref_axis',(1.,0.,0.));
#35292=DIRECTION('center_axis',(0.,0.,1.));
#35293=DIRECTION('ref_axis',(1.,0.,0.));
#35294=DIRECTION('center_axis',(0.,0.,1.));
#35295=DIRECTION('ref_axis',(1.,0.,0.));
#35296=DIRECTION('center_axis',(0.,0.,1.));
#35297=DIRECTION('ref_axis',(1.,0.,0.));
#35298=DIRECTION('center_axis',(0.,0.,1.));
#35299=DIRECTION('ref_axis',(1.,0.,0.));
#35300=DIRECTION('center_axis',(0.,0.,1.));
#35301=DIRECTION('ref_axis',(1.,0.,0.));
#35302=DIRECTION('center_axis',(0.,0.,1.));
#35303=DIRECTION('ref_axis',(1.,0.,0.));
#35304=DIRECTION('center_axis',(0.,0.,1.));
#35305=DIRECTION('ref_axis',(1.,0.,0.));
#35306=DIRECTION('center_axis',(0.,0.,1.));
#35307=DIRECTION('ref_axis',(1.,0.,0.));
#35308=DIRECTION('center_axis',(0.,0.,1.));
#35309=DIRECTION('ref_axis',(1.,0.,0.));
#35310=DIRECTION('center_axis',(0.,0.,1.));
#35311=DIRECTION('ref_axis',(1.,0.,0.));
#35312=DIRECTION('center_axis',(0.,0.,1.));
#35313=DIRECTION('ref_axis',(1.,0.,0.));
#35314=DIRECTION('center_axis',(0.,0.,1.));
#35315=DIRECTION('ref_axis',(1.,0.,0.));
#35316=DIRECTION('center_axis',(0.,0.,1.));
#35317=DIRECTION('ref_axis',(1.,0.,0.));
#35318=DIRECTION('center_axis',(0.,0.,1.));
#35319=DIRECTION('ref_axis',(1.,0.,0.));
#35320=DIRECTION('center_axis',(0.,0.,1.));
#35321=DIRECTION('ref_axis',(1.,0.,0.));
#35322=DIRECTION('center_axis',(0.,0.,1.));
#35323=DIRECTION('ref_axis',(1.,0.,0.));
#35324=DIRECTION('center_axis',(0.,0.,1.));
#35325=DIRECTION('ref_axis',(1.,0.,0.));
#35326=DIRECTION('center_axis',(0.,0.,-1.));
#35327=DIRECTION('ref_axis',(1.,0.,0.));
#35328=DIRECTION('center_axis',(0.,0.,1.));
#35329=DIRECTION('ref_axis',(1.,0.,0.));
#35330=DIRECTION('',(-0.707106781186548,-8.65956056235493E-17,-0.707106781186547));
#35331=DIRECTION('center_axis',(0.,0.,1.));
#35332=DIRECTION('ref_axis',(1.,0.,0.));
#69065=CARTESIAN_POINT('',(0.,0.,0.));
#69066=CARTESIAN_POINT('Origin',(0.,0.,-1.725));
#69067=CARTESIAN_POINT('',(-0.493073791100261,0.0002448543660152,-3.40911584740964));
#69068=CARTESIAN_POINT('',(-0.492742936816498,0.00014446300365779,-3.43088415259036));
#69069=CARTESIAN_POINT('',(-0.4925,-6.03138548580071E-17,-1.725));
#69070=CARTESIAN_POINT('',(0.217167145730328,0.442422208592295,-3.4575));
#69071=CARTESIAN_POINT('Ctrl Pts',(-0.493073791100261,0.0002448543660152,
-3.40911584740964));
#69072=CARTESIAN_POINT('Ctrl Pts',(-0.493182091264478,0.0161839881931373,
-3.40989118236287));
#69073=CARTESIAN_POINT('Ctrl Pts',(-0.492479030563148,0.0321141508308048,
-3.41066651731609));
#69074=CARTESIAN_POINT('Ctrl Pts',(-0.490933795885643,0.0479625955988295,
-3.41144185226931));
#69075=CARTESIAN_POINT('Ctrl Pts',(-0.475090734441219,0.21045434388385,
-3.41939124628873));
#69076=CARTESIAN_POINT('Ctrl Pts',(-0.370717535510866,0.364355831202377,
-3.42734064030814));
#69077=CARTESIAN_POINT('Ctrl Pts',(-0.225430438464366,0.438880232373327,
-3.43529003432755));
#69078=CARTESIAN_POINT('Ctrl Pts',(-0.0901236284872688,0.508285287556358,
-3.44269335621837));
#69079=CARTESIAN_POINT('Ctrl Pts',(0.0806691021356228,0.508844079982147,
-3.45009667810918));
#69080=CARTESIAN_POINT('Ctrl Pts',(0.217494704229605,0.442648936192906,
-3.4575));
#69081=CARTESIAN_POINT('',(-0.21683958723106,0.44219548099168,-3.4575));
#69082=CARTESIAN_POINT('Origin',(0.,0.,-3.4575));
#69083=CARTESIAN_POINT('Ctrl Pts',(-0.216839587231058,0.442195480991681,
-3.4575));
#69084=CARTESIAN_POINT('Ctrl Pts',(-0.290461473000918,0.406093485363624,
-3.45352530299029));
#69085=CARTESIAN_POINT('Ctrl Pts',(-0.354334152100823,0.351257047124773,
-3.44955060598059));
#69086=CARTESIAN_POINT('Ctrl Pts',(-0.401848390604011,0.284326789074269,
-3.44557590897088));
#69087=CARTESIAN_POINT('Ctrl Pts',(-0.449362629107199,0.217396531023764,
-3.44160121196118));
#69088=CARTESIAN_POINT('Ctrl Pts',(-0.480518427013668,0.138372453161606,
-3.43762651495147));
#69089=CARTESIAN_POINT('Ctrl Pts',(-0.489782485247723,0.0570344034865685,
-3.43365181794177));
#69090=CARTESIAN_POINT('Ctrl Pts',(-0.491932738287992,0.0381552703696876,
-3.43272926282463));
#69091=CARTESIAN_POINT('Ctrl Pts',(-0.492903602897926,0.019151475091413,
-3.4318067077075));
#69092=CARTESIAN_POINT('Ctrl Pts',(-0.492742936816498,0.00014446300365779,
-3.43088415259036));
#69093=CARTESIAN_POINT('Origin',(0.,0.,-1.725));
#69094=CARTESIAN_POINT('',(-0.491853744940756,0.000283605033675694,-3.25911584740964));
#69095=CARTESIAN_POINT('',(-0.491800415587683,0.00023852271259368,-3.28088415259036));
#69096=CARTESIAN_POINT('',(-0.4925,-6.03138548580071E-17,-1.725));
#69097=CARTESIAN_POINT('Ctrl Pts',(-0.491853744940756,0.000283605033675694,
-3.25911584740964));
#69098=CARTESIAN_POINT('Ctrl Pts',(-0.492187195010901,0.0639943662937747,
-3.2621948182464));
#69099=CARTESIAN_POINT('Ctrl Pts',(-0.480703508315908,0.127589580024711,
-3.26527378908315));
#69100=CARTESIAN_POINT('Ctrl Pts',(-0.456846036553436,0.186143136808157,
-3.26835275991991));
#69101=CARTESIAN_POINT('Ctrl Pts',(-0.395249985989105,0.337318746707772,
-3.27630215393932));
#69102=CARTESIAN_POINT('Ctrl Pts',(-0.251171881922387,0.454887322396288,
-3.28425154795873));
#69103=CARTESIAN_POINT('Ctrl Pts',(-0.0907115246557711,0.4849032574776,
-3.29220094197814));
#69104=CARTESIAN_POINT('Ctrl Pts',(0.0697488326108451,0.514919192558913,
-3.30015033599755));
#69105=CARTESIAN_POINT('Ctrl Pts',(0.246591443077359,0.457382487033021,
-3.30809973001697));
#69106=CARTESIAN_POINT('Ctrl Pts',(0.358668040949174,0.338698380513017,
-3.31604912403638));
#69107=CARTESIAN_POINT('Ctrl Pts',(0.470744638820989,0.220014273993013,
-3.32399851805579));
#69108=CARTESIAN_POINT('Ctrl Pts',(0.518055224098106,0.0401827664788985,
-3.3319479120752));
#69109=CARTESIAN_POINT('Ctrl Pts',(0.478912723457106,-0.118299377058885,
-3.33989730609461));
#69110=CARTESIAN_POINT('Ctrl Pts',(0.439770222816105,-0.276781520596668,
-3.34784670011402));
#69111=CARTESIAN_POINT('Ctrl Pts',(0.314174636256986,-0.41391430015812,
-3.35579609413343));
#69112=CARTESIAN_POINT('Ctrl Pts',(0.159713217153272,-0.46675503851712,
-3.36374548815285));
#69113=CARTESIAN_POINT('Ctrl Pts',(0.00525179804955778,-0.519595776876121,
-3.37169488217226));
#69114=CARTESIAN_POINT('Ctrl Pts',(-0.178075453598752,-0.488144474032672,
-3.37964427619167));
#69115=CARTESIAN_POINT('Ctrl Pts',(-0.306082617443658,-0.386877817985189,
-3.38759367021108));
#69116=CARTESIAN_POINT('Ctrl Pts',(-0.421604750586888,-0.295488088133343,
-3.39476772927727));
#69117=CARTESIAN_POINT('Ctrl Pts',(-0.49207170577992,-0.147237581533594,
-3.40194178834345));
#69118=CARTESIAN_POINT('Ctrl Pts',(-0.493073791100261,0.0002448543660152,
-3.40911584740964));
#69119=CARTESIAN_POINT('Ctrl Pts',(-0.492742936816498,0.00014446300365779,
-3.43088415259036));
#69120=CARTESIAN_POINT('Ctrl Pts',(-0.491519189150602,-0.144626520836325,
-3.42385731368808));
#69121=CARTESIAN_POINT('Ctrl Pts',(-0.424650436153211,-0.289584125752622,
-3.41683047478581));
#69122=CARTESIAN_POINT('Ctrl Pts',(-0.313283991213996,-0.3810642428305,
-3.40980363588353));
#69123=CARTESIAN_POINT('Ctrl Pts',(-0.187296222933706,-0.484554803195898,
-3.40185424186412));
#69124=CARTESIAN_POINT('Ctrl Pts',(-0.0043595285946734,-0.5196039373251,
-3.39390484784471));
#69125=CARTESIAN_POINT('Ctrl Pts',(0.151107539993508,-0.469682036256402,
-3.3859554538253));
#69126=CARTESIAN_POINT('Ctrl Pts',(0.30657460858169,-0.419760135187704,
-3.37800605980589));
#69127=CARTESIAN_POINT('Ctrl Pts',(0.43457205141902,-0.284867198921108,
-3.37005666578647));
#69128=CARTESIAN_POINT('Ctrl Pts',(0.47661233007598,-0.12711047662137,-3.36210727176706));
#69129=CARTESIAN_POINT('Ctrl Pts',(0.518652608732941,0.0306462456783684,
-3.35415787774765));
#69130=CARTESIAN_POINT('Ctrl Pts',(0.474735723209532,0.211266754011248,
-3.34620848372824));
#69131=CARTESIAN_POINT('Ctrl Pts',(0.364887977701248,0.331990579512092,
-3.33825908970883));
#69132=CARTESIAN_POINT('Ctrl Pts',(0.255040232192964,0.452714405012937,
-3.33030969568942));
#69133=CARTESIAN_POINT('Ctrl Pts',(0.0792616266998056,0.513541547681747,
-3.32236030167));
#69134=CARTESIAN_POINT('Ctrl Pts',(-0.0817338726622884,0.48650604301746,
-3.31441090765059));
#69135=CARTESIAN_POINT('Ctrl Pts',(-0.242729372024383,0.459470538353173,
-3.30646151363118));
#69136=CARTESIAN_POINT('Ctrl Pts',(-0.388941765255412,0.344572386355788,
-3.29851211961177));
#69137=CARTESIAN_POINT('Ctrl Pts',(-0.453320072358766,0.194558532483742,
-3.29056272559236));
#69138=CARTESIAN_POINT('Ctrl Pts',(-0.479447436848157,0.13367674147484,
-3.28733653459169));
#69139=CARTESIAN_POINT('Ctrl Pts',(-0.492096153073964,0.0670111479394572,
-3.28411034359102));
#69140=CARTESIAN_POINT('Ctrl Pts',(-0.491800415587683,0.00023852271259368,
-3.28088415259036));
#69141=CARTESIAN_POINT('Origin',(0.,0.,-1.725));
#69142=CARTESIAN_POINT('',(-0.492081943586782,-0.000397447809200757,-3.10911584740964));
#69143=CARTESIAN_POINT('',(-0.492160810488226,-0.000419635530953083,-3.13088415259036));
#69144=CARTESIAN_POINT('',(-0.4925,-6.03138548580071E-17,-1.725));
#69145=CARTESIAN_POINT('Ctrl Pts',(-0.492081943586782,-0.000397447809200757,
-3.10911584740964));
#69146=CARTESIAN_POINT('Ctrl Pts',(-0.491241598635805,0.110851625858574,
-3.11449845412993));
#69147=CARTESIAN_POINT('Ctrl Pts',(-0.453894375407504,0.222611533621158,
-3.11988106085021));
#69148=CARTESIAN_POINT('Ctrl Pts',(-0.38470206106664,0.308808692434093,
-3.1252636675705));
#69149=CARTESIAN_POINT('Ctrl Pts',(-0.282514218187923,0.436110428259485,
-3.13321306158991));
#69150=CARTESIAN_POINT('Ctrl Pts',(-0.110867900179577,0.507656331705935,
-3.14116245560932));
#69151=CARTESIAN_POINT('Ctrl Pts',(0.0514831441757647,0.490620021386414,
-3.14911184962873));
#69152=CARTESIAN_POINT('Ctrl Pts',(0.213834188531107,0.473583711066893,
-3.15706124364815));
#69153=CARTESIAN_POINT('Ctrl Pts',(0.366889959233445,0.3679651869814,-3.16501063766755));
#69154=CARTESIAN_POINT('Ctrl Pts',(0.44042601136825,0.222223912935534,-3.17296003168697));
#69155=CARTESIAN_POINT('Ctrl Pts',(0.513962063503055,0.0764826388896689,
-3.18090942570638));
#69156=CARTESIAN_POINT('Ctrl Pts',(0.507978397070326,-0.109381385116569,
-3.18885881972579));
#69157=CARTESIAN_POINT('Ctrl Pts',(0.425220800855701,-0.250091262149485,
-3.1968082137452));
#69158=CARTESIAN_POINT('Ctrl Pts',(0.342463204641076,-0.390801139182402,
-3.20475760776462));
#69159=CARTESIAN_POINT('Ctrl Pts',(0.182931678644556,-0.486356869241995,
-3.21270700178403));
#69160=CARTESIAN_POINT('Ctrl Pts',(0.0198208766646809,-0.492915594607009,
-3.22065639580344));
#69161=CARTESIAN_POINT('Ctrl Pts',(-0.143289925315194,-0.499474319972023,
-3.22860578982285));
#69162=CARTESIAN_POINT('Ctrl Pts',(-0.309980003278424,-0.417036040642455,
-3.23655518384226));
#69163=CARTESIAN_POINT('Ctrl Pts',(-0.403768043729067,-0.283425578922314,
-3.24450457786167));
#69164=CARTESIAN_POINT('Ctrl Pts',(-0.461229964141025,-0.201565315282324,
-3.24937500104433));
#69165=CARTESIAN_POINT('Ctrl Pts',(-0.491326282019541,-0.100496293535574,
-3.25424542422699));
#69166=CARTESIAN_POINT('Ctrl Pts',(-0.491853744940756,0.000283605033675694,
-3.25911584740964));
#69167=CARTESIAN_POINT('Ctrl Pts',(-0.491800415587683,0.00023852271259368,
-3.28088415259036));
#69168=CARTESIAN_POINT('Ctrl Pts',(-0.491367450463277,-0.0975178298951643,
-3.27616094957161));
#69169=CARTESIAN_POINT('Ctrl Pts',(-0.463189991711903,-0.195503588868632,
-3.27143774655287));
#69170=CARTESIAN_POINT('Ctrl Pts',(-0.40894429040333,-0.27590559389322,
-3.26671454353412));
#69171=CARTESIAN_POINT('Ctrl Pts',(-0.317645980368864,-0.411226310651424,
-3.25876514951471));
#69172=CARTESIAN_POINT('Ctrl Pts',(-0.152505139324254,-0.496738188421124,
-3.2508157554953));
#69173=CARTESIAN_POINT('Ctrl Pts',(0.0107001108864536,-0.493198978205245,
-3.24286636147589));
#69174=CARTESIAN_POINT('Ctrl Pts',(0.17390536109716,-0.489659767989366,
-3.23491696745648));
#69175=CARTESIAN_POINT('Ctrl Pts',(0.335175020473964,-0.397069469787909,
-3.22696757343707));
#69176=CARTESIAN_POINT('Ctrl Pts',(0.4205209257937,-0.257914117387704,-3.21901817941765));
#69177=CARTESIAN_POINT('Ctrl Pts',(0.505866831113436,-0.118758764987498,
-3.21106878539824));
#69178=CARTESIAN_POINT('Ctrl Pts',(0.515288982376103,0.0669616416114556,
-3.20311939137883));
#69179=CARTESIAN_POINT('Ctrl Pts',(0.444461893468698,0.2140380586944,-3.19516999735942));
#69180=CARTESIAN_POINT('Ctrl Pts',(0.373634804561292,0.361114475777343,
-3.18722060334001));
#69181=CARTESIAN_POINT('Ctrl Pts',(0.222558475483815,0.469546903344277,
-3.1792712093206));
#69182=CARTESIAN_POINT('Ctrl Pts',(0.0605502329573067,0.489583796109161,
-3.17132181530119));
#69183=CARTESIAN_POINT('Ctrl Pts',(-0.101458009569203,0.509620688874046,
-3.16337242128177));
#69184=CARTESIAN_POINT('Ctrl Pts',(-0.274398165544743,0.441262046836879,
-3.15542302726236));
#69185=CARTESIAN_POINT('Ctrl Pts',(-0.378923416489071,0.315872421142784,
-3.14747363324295));
#69186=CARTESIAN_POINT('Ctrl Pts',(-0.451634184295762,0.228647794778889,
-3.14194380635875));
#69187=CARTESIAN_POINT('Ctrl Pts',(-0.491239025177775,0.113825913452389,
-3.13641397947456));
#69188=CARTESIAN_POINT('Ctrl Pts',(-0.492160810488226,-0.000419635530953083,
-3.13088415259036));
#69189=CARTESIAN_POINT('Origin',(0.,0.,-1.725));
#69190=CARTESIAN_POINT('',(-0.493288832552248,-0.000100558029926257,-2.95911584740964));
#69191=CARTESIAN_POINT('',(-0.493308766107567,-4.46620548418582E-5,-2.98088415259036));
#69192=CARTESIAN_POINT('',(-0.4925,-6.03138548580071E-17,-1.725));
#69193=CARTESIAN_POINT('Ctrl Pts',(-0.493288832552248,-0.000100558029926257,
-2.95911584740964));
#69194=CARTESIAN_POINT('Ctrl Pts',(-0.492849426102292,0.15775946830591,
-2.96680209001346));
#69195=CARTESIAN_POINT('Ctrl Pts',(-0.410373732182605,0.316014099494504,
-2.97448833261728));
#69196=CARTESIAN_POINT('Ctrl Pts',(-0.280543525334876,0.405775594702927,
-2.98217457522109));
#69197=CARTESIAN_POINT('Ctrl Pts',(-0.146268363457757,0.498610225349239,
-2.9901239692405));
#69198=CARTESIAN_POINT('Ctrl Pts',(0.0386593403997117,0.518181480847482,
-2.99807336325992));
#69199=CARTESIAN_POINT('Ctrl Pts',(0.18939203724908,0.455509779881214,-3.00602275727933));
#69200=CARTESIAN_POINT('Ctrl Pts',(0.34012473409845,0.392838078914945,-3.01397215129874));
#69201=CARTESIAN_POINT('Ctrl Pts',(0.45666242393972,0.247923421484165,-3.02192154531815));
#69202=CARTESIAN_POINT('Ctrl Pts',(0.485535896090777,0.0872547869843185,
-3.02987093933756));
#69203=CARTESIAN_POINT('Ctrl Pts',(0.514409368241833,-0.0734138475155269,
-3.03782033335697));
#69204=CARTESIAN_POINT('Ctrl Pts',(0.455618622702678,-0.249836459084439,
-3.04576972737638));
#69205=CARTESIAN_POINT('Ctrl Pts',(0.336137726335389,-0.361067763092586,
-3.0537191213958));
#69206=CARTESIAN_POINT('Ctrl Pts',(0.216656829968098,-0.472299067100733,
-3.06166851541521));
#69207=CARTESIAN_POINT('Ctrl Pts',(0.0364857827726722,-0.518339063548116,
-3.06961790943462));
#69208=CARTESIAN_POINT('Ctrl Pts',(-0.121710303328504,-0.47806391507255,
-3.07756730345403));
#69209=CARTESIAN_POINT('Ctrl Pts',(-0.279906389429679,-0.437788766596985,
-3.08551669747344));
#69210=CARTESIAN_POINT('Ctrl Pts',(-0.416127514436606,-0.311198473198473,
-3.09346609149285));
#69211=CARTESIAN_POINT('Ctrl Pts',(-0.467873393065525,-0.156374542397051,
-3.10141548551226));
#69212=CARTESIAN_POINT('Ctrl Pts',(-0.484581668403554,-0.106383298006425,
-3.10398227281139));
#69213=CARTESIAN_POINT('Ctrl Pts',(-0.49248267632821,-0.0534484552799383,
-3.10654906011052));
#69214=CARTESIAN_POINT('Ctrl Pts',(-0.492081943586782,-0.000397447809200757,
-3.10911584740964));
#69215=CARTESIAN_POINT('Ctrl Pts',(-0.492160810488226,-0.000419635530953083,
-3.13088415259036));
#69216=CARTESIAN_POINT('Ctrl Pts',(-0.492564136214256,-0.0504075974425025,
-3.12846458545514));
#69217=CARTESIAN_POINT('Ctrl Pts',(-0.485561643610284,-0.100285221311515,
-3.12604501831993));
#69218=CARTESIAN_POINT('Ctrl Pts',(-0.47068614746544,-0.147692460569256,
-3.12362545118472));
#69219=CARTESIAN_POINT('Ctrl Pts',(-0.421813281584368,-0.303447107236178,
-3.1156760571653));
#69220=CARTESIAN_POINT('Ctrl Pts',(-0.287957203909111,-0.432535791218999,
-3.10772666314589));
#69221=CARTESIAN_POINT('Ctrl Pts',(-0.130533233909336,-0.475730562101413,
-3.09977726912648));
#69222=CARTESIAN_POINT('Ctrl Pts',(0.0268907360904382,-0.518925332983827,
-3.09182787510707));
#69223=CARTESIAN_POINT('Ctrl Pts',(0.207882598414731,-0.476226190765834,
-3.08387848108766));
#69224=CARTESIAN_POINT('Ctrl Pts',(0.329400718662921,-0.367224215067139,
-3.07592908706825));
#69225=CARTESIAN_POINT('Ctrl Pts',(0.450918838911112,-0.258222239368444,
-3.06797969304883));
#69226=CARTESIAN_POINT('Ctrl Pts',(0.512963217083201,-0.082917430189047,
-3.06003029902942));
#69227=CARTESIAN_POINT('Ctrl Pts',(0.487066930325681,0.0782578312794736,
-3.05208090501001));
#69228=CARTESIAN_POINT('Ctrl Pts',(0.461170643568161,0.239433092747993,
-3.0441315109906));
#69229=CARTESIAN_POINT('Ctrl Pts',(0.347333691881035,0.386478806505637,
-3.03618211697119));
#69230=CARTESIAN_POINT('Ctrl Pts',(0.197786169162767,0.451928212703762,
-3.02823272295178));
#69231=CARTESIAN_POINT('Ctrl Pts',(0.0482386464444978,0.517377618901888,
-3.02028332893236));
#69232=CARTESIAN_POINT('Ctrl Pts',(-0.137019447304913,0.501230717540495,
-3.01233393491295));
#69233=CARTESIAN_POINT('Ctrl Pts',(-0.272988986618268,0.410895956542165,
-3.00438454089354));
#69234=CARTESIAN_POINT('Ctrl Pts',(-0.406975592535066,0.321878606894628,
-2.99655107812582));
#69235=CARTESIAN_POINT('Ctrl Pts',(-0.493100776114359,0.160821480000113,
-2.98871761535809));
#69236=CARTESIAN_POINT('Ctrl Pts',(-0.493308766107567,-4.46620548418582E-5,
-2.98088415259036));
#69237=CARTESIAN_POINT('Origin',(0.,0.,-1.725));
#69238=CARTESIAN_POINT('',(-0.49238332947362,0.000451585811006003,-2.80911584740964));
#69239=CARTESIAN_POINT('',(-0.492294212910438,0.000443650235898252,-2.83088415259036));
#69240=CARTESIAN_POINT('',(-0.4925,-6.03138548580071E-17,-1.725));
#69241=CARTESIAN_POINT('Ctrl Pts',(-0.49238332947362,0.000451585811006003,
-2.80911584740964));
#69242=CARTESIAN_POINT('Ctrl Pts',(-0.492762312673717,0.0425594796056222,
-2.81115633187758));
#69243=CARTESIAN_POINT('Ctrl Pts',(-0.487812004432201,0.0845796032291862,
-2.81319681634551));
#69244=CARTESIAN_POINT('Ctrl Pts',(-0.477185120477568,0.125111406407132,
-2.81523730081345));
#69245=CARTESIAN_POINT('Ctrl Pts',(-0.435784517296601,0.283016687648826,
-2.82318669483286));
#69246=CARTESIAN_POINT('Ctrl Pts',(-0.30822744433155,0.418332921904744,
-2.83113608885227));
#69247=CARTESIAN_POINT('Ctrl Pts',(-0.153038963263602,0.468975030179542,
-2.83908548287168));
#69248=CARTESIAN_POINT('Ctrl Pts',(0.00214951780434441,0.519617138454339,
-2.84703487689109));
#69249=CARTESIAN_POINT('Ctrl Pts',(0.184969406975187,0.485585120748017,
-2.85498427091051));
#69250=CARTESIAN_POINT('Ctrl Pts',(0.311540249547337,0.382493367425997,
-2.86293366492992));
#69251=CARTESIAN_POINT('Ctrl Pts',(0.438111092119489,0.279401614103976,
-2.87088305894933));
#69252=CARTESIAN_POINT('Ctrl Pts',(0.508432888092948,0.107250125166256,
-2.87883245296874));
#69253=CARTESIAN_POINT('Ctrl Pts',(0.490240962838993,-0.0549754635675121,
-2.88678184698815));
#69254=CARTESIAN_POINT('Ctrl Pts',(0.472049037585039,-0.217201052301277,
-2.89473124100757));
#69255=CARTESIAN_POINT('Ctrl Pts',(0.365343391103676,-0.369500740831089,
-2.90268063502698));
#69256=CARTESIAN_POINT('Ctrl Pts',(0.219082143980931,-0.441997191571637,
-2.91063002904639));
#69257=CARTESIAN_POINT('Ctrl Pts',(0.0728208968581848,-0.514493642312186,
-2.9185794230658));
#69258=CARTESIAN_POINT('Ctrl Pts',(-0.112995950905944,-0.507186855263467,
-2.92652881708521));
#69259=CARTESIAN_POINT('Ctrl Pts',(-0.253112896177252,-0.423429291625341,
-2.93447821110462));
#69260=CARTESIAN_POINT('Ctrl Pts',(-0.39322984144856,-0.339671727987215,
-2.94242760512403));
#69261=CARTESIAN_POINT('Ctrl Pts',(-0.487646884227047,-0.179463387759685,
-2.95037699914345));
#69262=CARTESIAN_POINT('Ctrl Pts',(-0.493044095667907,-0.0163102147487279,
-2.95832639316286));
#69263=CARTESIAN_POINT('Ctrl Pts',(-0.493222761340719,-0.0109093013795094,
-2.95858954457845));
#69264=CARTESIAN_POINT('Ctrl Pts',(-0.493303876369531,-0.00550516097278517,
-2.95885269599405));
#69265=CARTESIAN_POINT('Ctrl Pts',(-0.493288832552248,-0.000100558029926257,
-2.95911584740964));
#69266=CARTESIAN_POINT('Ctrl Pts',(-0.493308766107567,-4.46620548418582E-5,
-2.98088415259036));
#69267=CARTESIAN_POINT('Ctrl Pts',(-0.493311844253333,-0.00242539887009011,
-2.98076822133867));
#69268=CARTESIAN_POINT('Ctrl Pts',(-0.493296104394717,-0.00480609385490379,
-2.98065229008699));
#69269=CARTESIAN_POINT('Ctrl Pts',(-0.493261423175586,-0.0071865128763955,
-2.98053635883531));
#69270=CARTESIAN_POINT('Ctrl Pts',(-0.490883335542247,-0.170411600661355,
-2.97258696481589));
#69271=CARTESIAN_POINT('Ctrl Pts',(-0.399446175398269,-0.332339155596008,
-2.96463757079648));
#69272=CARTESIAN_POINT('Ctrl Pts',(-0.26090266065602,-0.418674429978304,
-2.95668817677707));
#69273=CARTESIAN_POINT('Ctrl Pts',(-0.12235914591377,-0.505009704360601,
-2.94873878275766));
#69274=CARTESIAN_POINT('Ctrl Pts',(0.0632907234267497,-0.515752698190541,
-2.94078938873825));
#69275=CARTESIAN_POINT('Ctrl Pts',(0.210868057983077,-0.445974369553748,
-2.93283999471884));
#69276=CARTESIAN_POINT('Ctrl Pts',(0.358445392539404,-0.376196040916956,
-2.92489060069943));
#69277=CARTESIAN_POINT('Ctrl Pts',(0.467950192311538,-0.225896389813431,
-2.91694120668002));
#69278=CARTESIAN_POINT('Ctrl Pts',(0.489140043172359,-0.064035106446827,
-2.9089918126606));
#69279=CARTESIAN_POINT('Ctrl Pts',(0.51032989403318,0.0978261769197771,
-2.90104241864119));
#69280=CARTESIAN_POINT('Ctrl Pts',(0.443204795982688,0.27124909254946,-2.89309302462178));
#69281=CARTESIAN_POINT('Ctrl Pts',(0.318562732046716,0.376664654941548,
-2.88514363060237));
#69282=CARTESIAN_POINT('Ctrl Pts',(0.193920668110745,0.482080217333636,
-2.87719423658296));
#69283=CARTESIAN_POINT('Ctrl Pts',(0.0117616382892947,0.51948842648813,
-2.86924484256355));
#69284=CARTESIAN_POINT('Ctrl Pts',(-0.14433711493361,0.471725845947257,
-2.86129544854414));
#69285=CARTESIAN_POINT('Ctrl Pts',(-0.300435868156515,0.423963265406384,
-2.85334605452472));
#69286=CARTESIAN_POINT('Ctrl Pts',(-0.430474344780874,0.291029895170145,
-2.84539666050531));
#69287=CARTESIAN_POINT('Ctrl Pts',(-0.474788978503301,0.133917521054328,
-2.8374472664859));
#69288=CARTESIAN_POINT('Ctrl Pts',(-0.486984540733128,0.0906795751512453,
-2.83525956185405));
#69289=CARTESIAN_POINT('Ctrl Pts',(-0.492687617934248,0.0456103788587369,
-2.8330718572222));
#69290=CARTESIAN_POINT('Ctrl Pts',(-0.492294212910438,0.000443650235898252,
-2.83088415259036));
#69291=CARTESIAN_POINT('Origin',(0.,0.,-1.725));
#69292=CARTESIAN_POINT('',(-0.491717171688544,-0.000124746059964487,-2.65911584740964));
#69293=CARTESIAN_POINT('',(-0.491744581231444,-0.000172364191907249,-2.68088415259036));
#69294=CARTESIAN_POINT('',(-0.4925,-6.03138548580071E-17,-1.725));
#69295=CARTESIAN_POINT('Ctrl Pts',(-0.491717171688544,-0.000124746059964487,
-2.65911584740964));
#69296=CARTESIAN_POINT('Ctrl Pts',(-0.491513805740775,0.0898277571935297,
-2.66345996776111));
#69297=CARTESIAN_POINT('Ctrl Pts',(-0.467931427741527,0.179879518565837,
-2.66780408811258));
#69298=CARTESIAN_POINT('Ctrl Pts',(-0.42161619699015,0.256121622769783,
-2.67214820846404));
#69299=CARTESIAN_POINT('Ctrl Pts',(-0.336863016011095,0.395638597013269,
-2.68009760248345));
#69300=CARTESIAN_POINT('Ctrl Pts',(-0.175986415474485,0.48891243855205,
-2.68804699650286));
#69301=CARTESIAN_POINT('Ctrl Pts',(-0.0127989464766061,0.493147736670856,
-2.69599639052228));
#69302=CARTESIAN_POINT('Ctrl Pts',(0.150388522521273,0.497383034789663,
-2.70394578454169));
#69303=CARTESIAN_POINT('Ctrl Pts',(0.315886859980421,0.412579789488495,
-2.7118951785611));
#69304=CARTESIAN_POINT('Ctrl Pts',(0.40776299391215,0.277646977311601,-2.71984457258051));
#69305=CARTESIAN_POINT('Ctrl Pts',(0.499639127843881,0.142714165134706,
-2.72779396659992));
#69306=CARTESIAN_POINT('Ctrl Pts',(0.517893058248192,-0.042348213917915,
-2.73574336061933));
#69307=CARTESIAN_POINT('Ctrl Pts',(0.454149613307436,-0.192630817752104,
-2.74369275463874));
#69308=CARTESIAN_POINT('Ctrl Pts',(0.39040616836668,-0.342913421586293,
-2.75164214865816));
#69309=CARTESIAN_POINT('Ctrl Pts',(0.244665348080859,-0.45841625020205,
-2.75959154267757));
#69310=CARTESIAN_POINT('Ctrl Pts',(0.0837951848967256,-0.486144906588543,
-2.76754093669698));
#69311=CARTESIAN_POINT('Ctrl Pts',(-0.077074978287408,-0.513873562975036,
-2.77549033071639));
#69312=CARTESIAN_POINT('Ctrl Pts',(-0.253074484369854,-0.453828047132267,
-2.7834397247358));
#69313=CARTESIAN_POINT('Ctrl Pts',(-0.363452170712636,-0.333558125097149,
-2.79138911875521));
#69314=CARTESIAN_POINT('Ctrl Pts',(-0.445497640280255,-0.244159601218073,
-2.79729802830669));
#69315=CARTESIAN_POINT('Ctrl Pts',(-0.491285856061745,-0.121485993104857,
-2.80320693785816));
#69316=CARTESIAN_POINT('Ctrl Pts',(-0.49238332947362,0.000451585811006003,
-2.80911584740964));
#69317=CARTESIAN_POINT('Ctrl Pts',(-0.492294212910438,0.000443650235898252,
-2.83088415259036));
#69318=CARTESIAN_POINT('Ctrl Pts',(-0.491258114381547,-0.11851055280821,
-2.82512246320279));
#69319=CARTESIAN_POINT('Ctrl Pts',(-0.447935527320371,-0.23814126069821,
-2.81936077381523));
#69320=CARTESIAN_POINT('Ctrl Pts',(-0.369560505409501,-0.326777461536222,
-2.81359908442767));
#69321=CARTESIAN_POINT('Ctrl Pts',(-0.26142660777278,-0.449068692015562,
-2.80564969040825));
#69322=CARTESIAN_POINT('Ctrl Pts',(-0.0865680216788435,-0.512359774978848,
-2.79770029638884));
#69323=CARTESIAN_POINT('Ctrl Pts',(0.0747875611418878,-0.487611830476674,
-2.78975090236943));
#69324=CARTESIAN_POINT('Ctrl Pts',(0.236143143962619,-0.462863885974499,
-2.78180150835002));
#69325=CARTESIAN_POINT('Ctrl Pts',(0.383995723510146,-0.350076914006863,
-2.77385211433061));
#69326=CARTESIAN_POINT('Ctrl Pts',(0.450508361104208,-0.200999236583791,
-2.7659027203112));
#69327=CARTESIAN_POINT('Ctrl Pts',(0.517020998698271,-0.0519215591607172,
-2.75795332629178));
#69328=CARTESIAN_POINT('Ctrl Pts',(0.502193694338868,0.133446823717793,
-2.75000393227237));
#69329=CARTESIAN_POINT('Ctrl Pts',(0.412829433411397,0.270056170892213,
-2.74205453825296));
#69330=CARTESIAN_POINT('Ctrl Pts',(0.323465172483926,0.406665518066632,
-2.73410514423355));
#69331=CARTESIAN_POINT('Ctrl Pts',(0.159563954988387,0.494515829536961,
-2.72615575021414));
#69332=CARTESIAN_POINT('Ctrl Pts',(-0.0036739292267207,0.493300089977269,
-2.71820635619472));
#69333=CARTESIAN_POINT('Ctrl Pts',(-0.166911813441828,0.492084350417578,
-2.71025696217531));
#69334=CARTESIAN_POINT('Ctrl Pts',(-0.329486364376504,0.401802559827868,
-2.7023075681559));
#69335=CARTESIAN_POINT('Ctrl Pts',(-0.416805986309723,0.263877331927563,
-2.69435817413649));
#69336=CARTESIAN_POINT('Ctrl Pts',(-0.46614083558483,0.185950742473243,
-2.68986683362112));
#69337=CARTESIAN_POINT('Ctrl Pts',(-0.491453148001298,0.0928156312110853,
-2.68537549310574));
#69338=CARTESIAN_POINT('Ctrl Pts',(-0.491744581231444,-0.000172364191907249,
-2.68088415259036));
#69339=CARTESIAN_POINT('Origin',(0.,0.,-1.725));
#69340=CARTESIAN_POINT('',(-0.492842183013278,-0.000400497545981371,-2.50911584740964));
#69341=CARTESIAN_POINT('',(-0.492927675364674,-0.00037237350921324,-2.53088415259036));
#69342=CARTESIAN_POINT('',(-0.4925,-6.03138548580071E-17,-1.725));
#69343=CARTESIAN_POINT('Ctrl Pts',(-0.492842183013278,-0.000400497545981371,
-2.50911584740964));
#69344=CARTESIAN_POINT('Ctrl Pts',(-0.491635912823679,0.136456377594769,
-2.51576360364464));
#69345=CARTESIAN_POINT('Ctrl Pts',(-0.432193201139404,0.27423228448661,
-2.52241135987964));
#69346=CARTESIAN_POINT('Ctrl Pts',(-0.330961608144812,0.365818147648235,
-2.52905911611463));
#69347=CARTESIAN_POINT('Ctrl Pts',(-0.209908760916426,0.475336620820701,
-2.53700851013405));
#69348=CARTESIAN_POINT('Ctrl Pts',(-0.0291003124230802,0.518806093660808,
-2.54495790415346));
#69349=CARTESIAN_POINT('Ctrl Pts',(0.128506161165294,0.476282132519312,
-2.55290729817287));
#69350=CARTESIAN_POINT('Ctrl Pts',(0.286112634753665,0.433758171377816,
-2.56085669219228));
#69351=CARTESIAN_POINT('Ctrl Pts',(0.420517133437062,0.305240776254718,
-2.56880608621169));
#69352=CARTESIAN_POINT('Ctrl Pts',(0.470052895899761,0.149695618742931,
-2.5767554802311));
#69353=CARTESIAN_POINT('Ctrl Pts',(0.519588658362461,-0.00584953876885633,
-2.58470487425051));
#69354=CARTESIAN_POINT('Ctrl Pts',(0.484255684604462,-0.188422458669333,
-2.59265426826992));
#69355=CARTESIAN_POINT('Ctrl Pts',(0.380265262794311,-0.314255999348571,
-2.60060366228934));
#69356=CARTESIAN_POINT('Ctrl Pts',(0.276274840984159,-0.44008954002781,
-2.60855305630875));
#69357=CARTESIAN_POINT('Ctrl Pts',(0.103626971121853,-0.509183701485811,
-2.61650245032816));
#69358=CARTESIAN_POINT('Ctrl Pts',(-0.0584649641545909,-0.489837065952524,
-2.62445184434757));
#69359=CARTESIAN_POINT('Ctrl Pts',(-0.220556899431035,-0.470490430419237,
-2.63240123836698));
#69360=CARTESIAN_POINT('Ctrl Pts',(-0.372092900121619,-0.362702997894662,
-2.64035063238639));
#69361=CARTESIAN_POINT('Ctrl Pts',(-0.443546019756161,-0.215929228158279,
-2.64830002640581));
#69362=CARTESIAN_POINT('Ctrl Pts',(-0.47595201826144,-0.149363197353488,
-2.65190530007375));
#69363=CARTESIAN_POINT('Ctrl Pts',(-0.49188594921705,-0.0747781546000925,
-2.6555105737417));
#69364=CARTESIAN_POINT('Ctrl Pts',(-0.491717171688544,-0.000124746059964487,
-2.65911584740964));
#69365=CARTESIAN_POINT('Ctrl Pts',(-0.491744581231444,-0.000172364191907249,
-2.68088415259036));
#69366=CARTESIAN_POINT('Ctrl Pts',(-0.491968966734891,-0.0717673506409361,
-2.67742609908633));
#69367=CARTESIAN_POINT('Ctrl Pts',(-0.477360863836571,-0.143275126154708,
-2.67396804558229));
#69368=CARTESIAN_POINT('Ctrl Pts',(-0.447464606497128,-0.207687030072964,
-2.67050999207826));
#69369=CARTESIAN_POINT('Ctrl Pts',(-0.378738911819555,-0.355757498962288,
-2.66256059805885));
#69370=CARTESIAN_POINT('Ctrl Pts',(-0.229222829532647,-0.466329771530036,
-2.65461120403943));
#69371=CARTESIAN_POINT('Ctrl Pts',(-0.0675165378258877,-0.488671662415771,
-2.64666181002002));
#69372=CARTESIAN_POINT('Ctrl Pts',(0.0941897538808718,-0.511013553301507,
-2.63871241600061));
#69373=CARTESIAN_POINT('Ctrl Pts',(0.268086255007482,-0.44512506250523,
-2.6307630219812));
#69374=CARTESIAN_POINT('Ctrl Pts',(0.374386692522034,-0.321236798936182,
-2.62281362796179));
#69375=CARTESIAN_POINT('Ctrl Pts',(0.480687130036584,-0.197348535367138,
-2.61486423394238));
#69376=CARTESIAN_POINT('Ctrl Pts',(0.519391503939077,-0.0154604990253233,
-2.60691483992296));
#69377=CARTESIAN_POINT('Ctrl Pts',(0.472741678075792,0.140974403131689,
-2.59896544590355));
#69378=CARTESIAN_POINT('Ctrl Pts',(0.426091852212506,0.297409305288705,
-2.59101605188414));
#69379=CARTESIAN_POINT('Ctrl Pts',(0.29408782658344,0.428391073260918,-2.58306665786473));
#69380=CARTESIAN_POINT('Ctrl Pts',(0.137294990151839,0.473823344937194,
-2.57511726384532));
#69381=CARTESIAN_POINT('Ctrl Pts',(-0.0194978462797628,0.519255616613469,
-2.56716786982591));
#69382=CARTESIAN_POINT('Ctrl Pts',(-0.201079493513898,0.479138391993805,
-2.5592184758065));
#69383=CARTESIAN_POINT('Ctrl Pts',(-0.324137620423235,0.371878043926564,
-2.55126908178708));
#69384=CARTESIAN_POINT('Ctrl Pts',(-0.429325143648394,0.280194132942174,
-2.54447410538818));
#69385=CARTESIAN_POINT('Ctrl Pts',(-0.49175260747451,0.139452271736717,
-2.53767912898927));
#69386=CARTESIAN_POINT('Ctrl Pts',(-0.492927675364674,-0.00037237350921324,
-2.53088415259036));
#69387=CARTESIAN_POINT('Origin',(0.,0.,-1.725));
#69388=CARTESIAN_POINT('',(-0.493011002216929,0.000337434886769988,-2.35911584740964));
#69389=CARTESIAN_POINT('',(-0.492930612967012,0.000371277315277309,-2.38088415259036));
#69390=CARTESIAN_POINT('',(-0.4925,-6.03138548580071E-17,-1.725));
#69391=CARTESIAN_POINT('Ctrl Pts',(-0.493011002216929,0.000337434886769988,
-2.35911584740964));
#69392=CARTESIAN_POINT('Ctrl Pts',(-0.493172448397906,0.0209471144955579,
-2.36011784550876));
#69393=CARTESIAN_POINT('Ctrl Pts',(-0.49199234302067,0.0415381637358038,
-2.36111984360787));
#69394=CARTESIAN_POINT('Ctrl Pts',(-0.48940833138991,0.0619515002298427,
-2.36212184170699));
#69395=CARTESIAN_POINT('Ctrl Pts',(-0.468907966547148,0.223901562994389,
-2.3700712357264));
#69396=CARTESIAN_POINT('Ctrl Pts',(-0.360044213363923,0.374666191997443,
-2.37802062974581));
#69397=CARTESIAN_POINT('Ctrl Pts',(-0.212765363372498,0.445072357447139,
-2.38597002376523));
#69398=CARTESIAN_POINT('Ctrl Pts',(-0.0654865133810744,0.515478522896833,
-2.39391941778464));
#69399=CARTESIAN_POINT('Ctrl Pts',(0.120207433418549,0.505526224793171,
-2.40186881180405));
#69400=CARTESIAN_POINT('Ctrl Pts',(0.259117362359501,0.41978172392142,-2.40981820582346));
#69401=CARTESIAN_POINT('Ctrl Pts',(0.398027291300455,0.334037223049669,
-2.41776759984287));
#69402=CARTESIAN_POINT('Ctrl Pts',(0.490153202382736,0.172500519409826,
-2.42571699386228));
#69403=CARTESIAN_POINT('Ctrl Pts',(0.493226372272249,0.00928702911274082,
-2.43366638788169));
#69404=CARTESIAN_POINT('Ctrl Pts',(0.496299542161763,-0.153926461184346,
-2.44161578190111));
#69405=CARTESIAN_POINT('Ctrl Pts',(0.410319970858508,-0.318816738138676,
-2.44956517592052));
#69406=CARTESIAN_POINT('Ctrl Pts',(0.274736350582803,-0.409729716865921,
-2.45751456993993));
#69407=CARTESIAN_POINT('Ctrl Pts',(0.1391527303071,-0.500642695593164,-2.46546396395934));
#69408=CARTESIAN_POINT('Ctrl Pts',(-0.0460349389410497,-0.517578376093326,
-2.47341335797875));
#69409=CARTESIAN_POINT('Ctrl Pts',(-0.195859830083599,-0.452766419000138,
-2.48136275199816));
#69410=CARTESIAN_POINT('Ctrl Pts',(-0.345684721226149,-0.387954461906949,
-2.48931214601758));
#69411=CARTESIAN_POINT('Ctrl Pts',(-0.460146834263098,-0.24139486722041,
-2.49726154003699));
#69412=CARTESIAN_POINT('Ctrl Pts',(-0.48672926779986,-0.0803313331247288,
-2.5052109340564));
#69413=CARTESIAN_POINT('Ctrl Pts',(-0.491081888868664,-0.0539587088519548,
-2.50651257184081));
#69414=CARTESIAN_POINT('Ctrl Pts',(-0.493078372007202,-0.0271972201457358,
-2.50781420962523));
#69415=CARTESIAN_POINT('Ctrl Pts',(-0.492842183013278,-0.000400497545981371,
-2.50911584740964));
#69416=CARTESIAN_POINT('Ctrl Pts',(-0.492927675364674,-0.00037237350921324,
-2.53088415259036));
#69417=CARTESIAN_POINT('Ctrl Pts',(-0.49312731094809,-0.0241275751135129,
-2.52972973496985));
#69418=CARTESIAN_POINT('Ctrl Pts',(-0.491558983946496,-0.0478563025942449,
-2.52857531734935));
#69419=CARTESIAN_POINT('Ctrl Pts',(-0.488132013261578,-0.0713134921138267,
-2.52742089972885));
#69420=CARTESIAN_POINT('Ctrl Pts',(-0.464533672606046,-0.232841208572165,
-2.51947150570944));
#69421=CARTESIAN_POINT('Ctrl Pts',(-0.352802384710446,-0.381493169974031,
-2.51152211169003));
#69422=CARTESIAN_POINT('Ctrl Pts',(-0.204202108219394,-0.449065669503946,
-2.50357271767062));
#69423=CARTESIAN_POINT('Ctrl Pts',(-0.0556018317283395,-0.516638169033863,
-2.49562332365121));
#69424=CARTESIAN_POINT('Ctrl Pts',(0.129867433358168,-0.503131206691828,
-2.48767392963179));
#69425=CARTESIAN_POINT('Ctrl Pts',(0.267109659648677,-0.414741975510851,
-2.47972453561238));
#69426=CARTESIAN_POINT('Ctrl Pts',(0.404351885939185,-0.326352744329874,
-2.47177514159297));
#69427=CARTESIAN_POINT('Ctrl Pts',(0.493367073433696,-0.163081244309955,
-2.46382574757356));
#69428=CARTESIAN_POINT('Ctrl Pts',(0.493313744544244,0.000161158337056044,
-2.45587635355415));
#69429=CARTESIAN_POINT('Ctrl Pts',(0.493260415654792,0.163403560984069,
-2.44792695953474));
#69430=CARTESIAN_POINT('Ctrl Pts',(0.404138570381379,0.326616866258171,
-2.43997756551532));
#69431=CARTESIAN_POINT('Ctrl Pts',(0.266838622470047,0.41491640855305,-2.43202817149591));
#69432=CARTESIAN_POINT('Ctrl Pts',(0.129538674558719,0.503215950847926,
-2.4240787774765));
#69433=CARTESIAN_POINT('Ctrl Pts',(-0.0559393759905273,0.516601730163578,
-2.41612938345709));
#69434=CARTESIAN_POINT('Ctrl Pts',(-0.204495470886693,0.448932154022302,
-2.40817998943768));
#69435=CARTESIAN_POINT('Ctrl Pts',(-0.35305156578286,0.381262577881024,
-2.40023059541827));
#69436=CARTESIAN_POINT('Ctrl Pts',(-0.464685705025947,0.232537646282815,
-2.39228120139885));
#69437=CARTESIAN_POINT('Ctrl Pts',(-0.488178503202315,0.0709945458427664,
-2.38433180737944));
#69438=CARTESIAN_POINT('Ctrl Pts',(-0.491574781289422,0.0476407806578399,
-2.38318258911641));
#69439=CARTESIAN_POINT('Ctrl Pts',(-0.493128944776674,0.0240191214780956,
-2.38203337085339));
#69440=CARTESIAN_POINT('Ctrl Pts',(-0.492930612967012,0.000371277315277309,
-2.38088415259036));
#69441=CARTESIAN_POINT('Origin',(0.,0.,-1.725));
#69442=CARTESIAN_POINT('',(-0.491782200599552,0.000219480096867314,-2.20911584740964));
#69443=CARTESIAN_POINT('',(-0.491745711415915,0.000174011476622056,-2.23088415259036));
#69444=CARTESIAN_POINT('',(-0.4925,-6.03138548580071E-17,-1.725));
#69445=CARTESIAN_POINT('Ctrl Pts',(-0.491782200599552,0.000219480096867314,
-2.20911584740964));
#69446=CARTESIAN_POINT('Ctrl Pts',(-0.492056527069416,0.0686457329269439,
-2.21242148139229));
#69447=CARTESIAN_POINT('Ctrl Pts',(-0.478754286155654,0.136970012424534,
-2.21572711537494));
#69448=CARTESIAN_POINT('Ctrl Pts',(-0.45136026669906,0.199078911138115,
-2.21903274935758));
#69449=CARTESIAN_POINT('Ctrl Pts',(-0.385483083810998,0.348438492561131,
-2.226982143377));
#69450=CARTESIAN_POINT('Ctrl Pts',(-0.238112146179298,0.461854086097113,
-2.23493153739641));
#69451=CARTESIAN_POINT('Ctrl Pts',(-0.0768634080676502,0.487288948894606,
-2.24288093141582));
#69452=CARTESIAN_POINT('Ctrl Pts',(0.0843853300439994,0.5127238116921,-2.25083032543523));
#69453=CARTESIAN_POINT('Ctrl Pts',(0.259511868635597,0.450177943751104,
-2.25877971945464));
#69454=CARTESIAN_POINT('Ctrl Pts',(0.368165575390739,0.32834830943952,-2.26672911347405));
#69455=CARTESIAN_POINT('Ctrl Pts',(0.476819282145881,0.206518675127936,
-2.27467850749347));
#69456=CARTESIAN_POINT('Ctrl Pts',(0.519000157064568,0.025405274445765,
-2.28262790151288));
#69457=CARTESIAN_POINT('Ctrl Pts',(0.475354994181373,-0.131894399886466,
-2.29057729553229));
#69458=CARTESIAN_POINT('Ctrl Pts',(0.431709831298178,-0.289194074218698,
-2.2985266895517));
#69459=CARTESIAN_POINT('Ctrl Pts',(0.302238630613101,-0.42268002220099,
-2.30647608357111));
#69460=CARTESIAN_POINT('Ctrl Pts',(0.146344683743011,-0.471106927092717,
-2.31442547759052));
#69461=CARTESIAN_POINT('Ctrl Pts',(-0.00954926312707591,-0.519533831984444,
-2.32237487160993));
#69462=CARTESIAN_POINT('Ctrl Pts',(-0.191865956182174,-0.482901693785609,
-2.33032426562935));
#69463=CARTESIAN_POINT('Ctrl Pts',(-0.316955814458573,-0.378017876423175,
-2.33827365964876));
#69464=CARTESIAN_POINT('Ctrl Pts',(-0.426278458289986,-0.286354360553994,
-2.34522105556905));
#69465=CARTESIAN_POINT('Ctrl Pts',(-0.491891608337785,-0.142560644619424,
-2.35216845148935));
#69466=CARTESIAN_POINT('Ctrl Pts',(-0.493011002216929,0.000337434886769988,
-2.35911584740964));
#69467=CARTESIAN_POINT('Ctrl Pts',(-0.492930612967012,0.000371277315277309,
-2.38088415259036));
#69468=CARTESIAN_POINT('Ctrl Pts',(-0.491757040280975,-0.139558187556872,
-2.37408397683398));
#69469=CARTESIAN_POINT('Ctrl Pts',(-0.429222514293688,-0.280404479724611,
-2.36728380107759));
#69470=CARTESIAN_POINT('Ctrl Pts',(-0.323894577099873,-0.372089746504211,
-2.36048362532121));
#69471=CARTESIAN_POINT('Ctrl Pts',(-0.200766395711412,-0.479269669129251,
-2.3525342313018));
#69472=CARTESIAN_POINT('Ctrl Pts',(-0.0191585758248402,-0.519268245097442,
-2.34458483728238));
#69473=CARTESIAN_POINT('Ctrl Pts',(0.137604543034586,-0.473733539307189,
-2.33663544326297));
#69474=CARTESIAN_POINT('Ctrl Pts',(0.29436766189401,-0.428198833516938,
-2.32868604924356));
#69475=CARTESIAN_POINT('Ctrl Pts',(0.426286079726287,-0.297130845968246,
-2.32073665522415));
#69476=CARTESIAN_POINT('Ctrl Pts',(0.47283368568467,-0.140665497582472,
-2.31278726120474));
#69477=CARTESIAN_POINT('Ctrl Pts',(0.519381291643053,0.0157998508033048,
-2.30483786718533));
#69478=CARTESIAN_POINT('Ctrl Pts',(0.480558085727538,0.197662560026164,
-2.29688847316592));
#69479=CARTESIAN_POINT('Ctrl Pts',(0.37417672596785,0.321481343583503,-2.2889390791465));
#69480=CARTESIAN_POINT('Ctrl Pts',(0.267795366208163,0.445300127140841,
-2.28098968512709));
#69481=CARTESIAN_POINT('Ctrl Pts',(0.0938558526042994,0.511074985032659,
-2.27304029110768));
#69482=CARTESIAN_POINT('Ctrl Pts',(-0.0678358070548708,0.488627444797658,
-2.26509089708827));
#69483=CARTESIAN_POINT('Ctrl Pts',(-0.229527466714043,0.466179904562656,
-2.25714150306886));
#69484=CARTESIAN_POINT('Ctrl Pts',(-0.378971272428522,0.355509966200836,
-2.24919210904945));
#69485=CARTESIAN_POINT('Ctrl Pts',(-0.447600207562811,0.207394625576466,
-2.24124271503003));
#69486=CARTESIAN_POINT('Ctrl Pts',(-0.477409486442895,0.143060077962531,
-2.23778986088348));
#69487=CARTESIAN_POINT('Ctrl Pts',(-0.491971930291054,0.0716609410359785,
-2.23433700673692));
#69488=CARTESIAN_POINT('Ctrl Pts',(-0.491745711415915,0.000174011476622056,
-2.23088415259036));
#69489=CARTESIAN_POINT('Origin',(0.,0.,-1.725));
#69490=CARTESIAN_POINT('',(-0.49220542790095,-0.00042939446906537,-2.05911584740964));
#69491=CARTESIAN_POINT('',(-0.492291120116919,-0.000443263791466216,-2.08088415259036));
#69492=CARTESIAN_POINT('',(-0.4925,-6.03138548580071E-17,-1.725));
#69493=CARTESIAN_POINT('Ctrl Pts',(-0.49220542790095,-0.00042939446906537,
-2.05911584740964));
#69494=CARTESIAN_POINT('Ctrl Pts',(-0.49124239237179,0.115430969052258,
-2.06472511727582));
#69495=CARTESIAN_POINT('Ctrl Pts',(-0.45038633217708,0.231902596275435,
-2.070334387142));
#69496=CARTESIAN_POINT('Ctrl Pts',(-0.37575132226073,0.319639557992902,
-2.07594365700818));
#69497=CARTESIAN_POINT('Ctrl Pts',(-0.269979427589528,0.443979391054519,
-2.08389305102759));
#69498=CARTESIAN_POINT('Ctrl Pts',(-0.0963650834159402,0.510607835526395,
-2.091842445047));
#69499=CARTESIAN_POINT('Ctrl Pts',(0.0654348949895768,0.488954780866582,
-2.09979183906641));
#69500=CARTESIAN_POINT('Ctrl Pts',(0.227234873395094,0.46730172620677,-2.10774123308582));
#69501=CARTESIAN_POINT('Ctrl Pts',(0.377220486032541,0.357367172415269,
-2.11569062710523));
#69502=CARTESIAN_POINT('Ctrl Pts',(0.446576127279252,0.209590710096725,
-2.12364002112465));
#69503=CARTESIAN_POINT('Ctrl Pts',(0.515931768525963,0.061814247778182,
-2.13158941514406));
#69504=CARTESIAN_POINT('Ctrl Pts',(0.504657438381941,-0.123804123067402,
-2.13953880916347));
#69505=CARTESIAN_POINT('Ctrl Pts',(0.41792596538192,-0.262099963132723,
-2.14748820318288));
#69506=CARTESIAN_POINT('Ctrl Pts',(0.331194492381899,-0.400395803198045,
-2.15543759720229));
#69507=CARTESIAN_POINT('Ctrl Pts',(0.169005876525877,-0.491369112483102,
-2.1633869912217));
#69508=CARTESIAN_POINT('Ctrl Pts',(0.00577464084022879,-0.493279998315106,
-2.17133638524111));
#69509=CARTESIAN_POINT('Ctrl Pts',(-0.157456594845419,-0.49519088414711,
-2.17928577926053));
#69510=CARTESIAN_POINT('Ctrl Pts',(-0.321730450360695,-0.408039346526061,
-2.18723517327994));
#69511=CARTESIAN_POINT('Ctrl Pts',(-0.411675664046121,-0.27181179306051,
-2.19518456729935));
#69512=CARTESIAN_POINT('Ctrl Pts',(-0.464218535589615,-0.192232385228332,
-2.19982832733611));
#69513=CARTESIAN_POINT('Ctrl Pts',(-0.491396826325065,-0.0959058320295775,
-2.20447208737288));
#69514=CARTESIAN_POINT('Ctrl Pts',(-0.491782200599552,0.000219480096867314,
-2.20911584740964));
#69515=CARTESIAN_POINT('Ctrl Pts',(-0.491745711415915,0.000174011476622056,
-2.23088415259036));
#69516=CARTESIAN_POINT('Ctrl Pts',(-0.491451113918055,-0.0929210963697026,
-2.22638761271751));
#69517=CARTESIAN_POINT('Ctrl Pts',(-0.466076412307899,-0.186165091807305,
-2.22189107284465));
#69518=CARTESIAN_POINT('Ctrl Pts',(-0.416633487683608,-0.264149604332216,
-2.2173945329718));
#69519=CARTESIAN_POINT('Ctrl Pts',(-0.329223768116022,-0.402017750729617,
-2.20944513895239));
#69520=CARTESIAN_POINT('Ctrl Pts',(-0.166590264426753,-0.492193300637501,
-2.20149574493298));
#69521=CARTESIAN_POINT('Ctrl Pts',(-0.00335162072512794,-0.493302385121731,
-2.19354635091357));
#69522=CARTESIAN_POINT('Ctrl Pts',(0.159887022976497,-0.494411469605961,
-2.18559695689416));
#69523=CARTESIAN_POINT('Ctrl Pts',(0.323730806690478,-0.406454088666537,
-2.17764756287474));
#69524=CARTESIAN_POINT('Ctrl Pts',(0.413005792026864,-0.269786382681811,
-2.16969816885533));
#69525=CARTESIAN_POINT('Ctrl Pts',(0.502280777363249,-0.133118676697085,
-2.16174877483592));
#69526=CARTESIAN_POINT('Ctrl Pts',(0.516986964322038,0.0522593543329422,
-2.15379938081651));
#69527=CARTESIAN_POINT('Ctrl Pts',(0.450376937973405,0.20129354254415,-2.1458499867971));
#69528=CARTESIAN_POINT('Ctrl Pts',(0.383766911624772,0.350327730755355,
-2.13790059277768));
#69529=CARTESIAN_POINT('Ctrl Pts',(0.235840671968719,0.463018076147741,
-2.12995119875827));
#69530=CARTESIAN_POINT('Ctrl Pts',(0.0744689540071496,0.487660590387776,
-2.12200180473886));
#69531=CARTESIAN_POINT('Ctrl Pts',(-0.0869027639544218,0.512303104627812,
-2.11405241071945));
#69532=CARTESIAN_POINT('Ctrl Pts',(-0.261719960221509,0.448897787715494,
-2.10610301670004));
#69533=CARTESIAN_POINT('Ctrl Pts',(-0.369773933287149,0.32653593185073,
-2.09815362268063));
#69534=CARTESIAN_POINT('Ctrl Pts',(-0.448020352717991,0.237928573651006,
-2.09239713265054));
#69535=CARTESIAN_POINT('Ctrl Pts',(-0.491257364586673,0.118405489671946,
-2.08664064262045));
#69536=CARTESIAN_POINT('Ctrl Pts',(-0.492291120116919,-0.000443263791466216,
-2.08088415259036));
#69537=CARTESIAN_POINT('Origin',(0.,0.,-1.725));
#69538=CARTESIAN_POINT('',(-0.493313293442283,-1.40827548352207E-5,-1.90911584740964));
#69539=CARTESIAN_POINT('',(-0.493309198850653,4.2667367679637E-5,-1.93088415259036));
#69540=CARTESIAN_POINT('',(-0.4925,-6.03138548580071E-17,-1.725));
#69541=CARTESIAN_POINT('Ctrl Pts',(-0.493313293442283,-1.40827548352207E-5,
-1.90911584740964));
#69542=CARTESIAN_POINT('Ctrl Pts',(-0.49324531272362,0.162479492642686,
-1.91702875315935));
#69543=CARTESIAN_POINT('Ctrl Pts',(-0.405109814225056,0.325036240628224,
-1.92494165890906));
#69544=CARTESIAN_POINT('Ctrl Pts',(-0.2688734530373,0.413600736781722,-1.93285456465877));
#69545=CARTESIAN_POINT('Ctrl Pts',(-0.132008873942307,0.502573624659309,
-1.94080395867818));
#69546=CARTESIAN_POINT('Ctrl Pts',(0.0534011994185894,0.51687029601571,
-1.94875335269759));
#69547=CARTESIAN_POINT('Ctrl Pts',(0.202287897688472,0.449931227704149,
-1.956702746717));
#69548=CARTESIAN_POINT('Ctrl Pts',(0.351174595958352,0.382992159392589,
-1.96465214073641));
#69549=CARTESIAN_POINT('Ctrl Pts',(0.463537919137217,0.234817351413069,
-1.97260153475583));
#69550=CARTESIAN_POINT('Ctrl Pts',(0.487823921494154,0.0733915855711673,
-1.98055092877524));
#69551=CARTESIAN_POINT('Ctrl Pts',(0.512109923851091,-0.0880341802707372,
-1.98850032279465));
#69552=CARTESIAN_POINT('Ctrl Pts',(0.448318605386097,-0.262710903975027,
-1.99644971681406));
#69553=CARTESIAN_POINT('Ctrl Pts',(0.325718361490191,-0.370494334913139,
-2.00439911083347));
#69554=CARTESIAN_POINT('Ctrl Pts',(0.203118117594284,-0.478277765851253,
-2.01234850485288));
#69555=CARTESIAN_POINT('Ctrl Pts',(0.0217089482674663,-0.519167904023189,
-2.02029789887229));
#69556=CARTESIAN_POINT('Ctrl Pts',(-0.135275950764312,-0.474403752471875,
-2.02824729289171));
#69557=CARTESIAN_POINT('Ctrl Pts',(-0.292260849796088,-0.429639600920561,
-2.03619668691112));
#69558=CARTESIAN_POINT('Ctrl Pts',(-0.424821478532825,-0.299221159645997,
-2.04414608093053));
#69559=CARTESIAN_POINT('Ctrl Pts',(-0.472137070316785,-0.142986328183037,
-2.05209547494994));
#69560=CARTESIAN_POINT('Ctrl Pts',(-0.486065724361081,-0.0969942812685151,
-2.05443559910318));
#69561=CARTESIAN_POINT('Ctrl Pts',(-0.492607195467135,-0.0487650320024671,
-2.05677572325641));
#69562=CARTESIAN_POINT('Ctrl Pts',(-0.49220542790095,-0.00042939446906537,
-2.05911584740964));
#69563=CARTESIAN_POINT('Ctrl Pts',(-0.492291120116919,-0.000443263791466216,
-2.08088415259036));
#69564=CARTESIAN_POINT('Ctrl Pts',(-0.492684923739337,-0.0457180587157333,
-2.07869124860104));
#69565=CARTESIAN_POINT('Ctrl Pts',(-0.486954240838252,-0.0908949955950586,
-2.07649834461171));
#69566=CARTESIAN_POINT('Ctrl Pts',(-0.474701379384562,-0.134227705555401,
-2.07430544062239));
#69567=CARTESIAN_POINT('Ctrl Pts',(-0.430284102552143,-0.291311092279559,
-2.06635604660298));
#69568=CARTESIAN_POINT('Ctrl Pts',(-0.30015879902311,-0.424159470910667,
-2.05840665258357));
#69569=CARTESIAN_POINT('Ctrl Pts',(-0.144028872422113,-0.471820050906157,
-2.05045725856416));
#69570=CARTESIAN_POINT('Ctrl Pts',(0.0121010541788825,-0.519480630901646,
-2.04250786454475));
#69571=CARTESIAN_POINT('Ctrl Pts',(0.194235603851841,-0.481953412261521,
-2.03455847052533));
#69572=CARTESIAN_POINT('Ctrl Pts',(0.31880876569642,-0.376456434987368,
-2.02660907650592));
#69573=CARTESIAN_POINT('Ctrl Pts',(0.443381927541001,-0.270959457713215,
-2.01865968248651));
#69574=CARTESIAN_POINT('Ctrl Pts',(0.510393701557199,-0.0974927218050333,
-2.0107102884671));
#69575=CARTESIAN_POINT('Ctrl Pts',(0.489098099968701,0.0643546823104579,
-2.00276089444769));
#69576=CARTESIAN_POINT('Ctrl Pts',(0.467802498380204,0.226202086425949,
-1.99481150042828));
#69577=CARTESIAN_POINT('Ctrl Pts',(0.358199521187009,0.376430158748751,
-1.98686210640886));
#69578=CARTESIAN_POINT('Ctrl Pts',(0.210576626772402,0.446112049585561,
-1.97891271238945));
#69579=CARTESIAN_POINT('Ctrl Pts',(0.0629537323577946,0.515793940422371,
-1.97096331837004));
#69580=CARTESIAN_POINT('Ctrl Pts',(-0.122689079278224,0.504929649773189,
-1.96301392435063));
#69581=CARTESIAN_POINT('Ctrl Pts',(-0.261176155034131,0.418503874020135,
-1.95506453033122));
#69582=CARTESIAN_POINT('Ctrl Pts',(-0.399663230790036,0.332078098267084,
-1.94711513631181));
#69583=CARTESIAN_POINT('Ctrl Pts',(-0.490994570665829,0.170090837410162,
-1.9391657422924));
#69584=CARTESIAN_POINT('Ctrl Pts',(-0.493266012286453,0.00686422983988139,
-1.93121634827298));
#69585=CARTESIAN_POINT('Ctrl Pts',(-0.493297652564017,0.00459054817341155,
-1.93110561637878));
#69586=CARTESIAN_POINT('Ctrl Pts',(-0.493312012210231,0.00231662603177743,
-1.93099488448457));
#69587=CARTESIAN_POINT('Ctrl Pts',(-0.493309198850653,4.2667367679637E-5,
-1.93088415259036));
#69588=CARTESIAN_POINT('Origin',(0.,0.,-1.725));
#69589=CARTESIAN_POINT('',(-0.492247450406692,0.000436970853093216,-1.75911584740964));
#69590=CARTESIAN_POINT('',(-0.492163707300124,0.000420305474583196,-1.78088415259036));
#69591=CARTESIAN_POINT('',(-0.4925,-6.03138548580071E-17,-1.725));
#69592=CARTESIAN_POINT('Ctrl Pts',(-0.492247450406692,0.000436970853093216,
-1.75911584740964));
#69593=CARTESIAN_POINT('Ctrl Pts',(-0.492646083681307,0.0472551432774344,
-1.76138299502347));
#69594=CARTESIAN_POINT('Ctrl Pts',(-0.48651356696863,0.0939709787487651,
-1.7636501426373));
#69595=CARTESIAN_POINT('Ctrl Pts',(-0.473428455624523,0.13865064233376,
-1.76591729025113));
#69596=CARTESIAN_POINT('Ctrl Pts',(-0.427547585218155,0.295312805981787,
-1.77386668427054));
#69597=CARTESIAN_POINT('Ctrl Pts',(-0.296188516357401,0.426941393847813,
-1.78181607828995));
#69598=CARTESIAN_POINT('Ctrl Pts',(-0.139620722351902,0.473143273337493,
-1.78976547230936));
#69599=CARTESIAN_POINT('Ctrl Pts',(0.0169470716535901,0.519345152827171,
-1.79771486632877));
#69600=CARTESIAN_POINT('Ctrl Pts',(0.198723590803828,0.480120323940512,
-1.80566426034818));
#69601=CARTESIAN_POINT('Ctrl Pts',(0.322307093869532,0.373465715234961,
-1.8136136543676));
#69602=CARTESIAN_POINT('Ctrl Pts',(0.44589059693524,0.266811106529407,-1.82156304838701));
#69603=CARTESIAN_POINT('Ctrl Pts',(0.511281083916411,0.0927267180049563,
-1.82951244240642));
#69604=CARTESIAN_POINT('Ctrl Pts',(0.488476437380305,-0.0689149718046035,
-1.83746183642583));
#69605=CARTESIAN_POINT('Ctrl Pts',(0.465671790844199,-0.230556661614166,
-1.84541123044524));
#69606=CARTESIAN_POINT('Ctrl Pts',(0.354672010790817,-0.379755652708832,
-1.85336062446465));
#69607=CARTESIAN_POINT('Ctrl Pts',(0.206405429305048,-0.448057253002318,
-1.86131001848406));
#69608=CARTESIAN_POINT('Ctrl Pts',(0.0581388478192817,-0.516358853295804,
-1.86925941250348));
#69609=CARTESIAN_POINT('Ctrl Pts',(-0.127394535098869,-0.503763062788106,
-1.87720880652289));
#69610=CARTESIAN_POINT('Ctrl Pts',(-0.265069273853518,-0.416049015469756,
-1.8851582005423));
#69611=CARTESIAN_POINT('Ctrl Pts',(-0.402744012608164,-0.328334968151407,
-1.89310759456171));
#69612=CARTESIAN_POINT('Ctrl Pts',(-0.492560107199312,-0.165502664022405,
-1.90105698858112));
#69613=CARTESIAN_POINT('Ctrl Pts',(-0.493308612080344,-0.00226195975852084,
-1.90900638260053));
#69614=CARTESIAN_POINT('Ctrl Pts',(-0.493312047769644,-0.00151267360803209,
-1.90904287087024));
#69615=CARTESIAN_POINT('Ctrl Pts',(-0.493313606917367,-0.0007633788530685,
-1.90907935913994));
#69616=CARTESIAN_POINT('Ctrl Pts',(-0.493313293442283,-1.40827548352207E-5,
-1.90911584740964));
#69617=CARTESIAN_POINT('Ctrl Pts',(-0.493309198850653,4.2667367679637E-5,
-1.93088415259036));
#69618=CARTESIAN_POINT('Ctrl Pts',(-0.49311004236262,-0.160929867076482,
-1.92304549046516));
#69619=CARTESIAN_POINT('Ctrl Pts',(-0.406854173941428,-0.322085421498344,
-1.91520682833995));
#69620=CARTESIAN_POINT('Ctrl Pts',(-0.27272046309321,-0.411074233610547,
-1.90736816621475));
#69621=CARTESIAN_POINT('Ctrl Pts',(-0.136691928913891,-0.501320135207048,
-1.89941877219534));
#69622=CARTESIAN_POINT('Ctrl Pts',(0.0485766828101977,-0.517345984116404,
-1.89146937817593));
#69623=CARTESIAN_POINT('Ctrl Pts',(0.198081407402245,-0.451798885091386,
-1.88351998415651));
#69624=CARTESIAN_POINT('Ctrl Pts',(0.347586131994292,-0.386251786066369,
-1.8755705901371));
#69625=CARTESIAN_POINT('Ctrl Pts',(0.461326969454297,-0.239131739106977,
-1.86762119611769));
#69626=CARTESIAN_POINT('Ctrl Pts',(0.48711795023357,-0.0779395861454187,
-1.85967180209828));
#69627=CARTESIAN_POINT('Ctrl Pts',(0.512908931012843,0.0832525668161397,
-1.85172240807887));
#69628=CARTESIAN_POINT('Ctrl Pts',(0.450750055111385,0.258516825779865,
-1.84377301405946));
#69629=CARTESIAN_POINT('Ctrl Pts',(0.329160729256043,0.367439370296521,
-1.83582362004004));
#69630=CARTESIAN_POINT('Ctrl Pts',(0.207571403400702,0.476361914813175,
-1.82787422602063));
#69631=CARTESIAN_POINT('Ctrl Pts',(0.0265516275914822,0.518942744882762,
-1.81992483200122));
#69632=CARTESIAN_POINT('Ctrl Pts',(-0.130844061920186,0.475645149232598,
-1.81197543798181));
#69633=CARTESIAN_POINT('Ctrl Pts',(-0.288239751431856,0.432347553582433,
-1.8040260439624));
#69634=CARTESIAN_POINT('Ctrl Pts',(-0.422011354645973,0.303171532212515,
-1.79607664994299));
#69635=CARTESIAN_POINT('Ctrl Pts',(-0.470782491999074,0.147384944127326,
-1.78812725592358));
#69636=CARTESIAN_POINT('Ctrl Pts',(-0.485595125794996,0.100069876141216,
-1.78571288814584));
#69637=CARTESIAN_POINT('Ctrl Pts',(-0.492566964375401,0.050300139206298,
-1.7832985203681));
#69638=CARTESIAN_POINT('Ctrl Pts',(-0.492163707300124,0.000420305474583196,
-1.78088415259036));
#69639=CARTESIAN_POINT('Origin',(0.,0.,-1.725));
#69640=CARTESIAN_POINT('',(-0.491763056642317,-0.000197237602559575,-1.60911584740964));
#69641=CARTESIAN_POINT('',(-0.491803762672827,-0.000241441601782219,-1.63088415259036));
#69642=CARTESIAN_POINT('',(-0.4925,-6.03138548580071E-17,-1.725));
#69643=CARTESIAN_POINT('Ctrl Pts',(-0.491763056642317,-0.000197237602559575,
-1.60911584740964));
#69644=CARTESIAN_POINT('Ctrl Pts',(-0.491422941966957,0.0944266719329545,
-1.613686630907));
#69645=CARTESIAN_POINT('Ctrl Pts',(-0.465147652160607,0.189225351877548,
-1.61825741440436));
#69646=CARTESIAN_POINT('Ctrl Pts',(-0.414150969357646,0.268025143959866,
-1.62282819790172));
#69647=CARTESIAN_POINT('Ctrl Pts',(-0.325458795353369,0.405071800462394,
-1.63077759192113));
#69648=CARTESIAN_POINT('Ctrl Pts',(-0.161991059533466,0.493726126140734,
-1.63872698594054));
#69649=CARTESIAN_POINT('Ctrl Pts',(0.00125083601822007,0.493312212117073,
-1.64667637995995));
#69650=CARTESIAN_POINT('Ctrl Pts',(0.164492731569907,0.492898298093412,
-1.65462577397937));
#69651=CARTESIAN_POINT('Ctrl Pts',(0.327508786853377,0.403416144367749,
-1.66257516799878));
#69652=CARTESIAN_POINT('Ctrl Pts',(0.415504837459898,0.265921479504776,
-1.67052456201819));
#69653=CARTESIAN_POINT('Ctrl Pts',(0.503500888066418,0.128426814641802,
-1.6784739560376));
#69654=CARTESIAN_POINT('Ctrl Pts',(0.516476933995988,-0.0570803613584818,
-1.68642335005701));
#69655=CARTESIAN_POINT('Ctrl Pts',(0.448479374476317,-0.205486627019658,
-1.69437274407642));
#69656=CARTESIAN_POINT('Ctrl Pts',(0.380481814956647,-0.353892892680831,
-1.70232213809583));
#69657=CARTESIAN_POINT('Ctrl Pts',(0.231510649987738,-0.465198248002898,
-1.71027153211525));
#69658=CARTESIAN_POINT('Ctrl Pts',(0.0699160416776696,-0.488334158472158,
-1.71822092613466));
#69659=CARTESIAN_POINT('Ctrl Pts',(-0.0916785666324007,-0.511470068941419,
-1.72617032015407));
#69660=CARTESIAN_POINT('Ctrl Pts',(-0.26589661828363,-0.44643653455787,
-1.73411971417348));
#69661=CARTESIAN_POINT('Ctrl Pts',(-0.372804308133253,-0.323071897651082,
-1.74206910819289));
#69662=CARTESIAN_POINT('Ctrl Pts',(-0.449222187897897,-0.234890551635539,
-1.74775135459847));
#69663=CARTESIAN_POINT('Ctrl Pts',(-0.491248339242509,-0.116905362902091,
-1.75343360100406));
#69664=CARTESIAN_POINT('Ctrl Pts',(-0.492247450406692,0.000436970853093216,
-1.75911584740964));
#69665=CARTESIAN_POINT('Ctrl Pts',(-0.492163707300124,0.000420305474583196,
-1.78088415259036));
#69666=CARTESIAN_POINT('Ctrl Pts',(-0.491239225738378,-0.113931033696202,
-1.77534912634869));
#69667=CARTESIAN_POINT('Ctrl Pts',(-0.451553280043693,-0.228861011197853,
-1.76981410010701));
#69668=CARTESIAN_POINT('Ctrl Pts',(-0.378717055390082,-0.316120022277836,
-1.76427907386534));
#69669=CARTESIAN_POINT('Ctrl Pts',(-0.274109809935903,-0.441441245797349,
-1.75632967984593));
#69670=CARTESIAN_POINT('Ctrl Pts',(-0.101124647535461,-0.50968653803592,
-1.74838028582652));
#69671=CARTESIAN_POINT('Ctrl Pts',(0.0608702943946502,-0.489543954909651,
-1.74043089180711));
#69672=CARTESIAN_POINT('Ctrl Pts',(0.222865236324764,-0.469401371783382,
-1.7324814977877));
#69673=CARTESIAN_POINT('Ctrl Pts',(0.373869957784543,-0.36087091329227,
-1.72453210376828));
#69674=CARTESIAN_POINT('Ctrl Pts',(0.444601271030807,-0.2137479504605,-1.71658270974887));
#69675=CARTESIAN_POINT('Ctrl Pts',(0.51533258427707,-0.0666249876287323,
-1.70863331572946));
#69676=CARTESIAN_POINT('Ctrl Pts',(0.505790489309818,0.119090479543697,
-1.70068392171005));
#69677=CARTESIAN_POINT('Ctrl Pts',(0.420353039680544,0.258189462526263,
-1.69273452769064));
#69678=CARTESIAN_POINT('Ctrl Pts',(0.33491559005127,0.39728844550883,-1.68478513367123));
#69679=CARTESIAN_POINT('Ctrl Pts',(0.173582785759975,0.489770944301538,
-1.67683573965181));
#69680=CARTESIAN_POINT('Ctrl Pts',(0.0103764908966829,0.493204627882733,
-1.6688863456324));
#69681=CARTESIAN_POINT('Ctrl Pts',(-0.152829803966609,0.496638311463928,
-1.66093695161299));
#69682=CARTESIAN_POINT('Ctrl Pts',(-0.317909589401894,0.41102317983361,
-1.65298755759358));
#69683=CARTESIAN_POINT('Ctrl Pts',(-0.409121831245792,0.275640714928625,
-1.64503816357417));
#69684=CARTESIAN_POINT('Ctrl Pts',(-0.463256736361998,0.195290569554802,
-1.6403201599129));
#69685=CARTESIAN_POINT('Ctrl Pts',(-0.491371949157338,0.0974099820344272,
-1.63560215625163));
#69686=CARTESIAN_POINT('Ctrl Pts',(-0.491803762672827,-0.000241441601782219,
-1.63088415259036));
#69687=CARTESIAN_POINT('Origin',(0.,0.,-1.725));
#69688=CARTESIAN_POINT('',(-0.492971877712692,-0.00035487951936386,-1.45911584740964));
#69689=CARTESIAN_POINT('',(-0.493049169896767,-0.00031838663161669,-1.48088415259036));
#69690=CARTESIAN_POINT('',(-0.4925,-6.03138548580071E-17,-1.725));
#69691=CARTESIAN_POINT('Ctrl Pts',(-0.492971877712692,-0.00035487951936386,
-1.45911584740964));
#69692=CARTESIAN_POINT('Ctrl Pts',(-0.491822722696216,0.141071489966078,
-1.46599026679053));
#69693=CARTESIAN_POINT('Ctrl Pts',(-0.427747046070754,0.283406525101959,
-1.47286468617142));
#69694=CARTESIAN_POINT('Ctrl Pts',(-0.320409052113906,0.375095377921473,
-1.47973910555231));
#69695=CARTESIAN_POINT('Ctrl Pts',(-0.196286277529025,0.481121905816508,
-1.48768849957172));
#69696=CARTESIAN_POINT('Ctrl Pts',(-0.0143131810680683,0.519424415916717,
-1.49563789359113));
#69697=CARTESIAN_POINT('Ctrl Pts',(0.142018303477539,0.472429153092764,
-1.50358728761054));
#69698=CARTESIAN_POINT('Ctrl Pts',(0.298349788023149,0.42543389026881,-1.51153668162996));
#69699=CARTESIAN_POINT('Ctrl Pts',(0.429039660653408,0.293140854520689,
-1.51948607564937));
#69700=CARTESIAN_POINT('Ctrl Pts',(0.47412548513425,0.136248036906213,-1.52743546966878));
#69701=CARTESIAN_POINT('Ctrl Pts',(0.519211309615092,-0.0206447807082635,
-1.53538486368819));
#69702=CARTESIAN_POINT('Ctrl Pts',(0.478693085946517,-0.202137380189096,
-1.5433342577076));
#69703=CARTESIAN_POINT('Ctrl Pts',(0.371161171239962,-0.32495828682827,
-1.55128365172701));
#69704=CARTESIAN_POINT('Ctrl Pts',(0.263629256533406,-0.447779193467444,
-1.55923304574643));
#69705=CARTESIAN_POINT('Ctrl Pts',(0.0890836507888685,-0.511928407264959,
-1.56718243976584));
#69706=CARTESIAN_POINT('Ctrl Pts',(-0.0723915542139933,-0.487973325185985,
-1.57513183378525));
#69707=CARTESIAN_POINT('Ctrl Pts',(-0.233866759216855,-0.464018243107011,
-1.58308122780466));
#69708=CARTESIAN_POINT('Ctrl Pts',(-0.382271563478042,-0.351958865151547,
-1.59103062182407));
#69709=CARTESIAN_POINT('Ctrl Pts',(-0.449515659514308,-0.203209682510457,
-1.59898001584348));
#69710=CARTESIAN_POINT('Ctrl Pts',(-0.478095399033977,-0.139989070676324,
-1.60235862636554));
#69711=CARTESIAN_POINT('Ctrl Pts',(-0.492014461028795,-0.0701408996856698,
-1.60573723688759));
#69712=CARTESIAN_POINT('Ctrl Pts',(-0.491763056642317,-0.000197237602559575,
-1.60911584740964));
#69713=CARTESIAN_POINT('Ctrl Pts',(-0.491803762672827,-0.000241441601782219,
-1.63088415259036));
#69714=CARTESIAN_POINT('Ctrl Pts',(-0.49209951446334,-0.0671235153456273,
-1.62765276223222));
#69715=CARTESIAN_POINT('Ctrl Pts',(-0.479409077259817,-0.133898089086301,
-1.62442137187408));
#69716=CARTESIAN_POINT('Ctrl Pts',(-0.453197923274928,-0.194859228335653,
-1.62118998151593));
#69717=CARTESIAN_POINT('Ctrl Pts',(-0.388717075207656,-0.344826908515301,
-1.61324058749652));
#69718=CARTESIAN_POINT('Ctrl Pts',(-0.242410680820596,-0.459612470694942,
-1.60529119347711));
#69719=CARTESIAN_POINT('Ctrl Pts',(-0.0814062662755531,-0.48655061025483,
-1.5973417994577));
#69720=CARTESIAN_POINT('Ctrl Pts',(0.079598148269487,-0.513488749814717,
-1.58939240543829));
#69721=CARTESIAN_POINT('Ctrl Pts',(0.255300582972512,-0.452579466754855,
-1.58144301141888));
#69722=CARTESIAN_POINT('Ctrl Pts',(0.365086175908778,-0.331768836222721,
-1.57349361739946));
#69723=CARTESIAN_POINT('Ctrl Pts',(0.474871768845042,-0.21095820569059,
-1.56554422338005));
#69724=CARTESIAN_POINT('Ctrl Pts',(0.518740520014552,-0.0302462276861947,
-1.55759482936064));
#69725=CARTESIAN_POINT('Ctrl Pts',(0.47656480099646,0.127453783700125,-1.54964543534123));
#69726=CARTESIAN_POINT('Ctrl Pts',(0.434389081978368,0.285153795086447,
-1.54169604132182));
#69727=CARTESIAN_POINT('Ctrl Pts',(0.306168892772669,0.419841839854689,
-1.53374664730241));
#69728=CARTESIAN_POINT('Ctrl Pts',(0.150733542524981,0.469721061573934,
-1.525797253283));
#69729=CARTESIAN_POINT('Ctrl Pts',(-0.00470180772270484,0.519600283293178,
-1.51784785926358));
#69730=CARTESIAN_POINT('Ctrl Pts',(-0.187352319012382,0.484670681963428,
-1.50989846524417));
#69731=CARTESIAN_POINT('Ctrl Pts',(-0.313415249663277,0.380958472548885,
-1.50194907122476));
#69732=CARTESIAN_POINT('Ctrl Pts',(-0.424765681762926,0.289350263278393,
-1.49492743167996));
#69733=CARTESIAN_POINT('Ctrl Pts',(-0.491966171457023,0.144077483952644,
-1.48790579213516));
#69734=CARTESIAN_POINT('Ctrl Pts',(-0.493049169896767,-0.00031838663161669,
-1.48088415259036));
#69735=CARTESIAN_POINT('Origin',(0.,0.,-1.725));
#69736=CARTESIAN_POINT('',(-0.492885109875619,0.000387266687590468,-1.30911584740964));
#69737=CARTESIAN_POINT('',(-0.492797570805203,0.000412494226899228,-1.33088415259036));
#69738=CARTESIAN_POINT('',(-0.4925,-6.03138548580071E-17,-1.725));
#69739=CARTESIAN_POINT('Ctrl Pts',(-0.492885109875619,0.000387266687590468,
-1.30911584740964));
#69740=CARTESIAN_POINT('Ctrl Pts',(-0.493103291714472,0.025675910579845,
-1.31034450865465));
#69741=CARTESIAN_POINT('Ctrl Pts',(-0.49132560003428,0.0509337966894253,
-1.31157316989966));
#69742=CARTESIAN_POINT('Ctrl Pts',(-0.487445469794451,0.0758644659340029,
-1.31280183114467));
#69743=CARTESIAN_POINT('Ctrl Pts',(-0.46234116684007,0.237164998361211,
-1.32075122516408));
#69744=CARTESIAN_POINT('Ctrl Pts',(-0.349227873070351,0.384768090768282,
-1.32870061918349));
#69745=CARTESIAN_POINT('Ctrl Pts',(-0.200003631756639,0.450951272865195,
-1.3366500132029));
#69746=CARTESIAN_POINT('Ctrl Pts',(-0.0507793904429269,0.517134454962107,
-1.34459940722231));
#69747=CARTESIAN_POINT('Ctrl Pts',(0.134555798414777,0.501897726748859,
-1.35254880124173));
#69748=CARTESIAN_POINT('Ctrl Pts',(0.270967423571298,0.412231923287992,
-1.36049819526114));
#69749=CARTESIAN_POINT('Ctrl Pts',(0.407379048727822,0.322566119827124,
-1.36844758928055));
#69750=CARTESIAN_POINT('Ctrl Pts',(0.494867110183159,0.158471241118635,
-1.37639698329996));
#69751=CARTESIAN_POINT('Ctrl Pts',(0.493290798242749,-0.00476356837000694,
-1.38434637731937));
#69752=CARTESIAN_POINT('Ctrl Pts',(0.49171448630234,-0.167998377858649,
-1.39229577133878));
#69753=CARTESIAN_POINT('Ctrl Pts',(0.401073800966179,-0.330373118127449,
-1.4002451653582));
#69754=CARTESIAN_POINT('Ctrl Pts',(0.262956022145839,-0.417387869531233,
-1.40819455937761));
#69755=CARTESIAN_POINT('Ctrl Pts',(0.1248382433255,-0.504402620935016,-1.41614395339702));
#69756=CARTESIAN_POINT('Ctrl Pts',(-0.0607566289790167,-0.516057383473792,
-1.42409334741643));
#69757=CARTESIAN_POINT('Ctrl Pts',(-0.208674936936753,-0.447004780633302,
-1.43204274143584));
#69758=CARTESIAN_POINT('Ctrl Pts',(-0.356593244894491,-0.377952177792812,
-1.43999213545525));
#69759=CARTESIAN_POINT('Ctrl Pts',(-0.466834988505445,-0.228192209573053,
-1.44794152947466));
#69760=CARTESIAN_POINT('Ctrl Pts',(-0.48881963395652,-0.0664369526182409,
-1.45589092349408));
#69761=CARTESIAN_POINT('Ctrl Pts',(-0.491792556954056,-0.0445632351437636,
-1.4569658981326));
#69762=CARTESIAN_POINT('Ctrl Pts',(-0.493151574706721,-0.022470166933687,
-1.45804087277112));
#69763=CARTESIAN_POINT('Ctrl Pts',(-0.492971877712692,-0.00035487951936386,
-1.45911584740964));
#69764=CARTESIAN_POINT('Ctrl Pts',(-0.493049169896767,-0.00031838663161669,
-1.48088415259036));
#69765=CARTESIAN_POINT('Ctrl Pts',(-0.493192264204308,-0.0193971095132318,
-1.47995639811575));
#69766=CARTESIAN_POINT('Ctrl Pts',(-0.492181093798244,-0.0384605235136697,
-1.47902864364114));
#69767=CARTESIAN_POINT('Ctrl Pts',(-0.489964987012965,-0.0573828199869844,
-1.47810088916653));
#69768=CARTESIAN_POINT('Ctrl Pts',(-0.470976443699642,-0.219517085608957,
-1.47015149514712));
#69769=CARTESIAN_POINT('Ctrl Pts',(-0.363524007060886,-0.371290799353565,
-1.4622021011277));
#69770=CARTESIAN_POINT('Ctrl Pts',(-0.216908435835479,-0.443067948504154,
-1.45425270710829));
#69771=CARTESIAN_POINT('Ctrl Pts',(-0.0702928646100672,-0.514845097654745,
-1.44630331308888));
#69772=CARTESIAN_POINT('Ctrl Pts',(0.115485841202,-0.506625682211315,-1.43835391906947));
#69773=CARTESIAN_POINT('Ctrl Pts',(0.255189678251986,-0.422180890900952,
-1.43040452505006));
#69774=CARTESIAN_POINT('Ctrl Pts',(0.394893515301968,-0.337736099590592,
-1.42245513103065));
#69775=CARTESIAN_POINT('Ctrl Pts',(0.488522483589872,-0.17706593241331,
-1.41450573701123));
#69776=CARTESIAN_POINT('Ctrl Pts',(0.49311823502313,-0.0138882258026879,
-1.40655634299182));
#69777=CARTESIAN_POINT('Ctrl Pts',(0.497713986456388,0.149289480807939,
-1.39860694897241));
#69778=CARTESIAN_POINT('Ctrl Pts',(0.413276521034989,0.314974726851901,
-1.390657554953));
#69779=CARTESIAN_POINT('Ctrl Pts',(0.278546990113647,0.407148683931192,
-1.38270816093359));
#69780=CARTESIAN_POINT('Ctrl Pts',(0.143817459192309,0.49932264101048,-1.37475876691418));
#69781=CARTESIAN_POINT('Ctrl Pts',(-0.041204137228972,0.517985309125103,
-1.36680937289476));
#69782=CARTESIAN_POINT('Ctrl Pts',(-0.191627168728328,0.454573981584339,
-1.35885997887535));
#69783=CARTESIAN_POINT('Ctrl Pts',(-0.342050200227689,0.391162654043573,
-1.35091058485594));
#69784=CARTESIAN_POINT('Ctrl Pts',(-0.457874666805125,0.245677330847414,
-1.34296119083653));
#69785=CARTESIAN_POINT('Ctrl Pts',(-0.485958599219122,0.0848688186159221,
-1.33501179681712));
#69786=CARTESIAN_POINT('Ctrl Pts',(-0.490819367273069,0.0570360754112031,
-1.3336359154082));
#69787=CARTESIAN_POINT('Ctrl Pts',(-0.493051718544713,0.0287443000430391,
-1.33226003399928));
#69788=CARTESIAN_POINT('Ctrl Pts',(-0.492797570805203,0.000412494226899228,
-1.33088415259036));
#69789=CARTESIAN_POINT('Origin',(0.,0.,-1.725));
#69790=CARTESIAN_POINT('',(-0.491729663766022,0.000148572764139432,-1.15911584740964));
#69791=CARTESIAN_POINT('',(-0.491706700480042,0.000100130005186201,-1.18088415259036));
#69792=CARTESIAN_POINT('',(-0.4925,-6.03138548580071E-17,-1.725));
#69793=CARTESIAN_POINT('Ctrl Pts',(-0.491729663766022,0.000148572764139432,
-1.15911584740964));
#69794=CARTESIAN_POINT('Ctrl Pts',(-0.491926890574513,0.0732862396464759,
-1.16264814453818));
#69795=CARTESIAN_POINT('Ctrl Pts',(-0.476658155659677,0.146345621070356,
-1.16618044166672));
#69796=CARTESIAN_POINT('Ctrl Pts',(-0.44550752094592,0.211852665773185,
-1.16971273879526));
#69797=CARTESIAN_POINT('Ctrl Pts',(-0.37540337616897,0.359275515675158,
-1.17766213281467));
#69798=CARTESIAN_POINT('Ctrl Pts',(-0.224862198434001,0.468448057652222,
-1.18561152683408));
#69799=CARTESIAN_POINT('Ctrl Pts',(-0.0629544948037265,0.489280323330698,
-1.1935609208535));
#69800=CARTESIAN_POINT('Ctrl Pts',(0.0989532088265435,0.510112589009172,
-1.20151031487291));
#69801=CARTESIAN_POINT('Ctrl Pts',(0.27222743835212,0.442604578389054,-1.20945970889232));
#69802=CARTESIAN_POINT('Ctrl Pts',(0.377367428106713,0.317729959901029,
-1.21740910291173));
#69803=CARTESIAN_POINT('Ctrl Pts',(0.482507417861307,0.192855341413001,
-1.22535849693114));
#69804=CARTESIAN_POINT('Ctrl Pts',(0.519513167844922,0.010614115057068,
-1.23330789095055));
#69805=CARTESIAN_POINT('Ctrl Pts',(0.471405895547274,-0.145378763434889,
-1.24125728496997));
#69806=CARTESIAN_POINT('Ctrl Pts',(0.423298623249626,-0.301371641926843,
-1.24920667898938));
#69807=CARTESIAN_POINT('Ctrl Pts',(0.290078328670708,-0.431116172554822,
-1.25715607300879));
#69808=CARTESIAN_POINT('Ctrl Pts',(0.132868442861468,-0.475083655902993,
-1.2651054670282));
#69809=CARTESIAN_POINT('Ctrl Pts',(-0.0243414429477769,-0.519051139251165,
-1.27305486104761));
#69810=CARTESIAN_POINT('Ctrl Pts',(-0.205540919987342,-0.477241575319532,
-1.28100425506702));
#69811=CARTESIAN_POINT('Ctrl Pts',(-0.327593002437608,-0.368837807130042,
-1.28895364908643));
#69812=CARTESIAN_POINT('Ctrl Pts',(-0.430780670416379,-0.277188964971672,
-1.29567438186084));
#69813=CARTESIAN_POINT('Ctrl Pts',(-0.491691663072351,-0.137940704929582,
-1.30239511463524));
#69814=CARTESIAN_POINT('Ctrl Pts',(-0.492885109875619,0.000387266687590468,
-1.30911584740964));
#69815=CARTESIAN_POINT('Ctrl Pts',(-0.492797570805203,0.000412494226899228,
-1.33088415259036));
#69816=CARTESIAN_POINT('Ctrl Pts',(-0.491583335799359,-0.134947633181582,
-1.32431063997987));
#69817=CARTESIAN_POINT('Ctrl Pts',(-0.433611858386805,-0.271221502292443,
-1.31773712736938));
#69818=CARTESIAN_POINT('Ctrl Pts',(-0.334360120503988,-0.362714469445089,
-1.31116361475888));
#69819=CARTESIAN_POINT('Ctrl Pts',(-0.214334311124291,-0.473357544007792,
-1.30321422073947));
#69820=CARTESIAN_POINT('Ctrl Pts',(-0.0339392941143324,-0.518511991866373,
-1.29526482672006));
#69821=CARTESIAN_POINT('Ctrl Pts',(0.124057042802824,-0.477460288044243,
-1.28731543270065));
#69822=CARTESIAN_POINT('Ctrl Pts',(0.282053379719976,-0.436408584222115,
-1.27936603868124));
#69823=CARTESIAN_POINT('Ctrl Pts',(0.41765103654433,-0.309150728719275,
-1.27141664466183));
#69824=CARTESIAN_POINT('Ctrl Pts',(0.468635813451673,-0.1540744978209,-1.26346725064242));
#69825=CARTESIAN_POINT('Ctrl Pts',(0.519620590359018,0.00100173307748005,
-1.255517856623));
#69826=CARTESIAN_POINT('Ctrl Pts',(0.485992487349354,0.1838963393714,-1.24756846260359));
#69827=CARTESIAN_POINT('Ctrl Pts',(0.383180572810361,0.310694585001086,
-1.23961906858418));
#69828=CARTESIAN_POINT('Ctrl Pts',(0.280368658271367,0.437492830630774,
-1.23166967456477));
#69829=CARTESIAN_POINT('Ctrl Pts',(0.10837293220305,0.508194715596224,-1.22372028054536));
#69830=CARTESIAN_POINT('Ctrl Pts',(-0.0538924359234794,0.490361174929773,
-1.21577088652595));
#69831=CARTESIAN_POINT('Ctrl Pts',(-0.216157804050004,0.472527634263322,
-1.20782149250653));
#69832=CARTESIAN_POINT('Ctrl Pts',(-0.36869281423474,0.366158667964968,
-1.19987209848712));
#69833=CARTESIAN_POINT('Ctrl Pts',(-0.441512159754325,0.220057922641619,
-1.19192270446771));
#69834=CARTESIAN_POINT('Ctrl Pts',(-0.47521787875756,0.152432614656566,
-1.18824318717526));
#69835=CARTESIAN_POINT('Ctrl Pts',(-0.491844799023225,0.0762949137772939,
-1.18456366988281));
#69836=CARTESIAN_POINT('Ctrl Pts',(-0.491706700480042,0.000100130005186201,
-1.18088415259036));
#69837=CARTESIAN_POINT('Origin',(0.,0.,-1.725));
#69838=CARTESIAN_POINT('',(-0.492338823654994,-0.000448382455763341,-1.00911584740964));
#69839=CARTESIAN_POINT('',(-0.492429148680948,-0.000453349453110901,-1.03088415259036));
#69840=CARTESIAN_POINT('',(-0.4925,-6.03138548580071E-17,-1.725));
#69841=CARTESIAN_POINT('Ctrl Pts',(-0.492338823654994,-0.000448382455763341,
-1.00911584740964));
#69842=CARTESIAN_POINT('Ctrl Pts',(-0.491270535922525,0.120010930195667,
-1.01495178042171));
#69843=CARTESIAN_POINT('Ctrl Pts',(-0.446714827583699,0.241177295005307,
-1.02078771343378));
#69844=CARTESIAN_POINT('Ctrl Pts',(-0.366495740713805,0.330211107101538,
-1.02662364644585));
#69845=CARTESIAN_POINT('Ctrl Pts',(-0.257225615767691,0.451488176584551,
-1.03457304046526));
#69846=CARTESIAN_POINT('Ctrl Pts',(-0.0817841500725429,0.513145148861044,
-1.04252243448468));
#69847=CARTESIAN_POINT('Ctrl Pts',(0.0793335308670154,0.486892897971162,
-1.05047182850409));
#69848=CARTESIAN_POINT('Ctrl Pts',(0.240451211806571,0.460640647081281,
-1.0584212225235));
#69849=CARTESIAN_POINT('Ctrl Pts',(0.387245107990538,0.346479173025028,
-1.06637061654291));
#69850=CARTESIAN_POINT('Ctrl Pts',(0.452364020260708,0.196787439609733,
-1.07432001056232));
#69851=CARTESIAN_POINT('Ctrl Pts',(0.517482932530879,0.0470957061944376,
-1.08226940458173));
#69852=CARTESIAN_POINT('Ctrl Pts',(0.500926860887252,-0.138126286579906,
-1.09021879860114));
#69853=CARTESIAN_POINT('Ctrl Pts',(0.410291974568023,-0.273895963496465,
-1.09816819262056));
#69854=CARTESIAN_POINT('Ctrl Pts',(0.319657088248792,-0.409665640413027,
-1.10611758663997));
#69855=CARTESIAN_POINT('Ctrl Pts',(0.154943387253964,-0.495983001471805,
-1.11406698065938));
#69856=CARTESIAN_POINT('Ctrl Pts',(-0.00827605918009707,-0.493244371543186,
-1.12201637467879));
#69857=CARTESIAN_POINT('Ctrl Pts',(-0.171495505614156,-0.490505741614567,
-1.1299657686982));
#69858=CARTESIAN_POINT('Ctrl Pts',(-0.333220697487443,-0.398711120698549,
-1.13791516271761));
#69859=CARTESIAN_POINT('Ctrl Pts',(-0.419249737514621,-0.259977231327102,
-1.14586455673703));
#69860=CARTESIAN_POINT('Ctrl Pts',(-0.467051947884461,-0.182889464648957,
-1.1502816536279));
#69861=CARTESIAN_POINT('Ctrl Pts',(-0.491483033912735,-0.0913092376168913,
-1.15469875051877));
#69862=CARTESIAN_POINT('Ctrl Pts',(-0.491729663766022,0.000148572764139432,
-1.15911584740964));
#69863=CARTESIAN_POINT('Ctrl Pts',(-0.491706700480042,0.000100130005186201,
-1.18088415259036));
#69864=CARTESIAN_POINT('Ctrl Pts',(-0.491546444743027,-0.0883197109918345,
-1.1766142758634));
#69865=CARTESIAN_POINT('Ctrl Pts',(-0.468809875758622,-0.176816421647303,
-1.17234439913644));
#69866=CARTESIAN_POINT('Ctrl Pts',(-0.423987334998264,-0.252176954318478,
-1.16807452240948));
#69867=CARTESIAN_POINT('Ctrl Pts',(-0.340539483868178,-0.392478561606883,
-1.16012512839007));
#69868=CARTESIAN_POINT('Ctrl Pts',(-0.18054010075356,-0.487249251835348,
-1.15217573437065));
#69869=CARTESIAN_POINT('Ctrl Pts',(-0.0173992564916812,-0.493006838088287,
-1.14422634035124));
#69870=CARTESIAN_POINT('Ctrl Pts',(0.1457415877702,-0.498764424341226,-1.13627694633183));
#69871=CARTESIAN_POINT('Ctrl Pts',(0.312023893179346,-0.415508906618639,
-1.12832755231242));
#69872=CARTESIAN_POINT('Ctrl Pts',(0.405154891717245,-0.281439141282553,
-1.12037815829301));
#69873=CARTESIAN_POINT('Ctrl Pts',(0.498285890255143,-0.147369375946468,
-1.1124287642736));
#69874=CARTESIAN_POINT('Ctrl Pts',(0.518265581921795,0.0375146370031122,
-1.10447937025418));
#69875=CARTESIAN_POINT('Ctrl Pts',(0.455926990245143,0.188385392465231,
-1.09652997623477));
#69876=CARTESIAN_POINT('Ctrl Pts',(0.39358839856849,0.339256147927351,-1.08858058221536));
#69877=CARTESIAN_POINT('Ctrl Pts',(0.248931523548531,0.456113645902006,
-1.08063118819595));
#69878=CARTESIAN_POINT('Ctrl Pts',(0.0883270675941921,0.485341947144984,
-1.07268179417654));
#69879=CARTESIAN_POINT('Ctrl Pts',(-0.0722773883601444,0.514570248387963,
-1.06473240015713));
#69880=CARTESIAN_POINT('Ctrl Pts',(-0.248829425248864,0.456169352899263,
-1.05678300613772));
#69881=CARTESIAN_POINT('Ctrl Pts',(-0.360324371165323,0.336934450706051,
-1.0488336121183));
#69882=CARTESIAN_POINT('Ctrl Pts',(-0.444241628020003,0.247191675092816,
-1.04285045894232));
#69883=CARTESIAN_POINT('Ctrl Pts',(-0.491304697860191,0.122987047183034,
-1.03686730576634));
#69884=CARTESIAN_POINT('Ctrl Pts',(-0.492429148680948,-0.000453349453110901,
-1.03088415259036));
#69885=CARTESIAN_POINT('Origin',(0.,0.,-1.725));
#69886=CARTESIAN_POINT('',(-0.493300545452038,7.30209052610606E-5,-0.859115847409639));
#69887=CARTESIAN_POINT('',(-0.493273413985951,0.000128110117115081,-0.880884152590357));
#69888=CARTESIAN_POINT('',(-0.4925,-6.03138548580071E-17,-1.725));
#69889=CARTESIAN_POINT('Ctrl Pts',(-0.493300545452038,7.30209052610606E-5,
-0.859115847409639));
#69890=CARTESIAN_POINT('Ctrl Pts',(-0.493308612914771,0.00397858311580164,
-0.85930602228583));
#69891=CARTESIAN_POINT('Ctrl Pts',(-0.493266254174895,0.00788396578159667,
-0.859496197162021));
#69892=CARTESIAN_POINT('Ctrl Pts',(-0.493172934372577,0.0117881303439544,
-0.859686372038211));
#69893=CARTESIAN_POINT('Ctrl Pts',(-0.489272125320914,0.174983937510891,
-0.867635766057623));
#69894=CARTESIAN_POINT('Ctrl Pts',(-0.396328223367036,0.336051380543862,
-0.875585160077034));
#69895=CARTESIAN_POINT('Ctrl Pts',(-0.256985258091237,0.421090347002093,
-0.883534554096445));
#69896=CARTESIAN_POINT('Ctrl Pts',(-0.117642292815437,0.506129313460325,
-0.891483948115857));
#69897=CARTESIAN_POINT('Ctrl Pts',(0.0680997357822896,0.515139803343804,
-0.899433342135269));
#69898=CARTESIAN_POINT('Ctrl Pts',(0.215019652398866,0.443987671334291,
-0.90738273615468));
#69899=CARTESIAN_POINT('Ctrl Pts',(0.361939569015442,0.372835539324777,
-0.915332130174092));
#69900=CARTESIAN_POINT('Ctrl Pts',(0.470037373650875,0.221520785422272,
-0.923281524193504));
#69901=CARTESIAN_POINT('Ctrl Pts',(0.489716203234967,0.059468844815788,
-0.931230918212915));
#69902=CARTESIAN_POINT('Ctrl Pts',(0.509395032819059,-0.102583095790696,
-0.939180312232327));
#69903=CARTESIAN_POINT('Ctrl Pts',(0.44065488735181,-0.275372223101158,
-0.947129706251738));
#69904=CARTESIAN_POINT('Ctrl Pts',(0.315034756858612,-0.379620343482295,
-0.95507910027115));
#69905=CARTESIAN_POINT('Ctrl Pts',(0.189414626365416,-0.48386846386343,
-0.963028494290561));
#69906=CARTESIAN_POINT('Ctrl Pts',(0.00691451084627304,-0.519575577315242,
-0.970977888309973));
#69907=CARTESIAN_POINT('Ctrl Pts',(-0.148731851810166,-0.470358734873397,
-0.978927282329384));
#69908=CARTESIAN_POINT('Ctrl Pts',(-0.304378214466607,-0.421141892431551,
-0.986876676348796));
#69909=CARTESIAN_POINT('Ctrl Pts',(-0.433170824260342,-0.287001094096046,
-0.994826070368207));
#69910=CARTESIAN_POINT('Ctrl Pts',(-0.47601773705867,-0.129482111583526,
-1.00277546438762));
#69911=CARTESIAN_POINT('Ctrl Pts',(-0.487409206554715,-0.0876034191142425,
-1.00488892539496));
#69912=CARTESIAN_POINT('Ctrl Pts',(-0.492725700005788,-0.0440722656862921,
-1.0070023864023));
#69913=CARTESIAN_POINT('Ctrl Pts',(-0.492338823654994,-0.000448382455763341,
-1.00911584740964));
#69914=CARTESIAN_POINT('Ctrl Pts',(-0.492429148680948,-0.000453349453110901,
-1.03088415259036));
#69915=CARTESIAN_POINT('Ctrl Pts',(-0.492798676430811,-0.041019509545657,
-1.02891791174693));
#69916=CARTESIAN_POINT('Ctrl Pts',(-0.488206954099861,-0.0815031346698257,
-1.0269516709035));
#69917=CARTESIAN_POINT('Ctrl Pts',(-0.478331564969346,-0.120654011463565,
-1.02498543006007));
#69918=CARTESIAN_POINT('Ctrl Pts',(-0.438405957912708,-0.27893866254224,
-1.01703603604066));
#69919=CARTESIAN_POINT('Ctrl Pts',(-0.312116888855228,-0.415439055801866,
-1.00908664202125));
#69920=CARTESIAN_POINT('Ctrl Pts',(-0.157407640608445,-0.467526802660934,
-1.00113724800183));
#69921=CARTESIAN_POINT('Ctrl Pts',(-0.00269839236166527,-0.519614549520002,
-0.993187853982423));
#69922=CARTESIAN_POINT('Ctrl Pts',(0.180431035074421,-0.487289649978516,
-0.985238459963011));
#69923=CARTESIAN_POINT('Ctrl Pts',(0.307958166245391,-0.385383243500609,
-0.977289065943599));
#69924=CARTESIAN_POINT('Ctrl Pts',(0.435485297416365,-0.283476837022699,
-0.969339671924188));
#69925=CARTESIAN_POINT('Ctrl Pts',(0.507410132322223,-0.111988923608367,
-0.961390277904777));
#69926=CARTESIAN_POINT('Ctrl Pts',(0.490732498570953,0.0503993191877119,
-0.953440883885366));
#69927=CARTESIAN_POINT('Ctrl Pts',(0.474054864819683,0.212787561983789,
-0.945491489865954));
#69928=CARTESIAN_POINT('Ctrl Pts',(0.368774762411284,0.366076134161612,
-0.937542095846542));
#69929=CARTESIAN_POINT('Ctrl Pts',(0.223196251180912,0.439933983669209,
-0.92959270182713));
#69930=CARTESIAN_POINT('Ctrl Pts',(0.0776177399505409,0.513791833176806,
-0.921643307807718));
#69931=CARTESIAN_POINT('Ctrl Pts',(-0.108259180101798,0.50821896001418,
-0.913693913788307));
#69932=CARTESIAN_POINT('Ctrl Pts',(-0.249151443489066,0.425772280374832,
-0.905744519768896));
#69933=CARTESIAN_POINT('Ctrl Pts',(-0.390043706876331,0.343325600735486,
-0.897795125749484));
#69934=CARTESIAN_POINT('Ctrl Pts',(-0.485951313598522,0.184005114619417,
-0.889845731730073));
#69935=CARTESIAN_POINT('Ctrl Pts',(-0.492870442726711,0.0209094049332138,
-0.881896337710662));
#69936=CARTESIAN_POINT('Ctrl Pts',(-0.493164110375336,0.0139871560956824,
-0.88155894267056));
#69937=CARTESIAN_POINT('Ctrl Pts',(-0.493297474482374,0.00705810658322154,
-0.881221547630459));
#69938=CARTESIAN_POINT('Ctrl Pts',(-0.493273413985951,0.000128110117115081,
-0.880884152590357));
#69939=CARTESIAN_POINT('Origin',(0.,0.,-1.725));
#69940=CARTESIAN_POINT('',(-0.492120428308753,0.000409080293566094,-0.709115847409639));
#69941=CARTESIAN_POINT('',(-0.492044152078047,0.000384352874199066,-0.730884152590357));
#69942=CARTESIAN_POINT('',(-0.4925,-6.03138548580071E-17,-1.725));
#69943=CARTESIAN_POINT('Ctrl Pts',(-0.492120428308753,0.000409080293566094,
-0.709115847409639));
#69944=CARTESIAN_POINT('Ctrl Pts',(-0.492523321585198,0.0519416275023631,
-0.71160965816936));
#69945=CARTESIAN_POINT('Ctrl Pts',(-0.485074880445966,0.103360635220992,
-0.714103468929082));
#69946=CARTESIAN_POINT('Ctrl Pts',(-0.469287724172531,0.152077398581539,
-0.716597279688803));
#69947=CARTESIAN_POINT('Ctrl Pts',(-0.418963807181502,0.307369353191063,
-0.724546673708215));
#69948=CARTESIAN_POINT('Ctrl Pts',(-0.283909306830873,0.435203511586707,
-0.732496067727626));
#69949=CARTESIAN_POINT('Ctrl Pts',(-0.126089214777759,0.476927681237711,
-0.740445461747037));
#69950=CARTESIAN_POINT('Ctrl Pts',(0.0317308772753556,0.518651850888716,
-0.748394855766449));
#69951=CARTESIAN_POINT('Ctrl Pts',(0.212316561030953,0.474266031795081,
-0.756344249785862));
#69952=CARTESIAN_POINT('Ctrl Pts',(0.332812468065237,0.36413509074818,-0.764293643805273));
#69953=CARTESIAN_POINT('Ctrl Pts',(0.453308375099515,0.254004149701284,
-0.772243037824685));
#69954=CARTESIAN_POINT('Ctrl Pts',(0.513714505412483,0.078128086701122,
-0.780192431844096));
#69955=CARTESIAN_POINT('Ctrl Pts',(0.486315637735422,-0.0827985731104579,
-0.788141825863507));
#69956=CARTESIAN_POINT('Ctrl Pts',(0.45891677005836,-0.243725232922049,
-0.796091219882918));
#69957=CARTESIAN_POINT('Ctrl Pts',(0.343712904391259,-0.389702489545059,
-0.80404061390233));
#69958=CARTESIAN_POINT('Ctrl Pts',(0.193561269149825,-0.453753830066015,
-0.811990007921742));
#69959=CARTESIAN_POINT('Ctrl Pts',(0.0434096339083948,-0.517805170586969,
-0.819939401941154));
#69960=CARTESIAN_POINT('Ctrl Pts',(-0.141689770907357,-0.499930595005874,
-0.827888795960565));
#69961=CARTESIAN_POINT('Ctrl Pts',(-0.276810615240517,-0.408331221564878,
-0.835838189979976));
#69962=CARTESIAN_POINT('Ctrl Pts',(-0.408698937726213,-0.318923197484696,
-0.843597409123197));
#69963=CARTESIAN_POINT('Ctrl Pts',(-0.492971389400891,-0.159275646363948,
-0.851356628266418));
#69964=CARTESIAN_POINT('Ctrl Pts',(-0.493300545452038,7.30209052610606E-5,
-0.859115847409639));
#69965=CARTESIAN_POINT('Ctrl Pts',(-0.493273413985951,0.000128110117115081,
-0.880884152590357));
#69966=CARTESIAN_POINT('Ctrl Pts',(-0.492730583023898,-0.156220145656787,
-0.873272153611047));
#69967=CARTESIAN_POINT('Ctrl Pts',(-0.412058209599762,-0.313050403358555,
-0.865660154631737));
#69968=CARTESIAN_POINT('Ctrl Pts',(-0.284317021785768,-0.403140555701278,
-0.858048155652426));
#69969=CARTESIAN_POINT('Ctrl Pts',(-0.150913820182463,-0.49722387339321,
-0.850098761633015));
#69970=CARTESIAN_POINT('Ctrl Pts',(0.0338232345583237,-0.518519575520737,
-0.842149367613603));
#69971=CARTESIAN_POINT('Ctrl Pts',(0.185134063923977,-0.457256880651614,
-0.834199973594192));
#69972=CARTESIAN_POINT('Ctrl Pts',(0.33644489328963,-0.395994185782491,
-0.826250579574781));
#69973=CARTESIAN_POINT('Ctrl Pts',(0.454329497280149,-0.252173093916718,
-0.81830118555537));
#69974=CARTESIAN_POINT('Ctrl Pts',(0.484700685300486,-0.0917808378562355,
-0.810351791535958));
#69975=CARTESIAN_POINT('Ctrl Pts',(0.515071873320824,0.068611418204249,
-0.802402397516546));
#69976=CARTESIAN_POINT('Ctrl Pts',(0.457929645370978,0.245574838459443,
-0.794453003497134));
#69977=CARTESIAN_POINT('Ctrl Pts',(0.33949169629466,0.35791600226193,-0.786503609477722));
#69978=CARTESIAN_POINT('Ctrl Pts',(0.221053747218343,0.470257166064418,
-0.778554215458311));
#69979=CARTESIAN_POINT('Ctrl Pts',(0.0413200770155548,0.517976073414199,
-0.7706048214389));
#69980=CARTESIAN_POINT('Ctrl Pts',(-0.11724486223632,0.47917858759271,-0.762655427419488));
#69981=CARTESIAN_POINT('Ctrl Pts',(-0.275809801488195,0.440381101771221,
-0.754706033400077));
#69982=CARTESIAN_POINT('Ctrl Pts',(-0.413206009789156,0.315067222778461,
-0.746756639380665));
#69983=CARTESIAN_POINT('Ctrl Pts',(-0.466394085435827,0.16073280187724,
-0.738807245361253));
#69984=CARTESIAN_POINT('Ctrl Pts',(-0.484064784888934,0.109458204444321,
-0.736166214437621));
#69985=CARTESIAN_POINT('Ctrl Pts',(-0.492440836022914,0.0549804041547731,
-0.733525183513989));
#69986=CARTESIAN_POINT('Ctrl Pts',(-0.492044152078047,0.000384352874199066,
-0.730884152590357));
#69987=CARTESIAN_POINT('Origin',(0.,0.,-1.725));
#69988=CARTESIAN_POINT('',(-0.491829192176605,-0.000264117888597593,-0.559115847409639));
#69989=CARTESIAN_POINT('',(-0.491882295318969,-0.000303616531414571,-0.580884152590356));
#69990=CARTESIAN_POINT('',(-0.4925,-6.03138548580071E-17,-1.725));
#69991=CARTESIAN_POINT('Ctrl Pts',(-0.491829192176605,-0.000264117888597593,
-0.559115847409639));
#69992=CARTESIAN_POINT('Ctrl Pts',(-0.491347407742035,0.0990187616593992,
-0.563913294052891));
#69993=CARTESIAN_POINT('Ctrl Pts',(-0.462209103339611,0.198561720702376,
-0.568710740696144));
#69994=CARTESIAN_POINT('Ctrl Pts',(-0.406349763901535,0.27971123101388,
-0.573508187339396));
#69995=CARTESIAN_POINT('Ctrl Pts',(-0.313790548160828,0.414176391320723,
-0.581457581358807));
#69996=CARTESIAN_POINT('Ctrl Pts',(-0.147864289096749,0.498139280733203,
-0.589406975378218));
#69997=CARTESIAN_POINT('Ctrl Pts',(0.0152996038830409,0.493076490352761,
-0.597356369397629));
#69998=CARTESIAN_POINT('Ctrl Pts',(0.178463496862833,0.488013699972319,
-0.605305763417041));
#69999=CARTESIAN_POINT('Ctrl Pts',(0.338865023758333,0.393925229798948,
-0.613255157436453));
#70000=CARTESIAN_POINT('Ctrl Pts',(0.422909604609079,0.253980254149587,
-0.621204551455865));
#70001=CARTESIAN_POINT('Ctrl Pts',(0.506954185459824,0.114035278500226,
-0.629153945475276));
#70002=CARTESIAN_POINT('Ctrl Pts',(0.514641820265816,-0.0717662026251266,
-0.637103339494688));
#70003=CARTESIAN_POINT('Ctrl Pts',(0.442445308892405,-0.218175736228549,
-0.645052733514099));
#70004=CARTESIAN_POINT('Ctrl Pts',(0.370248797518995,-0.36458526983197,
-0.653002127533511));
#70005=CARTESIAN_POINT('Ctrl Pts',(0.21816813996618,-0.471602855913464,
-0.660951521552923));
#70006=CARTESIAN_POINT('Ctrl Pts',(0.0559801793831442,-0.490127251567516,
-0.668900915572334));
#70007=CARTESIAN_POINT('Ctrl Pts',(-0.106207781199894,-0.508651647221568,
-0.676850309591746));
#70008=CARTESIAN_POINT('Ctrl Pts',(-0.278503044813152,-0.43868285244818,
-0.684799703611157));
#70009=CARTESIAN_POINT('Ctrl Pts',(-0.381854009804069,-0.312323579649783,
-0.692749097630568));
#70010=CARTESIAN_POINT('Ctrl Pts',(-0.452782660856013,-0.225604575446169,
-0.698204680890258));
#70011=CARTESIAN_POINT('Ctrl Pts',(-0.491239039131227,-0.112326058403522,
-0.703660264149949));
#70012=CARTESIAN_POINT('Ctrl Pts',(-0.492120428308753,0.000409080293566094,
-0.709115847409639));
#70013=CARTESIAN_POINT('Ctrl Pts',(-0.492044152078047,0.000384352874199066,
-0.730884152590357));
#70014=CARTESIAN_POINT('Ctrl Pts',(-0.491246833729828,-0.109351455669271,
-0.725575789494578));
#70015=CARTESIAN_POINT('Ctrl Pts',(-0.455008244691688,-0.219564990411542,
-0.720267426398799));
#70016=CARTESIAN_POINT('Ctrl Pts',(-0.387566372929823,-0.30520613214935,
-0.714959063303019));
#70017=CARTESIAN_POINT('Ctrl Pts',(-0.286570641784764,-0.433455682465039,
-0.707009669283608));
#70018=CARTESIAN_POINT('Ctrl Pts',(-0.115599236502264,-0.506599820286735,
-0.699060275264196));
#70019=CARTESIAN_POINT('Ctrl Pts',(0.0469036468997333,-0.491078939107802,
-0.691110881244785));
#70020=CARTESIAN_POINT('Ctrl Pts',(0.209406530301733,-0.47555805792887,
-0.683161487225373));
#70021=CARTESIAN_POINT('Ctrl Pts',(0.363440891823226,-0.371372157749306,
-0.675212093205962));
#70022=CARTESIAN_POINT('Ctrl Pts',(0.438333500275854,-0.226323262321803,
-0.66726269918655));
#70023=CARTESIAN_POINT('Ctrl Pts',(0.513226108728484,-0.0812743668942985,
-0.659313305167138));
#70024=CARTESIAN_POINT('Ctrl Pts',(0.508976964112243,0.104637523781151,
-0.651363911147726));
#70025=CARTESIAN_POINT('Ctrl Pts',(0.427535636515494,0.246113299176732,
-0.643414517128314));
#70026=CARTESIAN_POINT('Ctrl Pts',(0.346094308918747,0.38758907457231,-0.635465123108903));
#70027=CARTESIAN_POINT('Ctrl Pts',(0.187460798341501,0.484628734688026,
-0.627515729089492));
#70028=CARTESIAN_POINT('Ctrl Pts',(0.0244184931561698,0.492709055851996,
-0.619566335070081));
#70029=CARTESIAN_POINT('Ctrl Pts',(-0.138623812029161,0.500789377015965,
-0.611616941050669));
#70030=CARTESIAN_POINT('Ctrl Pts',(-0.306074911822575,0.419910359228188,
-0.603667547031257));
#70031=CARTESIAN_POINT('Ctrl Pts',(-0.401105778050425,0.287180485702124,
-0.595718153011846));
#70032=CARTESIAN_POINT('Ctrl Pts',(-0.46021669502666,0.204620104578649,
-0.590773486204682));
#70033=CARTESIAN_POINT('Ctrl Pts',(-0.49130775347213,0.101998290745618,
-0.585828819397519));
#70034=CARTESIAN_POINT('Ctrl Pts',(-0.491882295318969,-0.000303616531414571,
-0.580884152590356));
#70035=CARTESIAN_POINT('Origin',(0.,0.,-1.725));
#70036=CARTESIAN_POINT('',(-0.493088042785032,-0.000296614551317576,-0.409115847409638));
#70037=CARTESIAN_POINT('',(-0.493153848081098,-0.000252729816838331,-0.430884152590357));
#70038=CARTESIAN_POINT('',(-0.4925,-6.03138548580071E-17,-1.725));
#70039=CARTESIAN_POINT('Ctrl Pts',(-0.493088042785032,-0.000296614551317576,
-0.409115847409638));
#70040=CARTESIAN_POINT('Ctrl Pts',(-0.492051112040595,0.145702757819977,
-0.416216929936422));
#70041=CARTESIAN_POINT('Ctrl Pts',(-0.42312608138996,0.292552439531534,
-0.423318012463205));
#70042=CARTESIAN_POINT('Ctrl Pts',(-0.309596575789553,0.384068313855645,
-0.430419094989988));
#70043=CARTESIAN_POINT('Ctrl Pts',(-0.18250457686648,0.486516882970195,
-0.438368489009399));
#70044=CARTESIAN_POINT('Ctrl Pts',(0.000485562329820693,0.51962135755884,
-0.446317883028811));
#70045=CARTESIAN_POINT('Ctrl Pts',(0.155415239341919,0.468192917728478,
-0.454267277048222));
#70046=CARTESIAN_POINT('Ctrl Pts',(0.310344916354022,0.416764477898114,
-0.462216671067634));
#70047=CARTESIAN_POINT('Ctrl Pts',(0.437214131181918,0.280803123648739,
-0.470166065087045));
#70048=CARTESIAN_POINT('Ctrl Pts',(0.477813439574123,0.122689924496489,
-0.478115459106457));
#70049=CARTESIAN_POINT('Ctrl Pts',(0.518412747966327,-0.035423274655759,
-0.486064853125868));
#70050=CARTESIAN_POINT('Ctrl Pts',(0.472742149922838,-0.215688318710885,
-0.49401424714528));
#70051=CARTESIAN_POINT('Ctrl Pts',(0.361755978352945,-0.335396953430194,
-0.501963641164691));
#70052=CARTESIAN_POINT('Ctrl Pts',(0.250769806783051,-0.455105588149505,
-0.509913035184103));
#70053=CARTESIAN_POINT('Ctrl Pts',(0.0744680616867539,-0.514257813533002,
-0.517862429203515));
#70054=CARTESIAN_POINT('Ctrl Pts',(-0.0862594177059559,-0.485713718354565,
-0.525811823222927));
#70055=CARTESIAN_POINT('Ctrl Pts',(-0.246986897098666,-0.457169623176128,
-0.533761217242338));
#70056=CARTESIAN_POINT('Ctrl Pts',(-0.392140110787785,-0.340929207435757,
-0.541710611261749));
#70057=CARTESIAN_POINT('Ctrl Pts',(-0.45512063142368,-0.190325283964967,
-0.549660005281161));
#70058=CARTESIAN_POINT('Ctrl Pts',(-0.480092508057637,-0.130610588698395,
-0.55281195265732));
#70059=CARTESIAN_POINT('Ctrl Pts',(-0.492145727053872,-0.0654934857084591,
-0.55596390003348));
#70060=CARTESIAN_POINT('Ctrl Pts',(-0.491829192176605,-0.000264117888597593,
-0.559115847409639));
#70061=CARTESIAN_POINT('Ctrl Pts',(-0.491882295318969,-0.000303616531414571,
-0.580884152590356));
#70062=CARTESIAN_POINT('Ctrl Pts',(-0.492231427341226,-0.0624694482543762,
-0.577879425378108));
#70063=CARTESIAN_POINT('Ctrl Pts',(-0.481311932613635,-0.124517150256906,
-0.57487469816586));
#70064=CARTESIAN_POINT('Ctrl Pts',(-0.458563585316289,-0.181873347975683,
-0.571869970953611));
#70065=CARTESIAN_POINT('Ctrl Pts',(-0.398379893692015,-0.333616578863071,
-0.5639205769342));
#70066=CARTESIAN_POINT('Ctrl Pts',(-0.255401877781181,-0.452522311373495,
-0.555971182914788));
#70067=CARTESIAN_POINT('Ctrl Pts',(-0.0952299543786173,-0.484034846183981,
-0.548021788895376));
#70068=CARTESIAN_POINT('Ctrl Pts',(0.0649419690239445,-0.515547380994467,
-0.540072394875965));
#70069=CARTESIAN_POINT('Ctrl Pts',(0.242307799918234,-0.459666718105021,
-0.532123000856554));
#70070=CARTESIAN_POINT('Ctrl Pts',(0.355489485052551,-0.342031727635589,
-0.524173606837142));
#70071=CARTESIAN_POINT('Ctrl Pts',(0.468671170186871,-0.224396737166155,
-0.516224212817731));
#70072=CARTESIAN_POINT('Ctrl Pts',(0.517668709561212,-0.0450074191167323,
-0.508274818798319));
#70073=CARTESIAN_POINT('Ctrl Pts',(0.48000131258373,0.113829768049986,-0.500325424778908));
#70074=CARTESIAN_POINT('Ctrl Pts',(0.442333915606249,0.272666955216704,
-0.492376030759496));
#70075=CARTESIAN_POINT('Ctrl Pts',(0.318001582276944,0.410952011500721,
-0.484426636740084));
#70076=CARTESIAN_POINT('Ctrl Pts',(0.164049813753438,0.465237719088328,
-0.476477242720673));
#70077=CARTESIAN_POINT('Ctrl Pts',(0.0100980452299302,0.519523426675936,
-0.468527848701261));
#70078=CARTESIAN_POINT('Ctrl Pts',(-0.173473158487775,0.489809785567135,
-0.46057845468185));
#70079=CARTESIAN_POINT('Ctrl Pts',(-0.302438623662206,0.389729850637384,
-0.452629060662438));
#70080=CARTESIAN_POINT('Ctrl Pts',(-0.42003006848778,0.298476396617569,
-0.445380757971745));
#70081=CARTESIAN_POINT('Ctrl Pts',(-0.492222869400628,0.148721136709646,
-0.438132455281051));
#70082=CARTESIAN_POINT('Ctrl Pts',(-0.493153848081098,-0.00025272981683833,
-0.430884152590357));
#70083=CARTESIAN_POINT('Origin',(0.,0.,-1.725));
#70084=CARTESIAN_POINT('',(-0.492748795109349,0.000423665976190507,-0.259115847409639));
#70085=CARTESIAN_POINT('',(-0.492657439364267,0.000439738527351781,-0.280884152590357));
#70086=CARTESIAN_POINT('',(-0.4925,-6.03138548580071E-17,-1.725));
#70087=CARTESIAN_POINT('Ctrl Pts',(-0.492748795109349,0.000423665976190507,
-0.259115847409639));
#70088=CARTESIAN_POINT('Ctrl Pts',(-0.493021314980458,0.0303989720533546,
-0.260571171800541));
#70089=CARTESIAN_POINT('Ctrl Pts',(-0.490521432313287,0.0603288797091717,
-0.262026496191444));
#70090=CARTESIAN_POINT('Ctrl Pts',(-0.485086207269442,0.0897158849497183,
-0.263481820582346));
#70091=CARTESIAN_POINT('Ctrl Pts',(-0.455397468643341,0.250236030951502,
-0.271431214601757));
#70092=CARTESIAN_POINT('Ctrl Pts',(-0.33812827529867,0.394557848344311,
-0.279380608621169));
#70093=CARTESIAN_POINT('Ctrl Pts',(-0.187080149952232,0.456464357226385,
-0.28733000264058));
#70094=CARTESIAN_POINT('Ctrl Pts',(-0.0360320246057905,0.51837086610846,
-0.295279396659992));
#70095=CARTESIAN_POINT('Ctrl Pts',(0.148795032742419,0.497862066479795,
-0.303228790679403));
#70096=CARTESIAN_POINT('Ctrl Pts',(0.282597925207516,0.404347700904736,
-0.311178184698815));
#70097=CARTESIAN_POINT('Ctrl Pts',(0.416400817672612,0.310833335329677,
-0.319127578718226));
#70098=CARTESIAN_POINT('Ctrl Pts',(0.499179545254594,0.144313403808224,
-0.327076972737638));
#70099=CARTESIAN_POINT('Ctrl Pts',(0.492954908135233,-0.0188103011477814,
-0.335026366757049));
#70100=CARTESIAN_POINT('Ctrl Pts',(0.486730271015873,-0.181934006103787,
-0.342975760776461));
#70101=CARTESIAN_POINT('Ctrl Pts',(0.391502269195169,-0.341661484494344,
-0.350925154795873));
#70102=CARTESIAN_POINT('Ctrl Pts',(0.250962442861246,-0.424707418399116,
-0.358874548815284));
#70103=CARTESIAN_POINT('Ctrl Pts',(0.110422616527323,-0.507753352303887,
-0.366823942834696));
#70104=CARTESIAN_POINT('Ctrl Pts',(-0.07542903431982,-0.514117741722873,
-0.374773336854107));
#70105=CARTESIAN_POINT('Ctrl Pts',(-0.221320794217617,-0.440880511665361,
-0.382722730873519));
#70106=CARTESIAN_POINT('Ctrl Pts',(-0.367212554115415,-0.367643281607849,
-0.39067212489293));
#70107=CARTESIAN_POINT('Ctrl Pts',(-0.473144423063867,-0.214804432073841,
-0.398621518912342));
#70108=CARTESIAN_POINT('Ctrl Pts',(-0.490513428213171,-0.0524886754866058,
-0.406570912931754));
#70109=CARTESIAN_POINT('Ctrl Pts',(-0.492366943921122,-0.0351673147122667,
-0.407419224424382));
#70110=CARTESIAN_POINT('Ctrl Pts',(-0.493211916893557,-0.0177380321143359,
-0.40826753591701));
#70111=CARTESIAN_POINT('Ctrl Pts',(-0.493088042785032,-0.000296614551317576,
-0.409115847409638));
#70112=CARTESIAN_POINT('Ctrl Pts',(-0.493153848081098,-0.00025272981683833,
-0.430884152590357));
#70113=CARTESIAN_POINT('Ctrl Pts',(-0.493243896897759,-0.014662211661654,
-0.430183061261639));
#70114=CARTESIAN_POINT('Ctrl Pts',(-0.492667241082679,-0.0290643830200086,
-0.429481969932921));
#70115=CARTESIAN_POINT('Ctrl Pts',(-0.491400476278679,-0.0434055967665068,
-0.428780878604204));
#70116=CARTESIAN_POINT('Ctrl Pts',(-0.477037137089573,-0.206014880489943,
-0.420831484584792));
#70117=CARTESIAN_POINT('Ctrl Pts',(-0.373950732080215,-0.360787219186121,
-0.412882090565381));
#70118=CARTESIAN_POINT('Ctrl Pts',(-0.229438802677289,-0.436710789854924,
-0.40493269654597));
#70119=CARTESIAN_POINT('Ctrl Pts',(-0.0849268732743565,-0.512634360523731,
-0.396983302526558));
#70120=CARTESIAN_POINT('Ctrl Pts',(0.101010580522155,-0.509709163165152,
-0.389033908507146));
#70121=CARTESIAN_POINT('Ctrl Pts',(0.243062685356905,-0.429277315683624,
-0.381084514487734));
#70122=CARTESIAN_POINT('Ctrl Pts',(0.385114790191649,-0.3488454682021,-0.373135120468323));
#70123=CARTESIAN_POINT('Ctrl Pts',(0.483281546064643,-0.190906970597636,
-0.365185726448912));
#70124=CARTESIAN_POINT('Ctrl Pts',(0.492522666606163,-0.027926340012255,
-0.3572363324295));
#70125=CARTESIAN_POINT('Ctrl Pts',(0.501763787147683,0.13505429057313,-0.349286938410089));
#70126=CARTESIAN_POINT('Ctrl Pts',(0.422079272357724,0.303077054139432,
-0.341337544390677));
#70127=CARTESIAN_POINT('Ctrl Pts',(0.290029424374363,0.399050655768452,
-0.333388150371265));
#70128=CARTESIAN_POINT('Ctrl Pts',(0.157979576391001,0.495024257397473,
-0.325438756351854));
#70129=CARTESIAN_POINT('Ctrl Pts',(-0.0264356047857588,0.518948697089211,
-0.317489362332442));
#70130=CARTESIAN_POINT('Ctrl Pts',(-0.178603480069354,0.45984704982415,
-0.309539968313031));
#70131=CARTESIAN_POINT('Ctrl Pts',(-0.330771355352949,0.40074540255909,
-0.301590574293619));
#70132=CARTESIAN_POINT('Ctrl Pts',(-0.450691924743376,0.258617668337232,
-0.293641180274208));
#70133=CARTESIAN_POINT('Ctrl Pts',(-0.48334432902377,0.0986742195455115,
-0.285691786254796));
#70134=CARTESIAN_POINT('Ctrl Pts',(-0.489926834879352,0.0664306922636456,
-0.284089241699983));
#70135=CARTESIAN_POINT('Ctrl Pts',(-0.492962774926304,0.0334631368774868,
-0.28248669714517));
#70136=CARTESIAN_POINT('Ctrl Pts',(-0.492657439364267,0.000439738527351781,
-0.280884152590357));
#70137=CARTESIAN_POINT('Origin',(0.,0.,-1.725));
#70138=CARTESIAN_POINT('',(-0.491761526237315,7.34498668767403E-5,-0.109115847409639));
#70139=CARTESIAN_POINT('',(-0.491698555522654,2.49815306513942E-5,-0.130884152590357));
#70140=CARTESIAN_POINT('',(-0.4925,-6.03138548580071E-17,-1.725));
#70141=CARTESIAN_POINT('Ctrl Pts',(-0.491761526237315,7.34498668767403E-5,
-0.109115847409639));
#70142=CARTESIAN_POINT('Ctrl Pts',(-0.491825690633276,0.0779166216940231,
-0.112874807684072));
#70143=CARTESIAN_POINT('Ctrl Pts',(-0.474387552418018,0.155716209514715,
-0.116633767958505));
#70144=CARTESIAN_POINT('Ctrl Pts',(-0.439245516028347,0.224454403316697,
-0.120392728232938));
#70145=CARTESIAN_POINT('Ctrl Pts',(-0.364927653238976,0.369820926722449,
-0.12834212225235));
#70146=CARTESIAN_POINT('Ctrl Pts',(-0.211432346318084,0.474662023942289,
-0.136291516271761));
#70147=CARTESIAN_POINT('Ctrl Pts',(-0.049019555660165,0.490874829170351,
-0.144240910291172));
#70148=CARTESIAN_POINT('Ctrl Pts',(0.113393234997754,0.507087634398413,
-0.152190304310584));
#70149=CARTESIAN_POINT('Ctrl Pts',(0.284723509392699,0.434672147634697,
-0.160139698329996));
#70150=CARTESIAN_POINT('Ctrl Pts',(0.38627620605837,0.306853825701618,-0.168089092349407));
#70151=CARTESIAN_POINT('Ctrl Pts',(0.48782890272404,0.17903550376854,-0.176038486368819));
#70152=CARTESIAN_POINT('Ctrl Pts',(0.519604021660437,-0.00418565333390042,
-0.18398788038823));
#70153=CARTESIAN_POINT('Ctrl Pts',(0.46706756334537,-0.158745174957354,
-0.191937274407642));
#70154=CARTESIAN_POINT('Ctrl Pts',(0.414531105030304,-0.313304696580808,
-0.199886668427054));
#70155=CARTESIAN_POINT('Ctrl Pts',(0.277683069463775,-0.439202582725276,
-0.207836062446465));
#70156=CARTESIAN_POINT('Ctrl Pts',(0.119287960412537,-0.478674982698152,
-0.215785456465877));
#70157=CARTESIAN_POINT('Ctrl Pts',(-0.039107148638701,-0.518147382671028,
-0.223734850485288));
#70158=CARTESIAN_POINT('Ctrl Pts',(-0.219049331174648,-0.471194296472313,
-0.2316842445047));
#70159=CARTESIAN_POINT('Ctrl Pts',(-0.337966280488859,-0.359358516067573,
-0.239633638524111));
#70160=CARTESIAN_POINT('Ctrl Pts',(-0.435112672650402,-0.267996917544017,
-0.24612770815262));
#70161=CARTESIAN_POINT('Ctrl Pts',(-0.491532734257764,-0.133334639744414,
-0.25262177778113));
#70162=CARTESIAN_POINT('Ctrl Pts',(-0.492748795109349,0.000423665976190507,
-0.259115847409639));
#70163=CARTESIAN_POINT('Ctrl Pts',(-0.492657439364267,0.000439738527351781,
-0.280884152590357));
#70164=CARTESIAN_POINT('Ctrl Pts',(-0.491448163252337,-0.130348848603208,
-0.274537303125758));
#70165=CARTESIAN_POINT('Ctrl Pts',(-0.437829573728453,-0.262013356113694,
-0.26819045366116));
#70166=CARTESIAN_POINT('Ctrl Pts',(-0.344554674086439,-0.353044898970412,
-0.261843604196561));
#70167=CARTESIAN_POINT('Ctrl Pts',(-0.227728375698354,-0.467061405333034,
-0.25389421017715));
#70168=CARTESIAN_POINT('Ctrl Pts',(-0.0486915397518234,-0.517335254696698,
-0.245944816157738));
#70169=CARTESIAN_POINT('Ctrl Pts',(0.110409397431204,-0.480799781899208,
-0.237995422138326));
#70170=CARTESIAN_POINT('Ctrl Pts',(0.269510334614231,-0.444264309101718,
-0.230046028118915));
#70171=CARTESIAN_POINT('Ctrl Pts',(0.408675373033755,-0.320919514143075,
-0.222096634099504));
#70172=CARTESIAN_POINT('Ctrl Pts',(0.46405681172168,-0.167358347485203,
-0.214147240080092));
#70173=CARTESIAN_POINT('Ctrl Pts',(0.519438250409602,-0.0137971808273366,
-0.206197846060681));
#70174=CARTESIAN_POINT('Ctrl Pts',(0.491036089365932,0.169980357529756,
-0.198248452041269));
#70175=CARTESIAN_POINT('Ctrl Pts',(0.391875390863108,0.299655473021211,
-0.190299058021858));
#70176=CARTESIAN_POINT('Ctrl Pts',(0.292714692360281,0.429330588512671,
-0.182349664002446));
#70177=CARTESIAN_POINT('Ctrl Pts',(0.122795456398295,0.50490328113849,-0.174400269983035));
#70178=CARTESIAN_POINT('Ctrl Pts',(-0.0399088460306932,0.491697684968673,
-0.166450875963623));
#70179=CARTESIAN_POINT('Ctrl Pts',(-0.202613148459681,0.478492088798855,
-0.158501481944212));
#70180=CARTESIAN_POINT('Ctrl Pts',(-0.358102517355672,0.376508203833402,
-0.1505520879248));
#70181=CARTESIAN_POINT('Ctrl Pts',(-0.435059219194714,0.232541579850291,
-0.142602693905388));
#70182=CARTESIAN_POINT('Ctrl Pts',(-0.472874273095562,0.161799129670568,
-0.138696513467045));
#70183=CARTESIAN_POINT('Ctrl Pts',(-0.491727206546983,0.0809197290486493,
-0.134790333028701));
#70184=CARTESIAN_POINT('Ctrl Pts',(-0.491698555522654,2.49815306513942E-5,
-0.130884152590357));
#70185=CARTESIAN_POINT('Origin',(0.,0.,-3.73478126690739));
#70186=CARTESIAN_POINT('',(-0.40643965330944,6.07061285855456E-5,-0.0597812669073879));
#70187=CARTESIAN_POINT('',(-0.406892273398771,-0.000115106065058088,-0.0302187330926113));
#70188=CARTESIAN_POINT('',(-0.40705,-1.06687458785308E-14,-3.73478126690739));
#70189=CARTESIAN_POINT('',(-0.0460018146225333,-0.405020972964472,-0.0249999999999997));
#70190=CARTESIAN_POINT('Ctrl Pts',(-0.40643965330944,6.07061285855248E-5,
-0.0597812669073879));
#70191=CARTESIAN_POINT('Ctrl Pts',(-0.406380534337011,-0.0716614422772074,
-0.0555908331624084));
#70192=CARTESIAN_POINT('Ctrl Pts',(-0.356479421834089,-0.270220379709696,
-0.0439970775266123));
#70193=CARTESIAN_POINT('Ctrl Pts',(-0.170735417371495,-0.390082040693776,
-0.0324033218908163));
#70194=CARTESIAN_POINT('Ctrl Pts',(-0.0460018146225332,-0.405020972964472,
-0.0249999999999997));
#70195=CARTESIAN_POINT('',(-0.39736287274916,-0.0882748540669144,-0.0249999999999999));
#70196=CARTESIAN_POINT('Origin',(0.,0.,-0.0249999999999999));
#70197=CARTESIAN_POINT('Ctrl Pts',(-0.406892273398771,-0.000115106065058105,
-0.0302187330926113));
#70198=CARTESIAN_POINT('Ctrl Pts',(-0.406947232354318,-0.029718523814811,
-0.0284791553950742));
#70199=CARTESIAN_POINT('Ctrl Pts',(-0.40379521950949,-0.0593201102248456,
-0.0267395776975371));
#70200=CARTESIAN_POINT('Ctrl Pts',(-0.39736287274916,-0.0882748540669144,
-0.0249999999999999));
#70201=CARTESIAN_POINT('Origin',(0.,0.,-3.73478126690739));
#70202=CARTESIAN_POINT('',(-0.407255628526418,0.000350158854048321,-0.209781266907387));
#70203=CARTESIAN_POINT('',(-0.406387608173597,2.06471716764911E-5,-0.180218733092611));
#70204=CARTESIAN_POINT('',(-0.40705,-1.06687458785308E-14,-3.73478126690739));
#70205=CARTESIAN_POINT('Ctrl Pts',(-0.407255628526418,0.000350158854048318,
-0.209781266907387));
#70206=CARTESIAN_POINT('Ctrl Pts',(-0.406250557319037,-0.110200741335954,
-0.203287197278877));
#70207=CARTESIAN_POINT('Ctrl Pts',(-0.302538442003538,-0.357738749730799,
-0.188843733630956));
#70208=CARTESIAN_POINT('Ctrl Pts',(0.116399798066751,-0.467054103255692,
-0.166450875963623));
#70209=CARTESIAN_POINT('Ctrl Pts',(0.45571346026384,-0.154891253173831,
-0.142602693905389));
#70210=CARTESIAN_POINT('Ctrl Pts',(0.376927294803572,0.299404210776717,
-0.118754511847154));
#70211=CARTESIAN_POINT('Ctrl Pts',(-0.0478848160134567,0.478957858820396,
-0.094906329788919));
#70212=CARTESIAN_POINT('Ctrl Pts',(-0.361600601784404,0.264682205348061,
-0.075248581475664));
#70213=CARTESIAN_POINT('Ctrl Pts',(-0.406492685019843,0.0643978900722083,
-0.0635402271818201));
#70214=CARTESIAN_POINT('Ctrl Pts',(-0.40643965330944,6.07061285855248E-5,
-0.0597812669073879));
#70215=CARTESIAN_POINT('Ctrl Pts',(-0.406387608173597,2.06471716765189E-5,
-0.180218733092611));
#70216=CARTESIAN_POINT('Ctrl Pts',(-0.406363097454078,-0.069184154866318,
-0.176175519511543));
#70217=CARTESIAN_POINT('Ctrl Pts',(-0.356697934417019,-0.27449337105559,
-0.164182911911064));
#70218=CARTESIAN_POINT('Ctrl Pts',(-0.0305910094676718,-0.480372488794092,
-0.144240910291172));
#70219=CARTESIAN_POINT('Ctrl Pts',(0.387186688863383,-0.285728547318658,
-0.120392728232938));
#70220=CARTESIAN_POINT('Ctrl Pts',(0.450204815655376,0.171019861124231,
-0.0965445461747034));
#70221=CARTESIAN_POINT('Ctrl Pts',(0.0990560712614088,0.471004678905531,
-0.0726963641164688));
#70222=CARTESIAN_POINT('Ctrl Pts',(-0.267488470034939,0.360553837565826,
-0.0528228790679404));
#70223=CARTESIAN_POINT('Ctrl Pts',(-0.391916341648465,0.143605734703497,
-0.038663668726654));
#70224=CARTESIAN_POINT('Ctrl Pts',(-0.406821658661013,0.0379212350609192,
-0.0324538524047797));
#70225=CARTESIAN_POINT('Ctrl Pts',(-0.406892273398771,-0.000115106065058105,
-0.0302187330926113));
#70226=CARTESIAN_POINT('Origin',(0.,0.,-3.73478126690739));
#70227=CARTESIAN_POINT('',(-0.407536015869335,-0.000245151173813718,-0.359781266907386));
#70228=CARTESIAN_POINT('',(-0.407180123234974,0.000363442776755235,-0.33021873309261));
#70229=CARTESIAN_POINT('',(-0.40705,-1.06687458785308E-14,-3.73478126690739));
#70230=CARTESIAN_POINT('Ctrl Pts',(-0.407536015869335,-0.000245151173813667,
-0.359781266907386));
#70231=CARTESIAN_POINT('Ctrl Pts',(-0.40763839750563,-0.0146604385220988,
-0.358932955414758));
#70232=CARTESIAN_POINT('Ctrl Pts',(-0.400395732273573,-0.164055109369366,
-0.350135249902717));
#70233=CARTESIAN_POINT('Ctrl Pts',(-0.215947823141546,-0.43017716036811,
-0.333388150371265));
#70234=CARTESIAN_POINT('Ctrl Pts',(0.244869930019852,-0.41439670526355,
-0.309539968313031));
#70235=CARTESIAN_POINT('Ctrl Pts',(0.480987035447976,-0.0183536387932365,
-0.285691786254796));
#70236=CARTESIAN_POINT('Ctrl Pts',(0.275737810703329,0.394531263495945,
-0.261843604196561));
#70237=CARTESIAN_POINT('Ctrl Pts',(-0.182539470678933,0.445382676016845,
-0.237995422138327));
#70238=CARTESIAN_POINT('Ctrl Pts',(-0.394128840463536,0.184982126500309,
-0.220641309708602));
#70239=CARTESIAN_POINT('Ctrl Pts',(-0.407480865508213,0.0251246732473596,
-0.211236591298289));
#70240=CARTESIAN_POINT('Ctrl Pts',(-0.407255628526418,0.000350158854048318,
-0.209781266907387));
#70241=CARTESIAN_POINT('Ctrl Pts',(-0.407180123234974,0.000363442776755221,
-0.33021873309261));
#70242=CARTESIAN_POINT('Ctrl Pts',(-0.406180659597689,-0.10773299253592,
-0.323871883628011));
#70243=CARTESIAN_POINT('Ctrl Pts',(-0.306359951108232,-0.352850302396471,
-0.309575640144001));
#70244=CARTESIAN_POINT('Ctrl Pts',(0.107730056479299,-0.469127483873643,
-0.28733000264058));
#70245=CARTESIAN_POINT('Ctrl Pts',(0.452788709608233,-0.16329500394726,
-0.263481820582346));
#70246=CARTESIAN_POINT('Ctrl Pts',(0.382365767560564,0.292380003087804,
-0.239633638524111));
#70247=CARTESIAN_POINT('Ctrl Pts',(-0.0389476842058911,0.479761919026928,
-0.215785456465877));
#70248=CARTESIAN_POINT('Ctrl Pts',(-0.359118952835858,0.269764862243941,
-0.195980487988709));
#70249=CARTESIAN_POINT('Ctrl Pts',(-0.406411288172487,0.0668799506786837,
-0.184124913530954));
#70250=CARTESIAN_POINT('Ctrl Pts',(-0.406387608173597,2.06471716765189E-5,
-0.180218733092611));
#70251=CARTESIAN_POINT('Origin',(0.,0.,-3.73478126690739));
#70252=CARTESIAN_POINT('',(-0.406495579036522,-0.000218292764554502,-0.509781266907387));
#70253=CARTESIAN_POINT('',(-0.407590403779514,-0.000208880552183932,-0.48021873309261));
#70254=CARTESIAN_POINT('',(-0.40705,-1.06687458785308E-14,-3.73478126690739));
#70255=CARTESIAN_POINT('Ctrl Pts',(-0.406495579036522,-0.000218292764554491,
-0.509781266907387));
#70256=CARTESIAN_POINT('Ctrl Pts',(-0.406757194309198,-0.0541301997109065,
-0.506629319531227));
#70257=CARTESIAN_POINT('Ctrl Pts',(-0.37167061156908,-0.243684261789019,
-0.495527978135656));
#70258=CARTESIAN_POINT('Ctrl Pts',(-0.0841652808768616,-0.473921941809059,
-0.476477242720672));
#70259=CARTESIAN_POINT('Ctrl Pts',(0.352973553690336,-0.327254449368329,
-0.452629060662438));
#70260=CARTESIAN_POINT('Ctrl Pts',(0.466213453793493,0.119711354789871,
-0.428780878604203));
#70261=CARTESIAN_POINT('Ctrl Pts',(0.151642201636973,0.456826497412456,
-0.404932696545969));
#70262=CARTESIAN_POINT('Ctrl Pts',(-0.285940937986012,0.377663980843574,
-0.381932825980363));
#70263=CARTESIAN_POINT('Ctrl Pts',(-0.406678995240854,0.120422959534271,
-0.366882349434169));
#70264=CARTESIAN_POINT('Ctrl Pts',(-0.407536015869335,-0.000245151173813667,
-0.359781266907386));
#70265=CARTESIAN_POINT('Ctrl Pts',(-0.407590403779514,-0.000208880552183977,
-0.48021873309261));
#70266=CARTESIAN_POINT('Ctrl Pts',(-0.407664828897934,-0.0121182807246313,
-0.479517641763892));
#70267=CARTESIAN_POINT('Ctrl Pts',(-0.401784195862354,-0.158989052611827,
-0.470867156415763));
#70268=CARTESIAN_POINT('Ctrl Pts',(-0.223868678851143,-0.426108666062932,
-0.454267277048223));
#70269=CARTESIAN_POINT('Ctrl Pts',(0.23716182206986,-0.418855661485411,
-0.430419094989988));
#70270=CARTESIAN_POINT('Ctrl Pts',(0.48056554579435,-0.0272483592525269,
-0.406570912931754));
#70271=CARTESIAN_POINT('Ctrl Pts',(0.282988398107527,0.389362803648974,
-0.382722730873519));
#70272=CARTESIAN_POINT('Ctrl Pts',(-0.174267639443746,0.448683269698852,
-0.358874548815284));
#70273=CARTESIAN_POINT('Ctrl Pts',(-0.392476459337574,0.190066042342598,
-0.341373216221648));
#70274=CARTESIAN_POINT('Ctrl Pts',(-0.407432482302036,0.0276571976974138,
-0.331821277647423));
#70275=CARTESIAN_POINT('Ctrl Pts',(-0.407180123234974,0.000363442776755221,
-0.33021873309261));
#70276=CARTESIAN_POINT('Origin',(0.,0.,-3.73478126690739));
#70277=CARTESIAN_POINT('',(-0.406736284960564,0.000338103824355545,-0.659781266907385));
#70278=CARTESIAN_POINT('',(-0.406539468648906,-0.000250938292638919,-0.630218733092608));
#70279=CARTESIAN_POINT('',(-0.40705,-1.06687458785308E-14,-3.73478126690739));
#70280=CARTESIAN_POINT('Ctrl Pts',(-0.406736284960564,0.000338103824355524,
-0.659781266907385));
#70281=CARTESIAN_POINT('Ctrl Pts',(-0.406007819042367,-0.0928372021789944,
-0.654325683647695));
#70282=CARTESIAN_POINT('Ctrl Pts',(-0.327910738459151,-0.322882824533624,
-0.640920706368594));
#70283=CARTESIAN_POINT('Ctrl Pts',(0.0546211364799233,-0.47822832672903,
-0.61956633507008));
#70284=CARTESIAN_POINT('Ctrl Pts',(0.431703968907574,-0.212879036894682,
-0.595718153011845));
#70285=CARTESIAN_POINT('Ctrl Pts',(0.412642536941405,0.247814320823537,
-0.571869970953611));
#70286=CARTESIAN_POINT('Ctrl Pts',(0.0149281723354398,0.481105966208734,
-0.548021788895376));
#70287=CARTESIAN_POINT('Ctrl Pts',(-0.342109434348876,0.300435894725022,
-0.527325554213302));
#70288=CARTESIAN_POINT('Ctrl Pts',(-0.406097385424149,0.0818387551948536,
-0.514578713550639));
#70289=CARTESIAN_POINT('Ctrl Pts',(-0.406495579036522,-0.000218292764554491,
-0.509781266907387));
#70290=CARTESIAN_POINT('Ctrl Pts',(-0.406539468648906,-0.000250938292638857,
-0.630218733092608));
#70291=CARTESIAN_POINT('Ctrl Pts',(-0.406828025379177,-0.0516308404303603,
-0.62721400588036));
#70292=CARTESIAN_POINT('Ctrl Pts',(-0.373926460083483,-0.238586974373572,
-0.616259884648701));
#70293=CARTESIAN_POINT('Ctrl Pts',(-0.0929180364960938,-0.472283827945071,
-0.59735636939763));
#70294=CARTESIAN_POINT('Ctrl Pts',(0.346859190705059,-0.333728149797965,
-0.573508187339396));
#70295=CARTESIAN_POINT('Ctrl Pts',(0.468348216506024,0.11106629839706,-0.549660005281161));
#70296=CARTESIAN_POINT('Ctrl Pts',(0.160067142708905,0.453943042521375,
-0.525811823222927));
#70297=CARTESIAN_POINT('Ctrl Pts',(-0.281715318279609,0.382434193485541,
-0.502664732493409));
#70298=CARTESIAN_POINT('Ctrl Pts',(-0.406820952263001,0.122917642025699,
-0.487467035783304));
#70299=CARTESIAN_POINT('Ctrl Pts',(-0.407590403779514,-0.000208880552183977,
-0.48021873309261));
#70300=CARTESIAN_POINT('Origin',(0.,0.,-3.73478126690739));
#70301=CARTESIAN_POINT('',(-0.407711648784268,6.03515928581689E-5,-0.809781266907385));
#70302=CARTESIAN_POINT('',(-0.40667324284948,0.000317666674979761,-0.780218733092609));
#70303=CARTESIAN_POINT('',(-0.40705,-1.06687458785308E-14,-3.73478126690739));
#70304=CARTESIAN_POINT('Ctrl Pts',(-0.407711648784268,6.03515928581763E-5,
-0.809781266907385));
#70305=CARTESIAN_POINT('Ctrl Pts',(-0.407439602143414,-0.131640917466901,
-0.802022047764164));
#70306=CARTESIAN_POINT('Ctrl Pts',(-0.266430554273655,-0.398771500841622,
-0.786313434601533));
#70307=CARTESIAN_POINT('Ctrl Pts',(0.188862140533343,-0.442737950614639,
-0.762655427419487));
#70308=CARTESIAN_POINT('Ctrl Pts',(0.474509248268113,-0.0807884543198489,
-0.738807245361255));
#70309=CARTESIAN_POINT('Ctrl Pts',(0.324732708102262,0.355294904731216,
-0.714959063303019));
#70310=CARTESIAN_POINT('Ctrl Pts',(-0.123028119751846,0.465349205210794,
-0.691110881244784));
#70311=CARTESIAN_POINT('Ctrl Pts',(-0.381289613521448,0.220894998825026,
-0.67271828244624));
#70312=CARTESIAN_POINT('Ctrl Pts',(-0.407069275230974,0.0429296232991591,
-0.662275077667107));
#70313=CARTESIAN_POINT('Ctrl Pts',(-0.406736284960564,0.000338103824355524,
-0.659781266907385));
#70314=CARTESIAN_POINT('Ctrl Pts',(-0.40667324284948,0.000317666674979726,
-0.780218733092608));
#70315=CARTESIAN_POINT('Ctrl Pts',(-0.406014261258321,-0.0903787005689077,
-0.77491036999683));
#70316=CARTESIAN_POINT('Ctrl Pts',(-0.331210705683951,-0.317881053446477,
-0.76165261288164));
#70317=CARTESIAN_POINT('Ctrl Pts',(0.0457649569583762,-0.479156909945254,
-0.740445461747037));
#70318=CARTESIAN_POINT('Ctrl Pts',(0.427691983500448,-0.220828763743674,
-0.716597279688803));
#70319=CARTESIAN_POINT('Ctrl Pts',(0.417156261778369,0.240138353613306,
-0.692749097630569));
#70320=CARTESIAN_POINT('Ctrl Pts',(0.0238256801714527,0.480747451989572,
-0.668900915572333));
#70321=CARTESIAN_POINT('Ctrl Pts',(-0.339056139434653,0.305475237122115,
-0.648057460726347));
#70322=CARTESIAN_POINT('Ctrl Pts',(-0.406064611270727,0.0843013284223252,
-0.635163399899772));
#70323=CARTESIAN_POINT('Ctrl Pts',(-0.406539468648906,-0.000250938292638857,
-0.630218733092608));
#70324=CARTESIAN_POINT('Origin',(0.,0.,-3.73478126690739));
#70325=CARTESIAN_POINT('',(-0.406916788159929,-0.000370586961657899,-0.959781266907386));
#70326=CARTESIAN_POINT('',(-0.407689224696409,0.000105882686618278,-0.930218733092609));
#70327=CARTESIAN_POINT('',(-0.40705,-1.06687458785308E-14,-3.73478126690739));
#70328=CARTESIAN_POINT('Ctrl Pts',(-0.406916788159929,-0.000370586961657902,
-0.959781266907386));
#70329=CARTESIAN_POINT('Ctrl Pts',(-0.407236540481942,-0.0364256157311761,
-0.957667805900046));
#70330=CARTESIAN_POINT('Ctrl Pts',(-0.386314993991867,-0.207730077702373,
-0.947604950873294));
#70331=CARTESIAN_POINT('Ctrl Pts',(-0.145121056613384,-0.458939734572041,
-0.92959270182713));
#70332=CARTESIAN_POINT('Ctrl Pts',(0.307386590221547,-0.370404218649844,
-0.905744519768897));
#70333=CARTESIAN_POINT('Ctrl Pts',(0.477827257505465,0.0580251068631922,
-0.88189633771066));
#70334=CARTESIAN_POINT('Ctrl Pts',(0.209799573991638,0.433208887021656,
-0.858048155652426));
#70335=CARTESIAN_POINT('Ctrl Pts',(-0.250746371636999,0.410867445963362,
-0.834199973594193));
#70336=CARTESIAN_POINT('Ctrl Pts',(-0.406219899087611,0.141439081117942,
-0.818111010679178));
#70337=CARTESIAN_POINT('Ctrl Pts',(-0.407718316521741,0.00328828884727744,
-0.809971441783576));
#70338=CARTESIAN_POINT('Ctrl Pts',(-0.407711648784268,6.03515928581763E-5,
-0.809781266907385));
#70339=CARTESIAN_POINT('Ctrl Pts',(-0.407689224696409,0.000105882686618259,
-0.930218733092609));
#70340=CARTESIAN_POINT('Ctrl Pts',(-0.407240576284007,-0.129115553887518,
-0.9226067341133));
#70341=CARTESIAN_POINT('Ctrl Pts',(-0.270934220145519,-0.394100455809237,
-0.907045341114577));
#70342=CARTESIAN_POINT('Ctrl Pts',(0.180639524384169,-0.446155956886755,
-0.883534554096447));
#70343=CARTESIAN_POINT('Ctrl Pts',(0.472933502380155,-0.0895526546900201,
-0.85968637203821));
#70344=CARTESIAN_POINT('Ctrl Pts',(0.331249783271615,0.34922679839552,-0.835838189979976));
#70345=CARTESIAN_POINT('Ctrl Pts',(-0.114398483465715,0.467545465827366,
-0.811990007921742));
#70346=CARTESIAN_POINT('Ctrl Pts',(-0.379241019134891,0.225992617481762,
-0.793450188959285));
#70347=CARTESIAN_POINT('Ctrl Pts',(-0.407001101123104,0.0454411644897258,
-0.782859764016241));
#70348=CARTESIAN_POINT('Ctrl Pts',(-0.40667324284948,0.000317666674979726,
-0.780218733092608));
#70349=CARTESIAN_POINT('Origin',(0.,0.,-3.73478126690739));
#70350=CARTESIAN_POINT('',(-0.406413319057786,0.000122795012471166,-1.10978126690739));
#70351=CARTESIAN_POINT('',(-0.40699144156463,-0.000374692172387947,-1.08021873309261));
#70352=CARTESIAN_POINT('',(-0.40705,-1.06687458785308E-14,-3.73478126690739));
#70353=CARTESIAN_POINT('Ctrl Pts',(-0.406413319057786,0.000122795012471158,
-1.10978126690739));
#70354=CARTESIAN_POINT('Ctrl Pts',(-0.406209480110007,-0.0754668531410285,
-1.10536417001651));
#70355=CARTESIAN_POINT('Ctrl Pts',(-0.34967754470652,-0.287377509622766,
-1.09299767910623));
#70356=CARTESIAN_POINT('Ctrl Pts',(-0.0080751395090761,-0.481269771711826,
-1.07268179417654));
#70357=CARTESIAN_POINT('Ctrl Pts',(0.400331227942373,-0.26724653220537,
-1.0488336121183));
#70358=CARTESIAN_POINT('Ctrl Pts',(0.441381881521284,0.192009988558863,
-1.02498543006007));
#70359=CARTESIAN_POINT('Ctrl Pts',(0.0774075336531558,0.475072494231541,
-1.00113724800183));
#70360=CARTESIAN_POINT('Ctrl Pts',(-0.319047392123228,0.335742773799606,
-0.97940252695094));
#70361=CARTESIAN_POINT('Ctrl Pts',(-0.406033851060433,0.0991887292104516,
-0.965617199919458));
#70362=CARTESIAN_POINT('Ctrl Pts',(-0.406916788159929,-0.000370586961657902,
-0.959781266907386));
#70363=CARTESIAN_POINT('Ctrl Pts',(-0.40699144156463,-0.000374692172387895,
-1.08021873309261));
#70364=CARTESIAN_POINT('Ctrl Pts',(-0.407296855312001,-0.0339025205290725,
-1.07825249224918));
#70365=CARTESIAN_POINT('Ctrl Pts',(-0.388158661228782,-0.202637347893537,
-1.06833685738634));
#70366=CARTESIAN_POINT('Ctrl Pts',(-0.153586221418629,-0.456176553787775,
-1.05047182850409));
#70367=CARTESIAN_POINT('Ctrl Pts',(0.300481799522643,-0.376027211503337,
-1.02662364644585));
#70368=CARTESIAN_POINT('Ctrl Pts',(0.478818880020692,0.0491757640619698,
-1.00277546438762));
#70369=CARTESIAN_POINT('Ctrl Pts',(0.217777667724211,0.429253611605008,
-0.978927282329384));
#70370=CARTESIAN_POINT('Ctrl Pts',(-0.243102740239076,0.415435715031318,
-0.955079100271148));
#70371=CARTESIAN_POINT('Ctrl Pts',(-0.405001862422473,0.146490969879461,
-0.938842917192225));
#70372=CARTESIAN_POINT('Ctrl Pts',(-0.407709110635635,0.00583350717703751,
-0.930556128132711));
#70373=CARTESIAN_POINT('Ctrl Pts',(-0.407689224696409,0.000105882686618259,
-0.930218733092609));
#70374=CARTESIAN_POINT('Origin',(0.,0.,-3.73478126690739));
#70375=CARTESIAN_POINT('',(-0.407368292334763,0.000320074934392933,-1.25978126690739));
#70376=CARTESIAN_POINT('',(-0.406394339960205,8.27571951184103E-5,-1.23021873309261));
#70377=CARTESIAN_POINT('',(-0.40705,-1.06687458785308E-14,-3.73478126690739));
#70378=CARTESIAN_POINT('Ctrl Pts',(-0.407368292334763,0.000320074934392955,
-1.25978126690739));
#70379=CARTESIAN_POINT('Ctrl Pts',(-0.406381911580918,-0.114007642520982,
-1.25306053413298));
#70380=CARTESIAN_POINT('Ctrl Pts',(-0.296492855911722,-0.36522436272828,
-1.23839040733917));
#70381=CARTESIAN_POINT('Ctrl Pts',(0.129642767060033,-0.463549947676258,
-1.21577088652594));
#70382=CARTESIAN_POINT('Ctrl Pts',(0.459961473100724,-0.141849371886711,
-1.19192270446771));
#70383=CARTESIAN_POINT('Ctrl Pts',(0.368205997786016,0.310016361239286,
-1.16807452240948));
#70384=CARTESIAN_POINT('Ctrl Pts',(-0.0614261349757158,0.477401959551476,
-1.14422634035124));
#70385=CARTESIAN_POINT('Ctrl Pts',(-0.365556557396479,0.256846415827171,
-1.12479525518388));
#70386=CARTESIAN_POINT('Ctrl Pts',(-0.406576326514428,0.0605708910621262,
-1.11331356403593));
#70387=CARTESIAN_POINT('Ctrl Pts',(-0.406413319057786,0.000122795012471158,
-1.10978126690739));
#70388=CARTESIAN_POINT('Ctrl Pts',(-0.406394339960205,8.27571951184519E-5,
-1.23021873309261));
#70389=CARTESIAN_POINT('Ctrl Pts',(-0.406261889000297,-0.0729960169730691,
-1.22594885636565));
#70390=CARTESIAN_POINT('Ctrl Pts',(-0.35248490968645,-0.282310174334548,
-1.21372958561928));
#70391=CARTESIAN_POINT('Ctrl Pts',(-0.0169768509947866,-0.481038004907766,
-1.19356092085349));
#70392=CARTESIAN_POINT('Ctrl Pts',(0.395318859158266,-0.274606582639873,
-1.16971273879526));
#70393=CARTESIAN_POINT('Ctrl Pts',(0.444858352516096,0.183811919722327,
-1.14586455673703));
#70394=CARTESIAN_POINT('Ctrl Pts',(0.0861827323523932,0.473559196172579,
-1.12201637467879));
#70395=CARTESIAN_POINT('Ctrl Pts',(-0.315484200393037,0.34069350414254,
-1.10013443346399));
#70396=CARTESIAN_POINT('Ctrl Pts',(-0.406062085815216,0.101648482346894,
-1.08620188626859));
#70397=CARTESIAN_POINT('Ctrl Pts',(-0.40699144156463,-0.000374692172387895,
-1.08021873309261));
#70398=CARTESIAN_POINT('Origin',(0.,0.,-3.73478126690739));
#70399=CARTESIAN_POINT('',(-0.407440005731881,-0.00029330702205249,-1.40978126690739));
#70400=CARTESIAN_POINT('',(-0.407295941515244,0.000340925431555991,-1.38021873309261));
#70401=CARTESIAN_POINT('',(-0.40705,-1.06687458785308E-14,-3.73478126690739));
#70402=CARTESIAN_POINT('Ctrl Pts',(-0.407440005731881,-0.000293307022052439,
-1.40978126690739));
#70403=CARTESIAN_POINT('Ctrl Pts',(-0.407588524841362,-0.0185715359398175,
-1.40870629226887));
#70404=CARTESIAN_POINT('Ctrl Pts',(-0.39815909867122,-0.171862363193748,
-1.39968192361093));
#70405=CARTESIAN_POINT('Ctrl Pts',(-0.203608890553224,-0.43615274930846,
-1.38270816093359));
#70406=CARTESIAN_POINT('Ctrl Pts',(0.256572182166905,-0.407254854335409,
-1.35885997887535));
#70407=CARTESIAN_POINT('Ctrl Pts',(0.481315071300406,-0.00464792219482722,
-1.33501179681712));
#70408=CARTESIAN_POINT('Ctrl Pts',(0.264389089074653,0.402224080109482,
-1.31116361475888));
#70409=CARTESIAN_POINT('Ctrl Pts',(-0.195148100516391,0.440003431698535,
-1.28731543270065));
#70410=CARTESIAN_POINT('Ctrl Pts',(-0.396573317235439,0.177160896699739,
-1.27018798341682));
#70411=CARTESIAN_POINT('Ctrl Pts',(-0.407548619070813,0.0212210749269621,
-1.2610099281524));
#70412=CARTESIAN_POINT('Ctrl Pts',(-0.407368292334763,0.000320074934392955,
-1.25978126690739));
#70413=CARTESIAN_POINT('Ctrl Pts',(-0.407295941515244,0.000340925431555998,
-1.38021873309261));
#70414=CARTESIAN_POINT('Ctrl Pts',(-0.406292379364719,-0.111533876317919,
-1.37364522048212));
#70415=CARTESIAN_POINT('Ctrl Pts',(-0.300437242591872,-0.360368125454541,
-1.35912231385222));
#70416=CARTESIAN_POINT('Ctrl Pts',(0.121045283258203,-0.465868881807192,
-1.3366500132029));
#70417=CARTESIAN_POINT('Ctrl Pts',(0.457258640884715,-0.150333998056345,
-1.31280183114467));
#70418=CARTESIAN_POINT('Ctrl Pts',(0.373878015523797,0.303151785650903,
-1.28895364908643));
#70419=CARTESIAN_POINT('Ctrl Pts',(-0.0525840776504784,0.478456571083512,
-1.2651054670282));
#70420=CARTESIAN_POINT('Ctrl Pts',(-0.363077306115782,0.261936811360845,
-1.24552716169692));
#70421=CARTESIAN_POINT('Ctrl Pts',(-0.406508478055647,0.0630575525949989,
-1.23389825038506));
#70422=CARTESIAN_POINT('Ctrl Pts',(-0.406394339960205,8.27571951184519E-5,
-1.23021873309261));
#70423=CARTESIAN_POINT('Origin',(0.,0.,-3.73478126690739));
#70424=CARTESIAN_POINT('',(-0.406440918185289,-0.000163016377902653,-1.55978126690739));
#70425=CARTESIAN_POINT('',(-0.407503887525846,-0.000263145742968152,-1.53021873309261));
#70426=CARTESIAN_POINT('',(-0.40705,-1.06687458785308E-14,-3.73478126690739));
#70427=CARTESIAN_POINT('Ctrl Pts',(-0.406440918185289,-0.000163016377902669,
-1.55978126690739));
#70428=CARTESIAN_POINT('Ctrl Pts',(-0.406648703272632,-0.0579712755676122,
-1.55640265638533));
#70429=CARTESIAN_POINT('Ctrl Pts',(-0.368077181138247,-0.251529596840672,
-1.54507465184387));
#70430=CARTESIAN_POINT('Ctrl Pts',(-0.0706340888623429,-0.476126691682194,
-1.525797253283));
#70431=CARTESIAN_POINT('Ctrl Pts',(0.362150411553781,-0.317069204517043,
-1.50194907122476));
#70432=CARTESIAN_POINT('Ctrl Pts',(0.462615038625616,0.132940313972334,
-1.47810088916653));
#70433=CARTESIAN_POINT('Ctrl Pts',(0.138570494539446,0.460959888802416,
-1.45425270710829));
#70434=CARTESIAN_POINT('Ctrl Pts',(-0.292292194285244,0.370269985671315,
-1.43147949968858));
#70435=CARTESIAN_POINT('Ctrl Pts',(-0.406490232027403,0.116595228407491,
-1.41665568628828));
#70436=CARTESIAN_POINT('Ctrl Pts',(-0.407440005731881,-0.000293307022052439,
-1.40978126690739));
#70437=CARTESIAN_POINT('Ctrl Pts',(-0.407503887525846,-0.000263145742968167,
-1.53021873309261));
#70438=CARTESIAN_POINT('Ctrl Pts',(-0.407622154607844,-0.0160316617814609,
-1.529290978618));
#70439=CARTESIAN_POINT('Ctrl Pts',(-0.399625537496969,-0.166790447514566,
-1.52041383012398));
#70440=CARTESIAN_POINT('Ctrl Pts',(-0.211642503026044,-0.432311492500735,
-1.50358728761054));
#70441=CARTESIAN_POINT('Ctrl Pts',(0.24899438347629,-0.411931514493132,
-1.47973910555231));
#70442=CARTESIAN_POINT('Ctrl Pts',(0.481146697435232,-0.0135510583539467,
-1.45589092349407));
#70443=CARTESIAN_POINT('Ctrl Pts',(0.271784644847739,0.397264247649257,
-1.43204274143584));
#70444=CARTESIAN_POINT('Ctrl Pts',(-0.186974994684948,0.443538191137929,
-1.40819455937761));
#70445=CARTESIAN_POINT('Ctrl Pts',(-0.395000964387442,0.182239984207465,
-1.39091988992986));
#70446=CARTESIAN_POINT('Ctrl Pts',(-0.407505993976906,0.0237570910304725,
-1.38159461450153));
#70447=CARTESIAN_POINT('Ctrl Pts',(-0.407295941515244,0.000340925431555998,
-1.38021873309261));
#70448=CARTESIAN_POINT('Origin',(0.,0.,-3.73478126690739));
#70449=CARTESIAN_POINT('',(-0.406841268402119,0.000361155301022391,-1.70978126690739));
#70450=CARTESIAN_POINT('',(-0.406474561616192,-0.000199550871096271,-1.68021873309261));
#70451=CARTESIAN_POINT('',(-0.40705,-1.06687458785308E-14,-3.73478126690739));
#70452=CARTESIAN_POINT('Ctrl Pts',(-0.406841268402119,0.000361155301022383,
-1.70978126690739));
#70453=CARTESIAN_POINT('Ctrl Pts',(-0.406015505560738,-0.0966219857244575,
-1.7040990205018));
#70454=CARTESIAN_POINT('Ctrl Pts',(-0.322687842220291,-0.330557993933317,
-1.69046738007681));
#70455=CARTESIAN_POINT('Ctrl Pts',(0.0682186748769831,-0.476478764940969,
-1.6688863456324));
#70456=CARTESIAN_POINT('Ctrl Pts',(0.437591544119186,-0.200497983922606,
-1.64503816357417));
#70457=CARTESIAN_POINT('Ctrl Pts',(0.405417537039194,0.259465646478908,
-1.62118998151593));
#70458=CARTESIAN_POINT('Ctrl Pts',(0.00122046920282805,0.481335965305491,
-1.5973417994577));
#70459=CARTESIAN_POINT('Ctrl Pts',(-0.346674621281165,0.29266017250168,
-1.57687222792152));
#70460=CARTESIAN_POINT('Ctrl Pts',(-0.406159814269338,0.0780434046909889,
-1.56435205040475));
#70461=CARTESIAN_POINT('Ctrl Pts',(-0.406440918185289,-0.000163016377902669,
-1.55978126690739));
#70462=CARTESIAN_POINT('Ctrl Pts',(-0.406474561616192,-0.000199550871096264,
-1.68021873309261));
#70463=CARTESIAN_POINT('Ctrl Pts',(-0.406718999720409,-0.0554774150689223,
-1.67698734273447));
#70464=CARTESIAN_POINT('Ctrl Pts',(-0.37042783086876,-0.246434376736608,
-1.66580655835692));
#70465=CARTESIAN_POINT('Ctrl Pts',(-0.0794299488178135,-0.474738516307812,
-1.64667637995995));
#70466=CARTESIAN_POINT('Ctrl Pts',(0.356222900192536,-0.323714412737155,
-1.62282819790172));
#70467=CARTESIAN_POINT('Ctrl Pts',(0.464995134691316,0.124359560745234,
-1.59898001584348));
#70468=CARTESIAN_POINT('Ctrl Pts',(0.147074151851645,0.458317542204598,
-1.57513183378525));
#70469=CARTESIAN_POINT('Ctrl Pts',(-0.288188203612822,0.375079119038563,
-1.55221140620162));
#70470=CARTESIAN_POINT('Ctrl Pts',(-0.406608792064132,0.119079674807948,
-1.53724037263741));
#70471=CARTESIAN_POINT('Ctrl Pts',(-0.407503887525846,-0.000263145742968167,
-1.53021873309261));
#70472=CARTESIAN_POINT('Origin',(0.,0.,-3.73478126690739));
#70473=CARTESIAN_POINT('',(-0.40772218496585,-1.16393611243039E-5,-1.85978126690739));
#70474=CARTESIAN_POINT('',(-0.406772054937087,0.00034738140794717,-1.83021873309261));
#70475=CARTESIAN_POINT('',(-0.40705,-1.06687458785308E-14,-3.73478126690739));
#70476=CARTESIAN_POINT('Ctrl Pts',(-0.40772218496585,-1.16393611242892E-5,
-1.85978126690739));
#70477=CARTESIAN_POINT('Ctrl Pts',(-0.407722444052212,-0.000630930684549266,
-1.85974477863768));
#70478=CARTESIAN_POINT('Ctrl Pts',(-0.407440412028103,-0.136169797995048,
-1.85175889634857));
#70479=CARTESIAN_POINT('Ctrl Pts',(-0.258634130007767,-0.405948503922317,
-1.83582362004005));
#70480=CARTESIAN_POINT('Ctrl Pts',(0.20139448024705,-0.437179670579116,
-1.81197543798181));
#70481=CARTESIAN_POINT('Ctrl Pts',(0.476617589713424,-0.0672419081928105,
-1.78812725592358));
#70482=CARTESIAN_POINT('Ctrl Pts',(0.314482375140717,0.364399007637914,
-1.76427907386534));
#70483=CARTESIAN_POINT('Ctrl Pts',(-0.136231120007138,0.461656672196172,
-1.74043089180711));
#70484=CARTESIAN_POINT('Ctrl Pts',(-0.384330302527872,0.213048446444068,
-1.72226495615446));
#70485=CARTESIAN_POINT('Ctrl Pts',(-0.407170737791829,0.0390562559818897,
-1.71204841452121));
#70486=CARTESIAN_POINT('Ctrl Pts',(-0.406841268402119,0.000361155301022383,
-1.70978126690739));
#70487=CARTESIAN_POINT('Ctrl Pts',(-0.406772054937087,0.000347381407947184,
-1.83021873309261));
#70488=CARTESIAN_POINT('Ctrl Pts',(-0.406007973272697,-0.0941637101848716,
-1.82468370685094));
#70489=CARTESIAN_POINT('Ctrl Pts',(-0.32609986428909,-0.325576544298442,
-1.81119928658986));
#70490=CARTESIAN_POINT('Ctrl Pts',(0.0593925331488187,-0.477659190889811,
-1.78976547230936));
#70491=CARTESIAN_POINT('Ctrl Pts',(0.433807590226198,-0.208558745435148,
-1.76591729025113));
#70492=CARTESIAN_POINT('Ctrl Pts',(0.410148038410438,0.251921341341723,
-1.74206910819289));
#70493=CARTESIAN_POINT('Ctrl Pts',(0.0101245785925387,0.481230992916775,
-1.71822092613466));
#70494=CARTESIAN_POINT('Ctrl Pts',(-0.343728093356254,0.297712804988723,
-1.69760413443456));
#70495=CARTESIAN_POINT('Ctrl Pts',(-0.406117668841617,0.0805091029179855,
-1.68493673675388));
#70496=CARTESIAN_POINT('Ctrl Pts',(-0.406474561616192,-0.000199550871096264,
-1.68021873309261));
#70497=CARTESIAN_POINT('Origin',(0.,0.,-3.73478126690739));
#70498=CARTESIAN_POINT('',(-0.40680653690778,-0.000354893438868044,-2.00978126690739));
#70499=CARTESIAN_POINT('',(-0.40771880079626,3.52644710581579E-5,-1.98021873309261));
#70500=CARTESIAN_POINT('',(-0.40705,-1.06687458785308E-14,-3.73478126690739));
#70501=CARTESIAN_POINT('Ctrl Pts',(-0.40680653690778,-0.000354893438868045,
-2.00978126690739));
#70502=CARTESIAN_POINT('Ctrl Pts',(-0.407138596781516,-0.0403041751809355,
-2.00744114275415));
#70503=CARTESIAN_POINT('Ctrl Pts',(-0.383366193393983,-0.215574408747965,
-1.99715162458151));
#70504=CARTESIAN_POINT('Ctrl Pts',(-0.131991827375041,-0.46288655040716,
-1.97891271238946));
#70505=CARTESIAN_POINT('Ctrl Pts',(0.317810826682713,-0.361499764156071,
-1.95506453033122));
#70506=CARTESIAN_POINT('Ctrl Pts',(0.475980915095963,0.0716098422428978,
-1.93121634827299));
#70507=CARTESIAN_POINT('Ctrl Pts',(0.197376910832261,0.439008150393539,
-1.90736816621475));
#70508=CARTESIAN_POINT('Ctrl Pts',(-0.261642567705972,0.403613899628779,
-1.88355647242622));
#70509=CARTESIAN_POINT('Ctrl Pts',(-0.407665999074413,0.134288888284683,
-1.8676941726571));
#70510=CARTESIAN_POINT('Ctrl Pts',(-0.40772218496585,-1.16393611242892E-5,
-1.85978126690739));
#70511=CARTESIAN_POINT('Ctrl Pts',(-0.40771880079626,3.52644710581694E-5,
-1.98021873309261));
#70512=CARTESIAN_POINT('Ctrl Pts',(-0.407554198464361,-0.133008126687299,
-1.97238007096741));
#70513=CARTESIAN_POINT('Ctrl Pts',(-0.263966612793417,-0.401278997996624,
-1.95659201482279));
#70514=CARTESIAN_POINT('Ctrl Pts',(0.193272542416614,-0.440830466260172,
-1.93285456465877));
#70515=CARTESIAN_POINT('Ctrl Pts',(0.475292082851708,-0.0760474300277662,
-1.90900638260053));
#70516=CARTESIAN_POINT('Ctrl Pts',(0.321169623344976,0.358518965573356,
-1.8851582005423));
#70517=CARTESIAN_POINT('Ctrl Pts',(-0.127667532450826,0.464097809511379,
-1.86131001848406));
#70518=CARTESIAN_POINT('Ctrl Pts',(-0.382370862514766,0.218144542773098,
-1.8429968626675));
#70519=CARTESIAN_POINT('Ctrl Pts',(-0.407105345886311,0.0415729373886564,
-1.83263310087035));
#70520=CARTESIAN_POINT('Ctrl Pts',(-0.406772054937087,0.000347381407947184,
-1.83021873309261));
#70521=CARTESIAN_POINT('Origin',(0.,0.,-3.73478126690739));
#70522=CARTESIAN_POINT('',(-0.406456740617355,0.000181399743008865,-2.15978126690739));
#70523=CARTESIAN_POINT('',(-0.406877361306786,-0.000366356398630974,-2.13021873309261));
#70524=CARTESIAN_POINT('',(-0.40705,-1.06687458785308E-14,-3.73478126690739));
#70525=CARTESIAN_POINT('Ctrl Pts',(-0.406456740617355,0.000181399743008834,
-2.15978126690739));
#70526=CARTESIAN_POINT('Ctrl Pts',(-0.4061382297576,-0.0792659267566264,
-2.15513750687062));
#70527=CARTESIAN_POINT('Ctrl Pts',(-0.34522264593974,-0.295165752186438,
-2.14254435281445));
#70528=CARTESIAN_POINT('Ctrl Pts',(0.00563444864094621,-0.481304533564932,
-2.12200180473886));
#70529=CARTESIAN_POINT('Ctrl Pts',(0.407779886717249,-0.255736905882805,
-2.09815362268063));
#70530=CARTESIAN_POINT('Ctrl Pts',(0.435734502464197,0.204502431290978,
-2.07430544062239));
#70531=CARTESIAN_POINT('Ctrl Pts',(0.0638463179520797,0.47708432035187,
-2.05045725856416));
#70532=CARTESIAN_POINT('Ctrl Pts',(-0.324388339227509,0.328090460304887,
-2.02894920065916));
#70533=CARTESIAN_POINT('Ctrl Pts',(-0.406010590487186,0.0954034029496748,
-2.01539053677357));
#70534=CARTESIAN_POINT('Ctrl Pts',(-0.40680653690778,-0.000354893438868045,
-2.00978126690739));
#70535=CARTESIAN_POINT('Ctrl Pts',(-0.406877361306786,-0.00036635639863097,
-2.13021873309261));
#70536=CARTESIAN_POINT('Ctrl Pts',(-0.407202839001211,-0.037785859492885,
-2.12802582910329));
#70537=CARTESIAN_POINT('Ctrl Pts',(-0.385296759883492,-0.210478987110743,
-2.11788353109455));
#70538=CARTESIAN_POINT('Ctrl Pts',(-0.14053225246876,-0.460365573920769,
-2.09979183906641));
#70539=CARTESIAN_POINT('Ctrl Pts',(0.311068976634055,-0.367317121042818,
-2.07594365700817));
#70540=CARTESIAN_POINT('Ctrl Pts',(0.477224160065282,0.0627923298288068,
-2.05209547494994));
#70541=CARTESIAN_POINT('Ctrl Pts',(0.205464412655191,0.435281691284622,
-2.02824729289171));
#70542=CARTESIAN_POINT('Ctrl Pts',(-0.254835525272372,0.408343765342997,
-2.00439911083347));
#70543=CARTESIAN_POINT('Ctrl Pts',(-0.406857244157191,0.138714721617122,
-1.98838959090044));
#70544=CARTESIAN_POINT('Ctrl Pts',(-0.407721126030811,0.00191468553547783,
-1.98032946498682));
#70545=CARTESIAN_POINT('Ctrl Pts',(-0.40771880079626,3.52644710581694E-5,
-1.98021873309261));
#70546=CARTESIAN_POINT('Origin',(0.,0.,-3.73478126690739));
#70547=CARTESIAN_POINT('',(-0.407472342035332,0.0002788890774828,-2.30978126690739));
#70548=CARTESIAN_POINT('',(-0.406426582399692,0.00014382004374669,-2.28021873309261));
#70549=CARTESIAN_POINT('',(-0.40705,-1.06687458785308E-14,-3.73478126690739));
#70550=CARTESIAN_POINT('Ctrl Pts',(-0.407472342035332,0.000278889077482811,
-2.30978126690739));
#70551=CARTESIAN_POINT('Ctrl Pts',(-0.406547165835321,-0.117826010948906,
-2.30283387098709));
#70552=CARTESIAN_POINT('Ctrl Pts',(-0.2902676921825,-0.37265690370858,-2.28793708104738));
#70553=CARTESIAN_POINT('Ctrl Pts',(0.142791842339502,-0.459669762767722,
-2.26509089708827));
#70554=CARTESIAN_POINT('Ctrl Pts',(0.463814698616821,-0.128692371136095,
-2.24124271503003));
#70555=CARTESIAN_POINT('Ctrl Pts',(0.359227540430107,0.3203769268193,-2.2173945329718));
#70556=CARTESIAN_POINT('Ctrl Pts',(-0.0749973785569536,0.475458930141424,
-2.19354635091357));
#70557=CARTESIAN_POINT('Ctrl Pts',(-0.369250167839865,0.249004140055587,
-2.17434192889209));
#70558=CARTESIAN_POINT('Ctrl Pts',(-0.406683470748437,0.0567355240363727,
-2.16308690089003));
#70559=CARTESIAN_POINT('Ctrl Pts',(-0.406456740617355,0.000181399743008834,
-2.15978126690739));
#70560=CARTESIAN_POINT('Ctrl Pts',(-0.406426582399692,0.000143820043746662,
-2.28021873309261));
#70561=CARTESIAN_POINT('Ctrl Pts',(-0.406183098315414,-0.0767990503092323,
-2.27572219321976));
#70562=CARTESIAN_POINT('Ctrl Pts',(-0.348134530504143,-0.290109160327883,
-2.26327625932749));
#70563=CARTESIAN_POINT('Ctrl Pts',(-0.00327025270698847,-0.481326376882232,
-2.24288093141582));
#70564=CARTESIAN_POINT('Ctrl Pts',(0.402979161470327,-0.263236720569178,
-2.21903274935758));
#70565=CARTESIAN_POINT('Ctrl Pts',(0.4394430400586,0.196406695861922,-2.19518456729935));
#70566=CARTESIAN_POINT('Ctrl Pts',(0.0726610551733367,0.47582154921403,
-2.17133638524111));
#70567=CARTESIAN_POINT('Ctrl Pts',(-0.320939240454663,0.33306470369783,
-2.14968110717221));
#70568=CARTESIAN_POINT('Ctrl Pts',(-0.406022964984787,0.0978618366923023,
-2.1359752231227));
#70569=CARTESIAN_POINT('Ctrl Pts',(-0.406877361306786,-0.00036635639863097,
-2.13021873309261));
#70570=CARTESIAN_POINT('Origin',(0.,0.,-3.73478126690739));
#70571=CARTESIAN_POINT('',(-0.40733281339199,-0.000331010205261331,-2.45978126690739));
#70572=CARTESIAN_POINT('',(-0.407405900524309,0.000306859758717713,-2.43021873309261));
#70573=CARTESIAN_POINT('',(-0.40705,-1.06687458785308E-14,-3.73478126690739));
#70574=CARTESIAN_POINT('Ctrl Pts',(-0.40733281339199,-0.000331010205261342,
-2.45978126690739));
#70575=CARTESIAN_POINT('Ctrl Pts',(-0.407528022996003,-0.0224784334219731,
-2.45847962912297));
#70576=CARTESIAN_POINT('Ctrl Pts',(-0.395800475568512,-0.179678172289964,
-2.44922859731915));
#70577=CARTESIAN_POINT('Ctrl Pts',(-0.191104898808961,-0.441774511139857,
-2.43202817149591));
#70578=CARTESIAN_POINT('Ctrl Pts',(0.268066517033437,-0.399782620291585,
-2.40817998943768));
#70579=CARTESIAN_POINT('Ctrl Pts',(0.481252209413066,0.00906156590694945,
-2.38433180737944));
#70580=CARTESIAN_POINT('Ctrl Pts',(0.252826714350878,0.409590592607036,
-2.36048362532121));
#70581=CARTESIAN_POINT('Ctrl Pts',(-0.207600012825493,0.434267239976145,
-2.33663544326297));
#70582=CARTESIAN_POINT('Ctrl Pts',(-0.398892410069302,0.169347774513397,
-2.31973465712503));
#70583=CARTESIAN_POINT('Ctrl Pts',(-0.407605776894147,0.0173127369653136,
-2.3107832650065));
#70584=CARTESIAN_POINT('Ctrl Pts',(-0.407472342035332,0.000278889077482811,
-2.30978126690739));
#70585=CARTESIAN_POINT('Ctrl Pts',(-0.407405900524309,0.00030685975871772,
-2.43021873309261));
#70586=CARTESIAN_POINT('Ctrl Pts',(-0.406435945677901,-0.115344487807178,
-2.42341855733623));
#70587=CARTESIAN_POINT('Ctrl Pts',(-0.294332076638151,-0.367835636378687,
-2.40866898756043));
#70588=CARTESIAN_POINT('Ctrl Pts',(0.134263887909296,-0.462232608151807,
-2.38597002376523));
#70589=CARTESIAN_POINT('Ctrl Pts',(0.461354600469472,-0.137250531004422,
-2.36212184170699));
#70590=CARTESIAN_POINT('Ctrl Pts',(0.365092757010119,0.313676671772215,
-2.33827365964876));
#70591=CARTESIAN_POINT('Ctrl Pts',(-0.0661889425581167,0.476764931091184,
-2.31442547759052));
#70592=CARTESIAN_POINT('Ctrl Pts',(-0.366868044521016,0.254098374107902,
-2.29507383540514));
#70593=CARTESIAN_POINT('Ctrl Pts',(-0.406613551725838,0.0592275858856569,
-2.28367158723917));
#70594=CARTESIAN_POINT('Ctrl Pts',(-0.406426582399692,0.000143820043746662,
-2.28021873309261));
#70595=CARTESIAN_POINT('Origin',(0.,0.,-3.73478126690739));
#70596=CARTESIAN_POINT('',(-0.406402994387456,-0.000103102301948036,-2.60978126690739));
#70597=CARTESIAN_POINT('',(-0.407403472603433,-0.000307765760287793,-2.58021873309261));
#70598=CARTESIAN_POINT('',(-0.40705,-1.06687458785308E-14,-3.73478126690739));
#70599=CARTESIAN_POINT('Ctrl Pts',(-0.406402994387456,-0.000103102301948009,
-2.60978126690739));
#70600=CARTESIAN_POINT('Ctrl Pts',(-0.406542488586396,-0.0618039549847077,
-2.60617599323944));
#70601=CARTESIAN_POINT('Ctrl Pts',(-0.364335566924364,-0.259370083859107,
-2.59462132555209));
#70602=CARTESIAN_POINT('Ctrl Pts',(-0.0570455976290363,-0.477945186012748,
-2.57511726384532));
#70603=CARTESIAN_POINT('Ctrl Pts',(0.371033481116859,-0.306626738775311,
-2.55126908178708));
#70604=CARTESIAN_POINT('Ctrl Pts',(0.458641320517021,0.146061425968784,
-2.52742089972885));
#70605=CARTESIAN_POINT('Ctrl Pts',(0.125386389416043,0.46471932861766,-2.50357271767061));
#70606=CARTESIAN_POINT('Ctrl Pts',(-0.298457773679393,0.362819873754557,
-2.4810261733968));
#70607=CARTESIAN_POINT('Ctrl Pts',(-0.406335834141885,0.112780849746093,
-2.46642902314238));
#70608=CARTESIAN_POINT('Ctrl Pts',(-0.40733281339199,-0.000331010205261342,
-2.45978126690739));
#70609=CARTESIAN_POINT('Ctrl Pts',(-0.407403472603433,-0.000307765760287751,
-2.58021873309261));
#70610=CARTESIAN_POINT('Ctrl Pts',(-0.407568470906435,-0.0199413795938409,
-2.57906431547211));
#70611=CARTESIAN_POINT('Ctrl Pts',(-0.39734641009149,-0.174600768307096,
-2.56996050383219));
#70612=CARTESIAN_POINT('Ctrl Pts',(-0.199244649661891,-0.438163605536162,
-2.55290729817287));
#70613=CARTESIAN_POINT('Ctrl Pts',(0.260624980917576,-0.404673195253975,
-2.52905911611463));
#70614=CARTESIAN_POINT('Ctrl Pts',(0.481337460529596,0.000157245861404591,
-2.5052109340564));
#70615=CARTESIAN_POINT('Ctrl Pts',(0.260360523766897,0.404843393547639,
-2.48136275199817));
#70616=CARTESIAN_POINT('Ctrl Pts',(-0.199530890300541,0.438033331438621,
-2.45751456993993));
#70617=CARTESIAN_POINT('Ctrl Pts',(-0.39740005747315,0.174421513829129,
-2.44046656363808));
#70618=CARTESIAN_POINT('Ctrl Pts',(-0.407569821261616,0.0198517429393876,
-2.43136795135564));
#70619=CARTESIAN_POINT('Ctrl Pts',(-0.407405900524309,0.00030685975871772,
-2.43021873309261));
#70620=CARTESIAN_POINT('Origin',(0.,0.,-3.73478126690739));
#70621=CARTESIAN_POINT('',(-0.406953572106064,0.000373234526637736,-2.75978126690739));
#70622=CARTESIAN_POINT('',(-0.406425648305095,-0.000142458567169629,-2.73021873309261));
#70623=CARTESIAN_POINT('',(-0.40705,-1.06687458785308E-14,-3.73478126690739));
#70624=CARTESIAN_POINT('Ctrl Pts',(-0.406953572106064,0.000373234526637737,
-2.75978126690739));
#70625=CARTESIAN_POINT('Ctrl Pts',(-0.406046513116615,-0.100407864961081,
-2.75387235735591));
#70626=CARTESIAN_POINT('Ctrl Pts',(-0.317290461654102,-0.338198853077946,
-2.74001405378502));
#70627=CARTESIAN_POINT('Ctrl Pts',(0.0817608711451184,-0.474342661995509,
-2.71820635619473));
#70628=CARTESIAN_POINT('Ctrl Pts',(0.443124125342135,-0.187954277905899,
-2.69435817413649));
#70629=CARTESIAN_POINT('Ctrl Pts',(0.397863643893962,0.270906481850664,
-2.67050999207826));
#70630=CARTESIAN_POINT('Ctrl Pts',(-0.0124882236963727,0.481175482864919,
-2.64666181002002));
#70631=CARTESIAN_POINT('Ctrl Pts',(-0.351077571508608,0.284866454272714,
-2.62641890162973));
#70632=CARTESIAN_POINT('Ctrl Pts',(-0.406234912947782,0.0742424133312181,
-2.61412538725885));
#70633=CARTESIAN_POINT('Ctrl Pts',(-0.406402994387456,-0.000103102301948009,
-2.60978126690739));
#70634=CARTESIAN_POINT('Ctrl Pts',(-0.406425648305095,-0.000142458567169636,
-2.73021873309261));
#70635=CARTESIAN_POINT('Ctrl Pts',(-0.406611102354183,-0.0593155331541186,
-2.72676067958858));
#70636=CARTESIAN_POINT('Ctrl Pts',(-0.366782770719768,-0.254278247849184,
-2.71535323206513));
#70637=CARTESIAN_POINT('Ctrl Pts',(-0.0658774242972122,-0.476808075228433,
-2.69599639052228));
#70638=CARTESIAN_POINT('Ctrl Pts',(0.365297626161182,-0.313438063988078,
-2.67214820846404));
#70639=CARTESIAN_POINT('Ctrl Pts',(0.461264826549058,0.137551937187166,
-2.64830002640581));
#70640=CARTESIAN_POINT('Ctrl Pts',(0.133961850108581,0.462320233551161,
-2.62445184434757));
#70641=CARTESIAN_POINT('Ctrl Pts',(-0.294474187986566,0.367664936403977,
-2.60175807990984));
#70642=CARTESIAN_POINT('Ctrl Pts',(-0.406432281974628,0.115256948650598,
-2.58701370949152));
#70643=CARTESIAN_POINT('Ctrl Pts',(-0.407403472603433,-0.000307765760287751,
-2.58021873309261));
#70644=CARTESIAN_POINT('Origin',(0.,0.,-3.73478126690739));
#70645=CARTESIAN_POINT('',(-0.40770196810232,-8.31109565067826E-5,-2.90978126690739));
#70646=CARTESIAN_POINT('',(-0.406879917492779,0.000366675793932125,-2.88021873309261));
#70647=CARTESIAN_POINT('',(-0.40705,-1.06687458785308E-14,-3.73478126690739));
#70648=CARTESIAN_POINT('Ctrl Pts',(-0.407701968102319,-8.31109565068242E-5,
-2.90978126690739));
#70649=CARTESIAN_POINT('Ctrl Pts',(-0.407714401779122,-0.00455000157151528,
-2.90951811549179));
#70650=CARTESIAN_POINT('Ctrl Pts',(-0.405622145279423,-0.143942763391086,
-2.90130557005679));
#70651=CARTESIAN_POINT('Ctrl Pts',(-0.246968019692694,-0.413149607648352,
-2.88514363060237));
#70652=CARTESIAN_POINT('Ctrl Pts',(0.213763439489368,-0.431266730500215,
-2.86129544854413));
#70653=CARTESIAN_POINT('Ctrl Pts',(0.478339277460365,-0.053640812432835,
-2.8374472664859));
#70654=CARTESIAN_POINT('Ctrl Pts',(0.303976919789322,0.373207493590096,
-2.81359908442767));
#70655=CARTESIAN_POINT('Ctrl Pts',(-0.149323603380172,0.457589622365882,
-2.78975090236943));
#70656=CARTESIAN_POINT('Ctrl Pts',(-0.387235890803543,0.205205383146445,
-2.77181162986267));
#70657=CARTESIAN_POINT('Ctrl Pts',(-0.407266800759058,0.0351753018750611,
-2.76182175137532));
#70658=CARTESIAN_POINT('Ctrl Pts',(-0.406953572106064,0.000373234526637737,
-2.75978126690739));
#70659=CARTESIAN_POINT('Ctrl Pts',(-0.406879917492779,0.000366675793932139,
-2.88021873309261));
#70660=CARTESIAN_POINT('Ctrl Pts',(-0.406023584688337,-0.0979486711077955,
-2.87445704370505));
#70661=CARTESIAN_POINT('Ctrl Pts',(-0.320816081720589,-0.333240111186755,
-2.86074596029807));
#70662=CARTESIAN_POINT('Ctrl Pts',(0.0729719274013494,-0.475773973046388,
-2.83908548287168));
#70663=CARTESIAN_POINT('Ctrl Pts',(0.439571272608378,-0.196119534836683,
-2.81523730081345));
#70664=CARTESIAN_POINT('Ctrl Pts',(0.402807084347494,0.263499959076195,
-2.79138911875521));
#70665=CARTESIAN_POINT('Ctrl Pts',(-0.00358473645388183,0.481324137455872,
-2.76754093669698));
#70666=CARTESIAN_POINT('Ctrl Pts',(-0.348236120974117,0.289930441795519,
-2.74715080814278));
#70667=CARTESIAN_POINT('Ctrl Pts',(-0.406184779480063,0.0767118836232727,
-2.73471007360799));
#70668=CARTESIAN_POINT('Ctrl Pts',(-0.406425648305095,-0.000142458567169636,
-2.73021873309261));
#70669=CARTESIAN_POINT('Origin',(0.,0.,-3.73478126690739));
#70670=CARTESIAN_POINT('',(-0.406704477435532,-0.000328489605546852,-3.05978126690739));
#70671=CARTESIAN_POINT('',(-0.407718443135198,-3.6913074990319E-5,-3.03021873309261));
#70672=CARTESIAN_POINT('',(-0.40705,-1.06687458785308E-14,-3.73478126690739));
#70673=CARTESIAN_POINT('Ctrl Pts',(-0.406704477435532,-0.000328489605546836,
-3.05978126690739));
#70674=CARTESIAN_POINT('Ctrl Pts',(-0.407035682029235,-0.0441750126328872,
-3.05721447960826));
#70675=CARTESIAN_POINT('Ctrl Pts',(-0.380281467477358,-0.223421781283086,
-3.04669829828972));
#70676=CARTESIAN_POINT('Ctrl Pts',(-0.118755506361991,-0.466457860652117,
-3.02823272295178));
#70677=CARTESIAN_POINT('Ctrl Pts',(0.3279772332983,-0.35230204001918,-3.00438454089354));
#70678=CARTESIAN_POINT('Ctrl Pts',(0.473748439217363,0.0851364820465625,
-2.9805363588353));
#70679=CARTESIAN_POINT('Ctrl Pts',(0.184794124598751,0.44445127173508,-2.95668817677707));
#70680=CARTESIAN_POINT('Ctrl Pts',(-0.26867312063451,0.396459958744006,
-2.93310314613443));
#70681=CARTESIAN_POINT('Ctrl Pts',(-0.407338799786674,0.130387800150095,
-2.9174675095112));
#70682=CARTESIAN_POINT('Ctrl Pts',(-0.407701968102319,-8.31109565068242E-5,
-2.90978126690739));
#70683=CARTESIAN_POINT('Ctrl Pts',(-0.407718443135198,-3.69130749903674E-5,
-3.03021873309261));
#70684=CARTESIAN_POINT('Ctrl Pts',(-0.407720987214861,-0.00200458601030759,
-3.03010280184093));
#70685=CARTESIAN_POINT('Ctrl Pts',(-0.406815955677249,-0.138892984777138,
-3.02203747656983));
#70686=CARTESIAN_POINT('Ctrl Pts',(-0.2545686693589,-0.408510181769555,
-3.00602275727932));
#70687=CARTESIAN_POINT('Ctrl Pts',(0.205748768093235,-0.435147353171444,
-2.98217457522109));
#70688=CARTESIAN_POINT('Ctrl Pts',(0.477265085335348,-0.0624805126738404,
-2.95832639316285));
#70689=CARTESIAN_POINT('Ctrl Pts',(0.310828915823958,0.367520286150906,
-2.93447821110462));
#70690=CARTESIAN_POINT('Ctrl Pts',(-0.140833011620641,0.460273655915389,
-2.91063002904639));
#70691=CARTESIAN_POINT('Ctrl Pts',(-0.385363902673548,0.210299061331091,
-2.89254353637572));
#70692=CARTESIAN_POINT('Ctrl Pts',(-0.40720506574647,0.0376968623643481,
-2.88240643772446));
#70693=CARTESIAN_POINT('Ctrl Pts',(-0.406879917492779,0.000366675793932139,
-2.88021873309261));
#70694=CARTESIAN_POINT('Origin',(0.,0.,-3.73478126690739));
#70695=CARTESIAN_POINT('',(-0.406515871833776,0.000234398840525714,-3.20978126690739));
#70696=CARTESIAN_POINT('',(-0.406769660729406,-0.000346827701298791,-3.18021873309261));
#70697=CARTESIAN_POINT('',(-0.40705,-1.06687458785308E-14,-3.73478126690739));
#70698=CARTESIAN_POINT('Ctrl Pts',(-0.406515871833776,0.000234398840525681,
-3.20978126690739));
#70699=CARTESIAN_POINT('Ctrl Pts',(-0.40607992506813,-0.0830599315404157,
-3.20491084372473));
#70700=CARTESIAN_POINT('Ctrl Pts',(-0.340605751677683,-0.302934358736486,
-3.19209102652267));
#70701=CARTESIAN_POINT('Ctrl Pts',(0.0193401667723502,-0.480949286387233,
-3.17132181530118));
#70702=CARTESIAN_POINT('Ctrl Pts',(0.414897370773675,-0.244019581286168,
-3.14747363324295));
#70703=CARTESIAN_POINT('Ctrl Pts',(0.429733826132711,0.216828851028994,
-3.12362545118471));
#70704=CARTESIAN_POINT('Ctrl Pts',(0.0502332080755313,0.478709177297012,
-3.09977726912648));
#70705=CARTESIAN_POINT('Ctrl Pts',(-0.329555527927946,0.32040500537278,
-3.07849587436737));
#70706=CARTESIAN_POINT('Ctrl Pts',(-0.406009934466403,0.091618587422811,
-3.06516387362767));
#70707=CARTESIAN_POINT('Ctrl Pts',(-0.406704477435532,-0.000328489605546836,
-3.05978126690739));
#70708=CARTESIAN_POINT('Ctrl Pts',(-0.406769660729406,-0.000346827701298773,
-3.18021873309261));
#70709=CARTESIAN_POINT('Ctrl Pts',(-0.407103008418297,-0.0416617513481845,
-3.1777991659574));
#70710=CARTESIAN_POINT('Ctrl Pts',(-0.382300719991004,-0.218324446081393,
-3.16743020480277));
#70711=CARTESIAN_POINT('Ctrl Pts',(-0.12736418971267,-0.464181203311474,
-3.14911184962874));
#70712=CARTESIAN_POINT('Ctrl Pts',(0.321403754809788,-0.358309005302331,
-3.12526366757049));
#70713=CARTESIAN_POINT('Ctrl Pts',(0.475242318068355,0.0763579342497911,
-3.10141548551227));
#70714=CARTESIAN_POINT('Ctrl Pts',(0.192984463138943,0.440956661874455,
-3.07756730345403));
#70715=CARTESIAN_POINT('Ctrl Pts',(-0.264128587748445,0.401115167263869,
-3.05383505264748));
#70716=CARTESIAN_POINT('Ctrl Pts',(-0.407546539933712,0.132918545043735,
-3.03805219586034));
#70717=CARTESIAN_POINT('Ctrl Pts',(-0.407718443135198,-3.69130749903674E-5,
-3.03021873309261));
#70718=CARTESIAN_POINT('Origin',(0.,0.,-3.73478126690739));
#70719=CARTESIAN_POINT('',(-0.407524236888043,0.000202371512057609,-3.35978126690739));
#70720=CARTESIAN_POINT('',(-0.406471795258815,0.000197138416556913,-3.33021873309261));
#70721=CARTESIAN_POINT('',(-0.40705,-1.06687458785308E-14,-3.73478126690739));
#70722=CARTESIAN_POINT('Ctrl Pts',(-0.407524236888043,0.000202371512057618,
-3.35978126690739));
#70723=CARTESIAN_POINT('Ctrl Pts',(-0.406696015914146,-0.121691487438068,
-3.3526072078412));
#70724=CARTESIAN_POINT('Ctrl Pts',(-0.283920138602621,-0.379991082756219,
-3.3374837547556));
#70725=CARTESIAN_POINT('Ctrl Pts',(0.155860105948259,-0.455439012791576,
-3.31441090765059));
#70726=CARTESIAN_POINT('Ctrl Pts',(0.467273406510021,-0.115419330027175,
-3.29056272559236));
#70727=CARTESIAN_POINT('Ctrl Pts',(0.349967170548287,0.330471523578635,
-3.26671454353412));
#70728=CARTESIAN_POINT('Ctrl Pts',(-0.0885127355860925,0.473133346833339,
-3.24286636147589));
#70729=CARTESIAN_POINT('Ctrl Pts',(-0.372795421348288,0.241157012369009,
-3.22388860260031));
#70730=CARTESIAN_POINT('Ctrl Pts',(-0.406791467470431,0.0528911813195563,
-3.21286023774414));
#70731=CARTESIAN_POINT('Ctrl Pts',(-0.406515871833776,0.000234398840525681,
-3.20978126690739));
#70732=CARTESIAN_POINT('Ctrl Pts',(-0.406471795258815,0.00019713841655692,
-3.33021873309261));
#70733=CARTESIAN_POINT('Ctrl Pts',(-0.406113950682387,-0.0805982389011809,
-3.32549553007387));
#70734=CARTESIAN_POINT('Ctrl Pts',(-0.343629442042593,-0.297885115520438,
-3.31282293303571));
#70735=CARTESIAN_POINT('Ctrl Pts',(0.0104433754015671,-0.481228201914669,
-3.29220094197814));
#70736=CARTESIAN_POINT('Ctrl Pts',(0.410310267884784,-0.251651262526424,
-3.26835275991991));
#70737=CARTESIAN_POINT('Ctrl Pts',(0.433672420198296,0.208841071520909,
-3.24450457786167));
#70738=CARTESIAN_POINT('Ctrl Pts',(0.0590798125780674,0.477698450045499,
-3.22065639580344));
#70739=CARTESIAN_POINT('Ctrl Pts',(-0.326218801964724,0.325400159805307,
-3.19922778088042));
#70740=CARTESIAN_POINT('Ctrl Pts',(-0.406007807509882,0.0940768285701207,
-3.18574855997681));
#70741=CARTESIAN_POINT('Ctrl Pts',(-0.406769660729406,-0.000346827701298773,
-3.18021873309261));
#70742=CARTESIAN_POINT('Origin',(4.52129938221115E-17,0.,-0.0249999999999999));
#70743=CARTESIAN_POINT('',(0.457029747534529,0.183521279061925,-0.0249999999999995));
#70744=CARTESIAN_POINT('Ctrl Pts',(-0.0460018146225333,-0.405020972964472,
-0.0249999999999997));
#70745=CARTESIAN_POINT('Ctrl Pts',(-0.0368688609768173,-0.407072845965971,
-0.0249999999999997));
#70746=CARTESIAN_POINT('Ctrl Pts',(-0.0276790887507462,-0.408785206362994,
-0.0249999999999986));
#70747=CARTESIAN_POINT('Ctrl Pts',(-0.0184481190379368,-0.410148694579132,
-0.0249999999999989));
#70748=CARTESIAN_POINT('Ctrl Pts',(-0.000736091208704569,-0.412764903057811,
-0.0249999999999994));
#70749=CARTESIAN_POINT('Ctrl Pts',(0.0171271945392099,-0.414098204546599,
-0.0250000000000001));
#70750=CARTESIAN_POINT('Ctrl Pts',(0.0350370752015178,-0.414220086012056,
-0.025));
#70751=CARTESIAN_POINT('Ctrl Pts',(0.0427871578566146,-0.414272827370261,
-0.0249999999999999));
#70752=CARTESIAN_POINT('Ctrl Pts',(0.0505460648098107,-0.414098441504754,
-0.0249999999999998));
#70753=CARTESIAN_POINT('Ctrl Pts',(0.058305636297932,-0.413701440723197,
-0.0249999999999998));
#70754=CARTESIAN_POINT('Ctrl Pts',(0.065639227935195,-0.413326234229375,
-0.0249999999999999));
#70755=CARTESIAN_POINT('Ctrl Pts',(0.0729656785645081,-0.412752439508174,
-0.0250000000000003));
#70756=CARTESIAN_POINT('Ctrl Pts',(0.0802705309395109,-0.411985704296353,
-0.0250000000000002));
#70757=CARTESIAN_POINT('Ctrl Pts',(0.0959965992620539,-0.410335057615571,
-0.0249999999999999));
#70758=CARTESIAN_POINT('Ctrl Pts',(0.111633086246646,-0.407790477600622,
-0.0250000000000002));
#70759=CARTESIAN_POINT('Ctrl Pts',(0.12711142996823,-0.404395753004662,
-0.0250000000000004));
#70760=CARTESIAN_POINT('Ctrl Pts',(0.137179327745643,-0.402187652394586,
-0.0250000000000005));
#70761=CARTESIAN_POINT('Ctrl Pts',(0.147180389015943,-0.399619615326678,
-0.0249999999999996));
#70762=CARTESIAN_POINT('Ctrl Pts',(0.15709598249321,-0.39670101471998,-0.0249999999999997));
#70763=CARTESIAN_POINT('Ctrl Pts',(0.16522061739264,-0.394309572956958,
-0.0249999999999997));
#70764=CARTESIAN_POINT('Ctrl Pts',(0.173292434393707,-0.391680787125226,
-0.0249999999999981));
#70765=CARTESIAN_POINT('Ctrl Pts',(0.18127262697246,-0.388829912162784,
-0.0249999999999984));
#70766=CARTESIAN_POINT('Ctrl Pts',(0.20372446637048,-0.380809129936173,
-0.0249999999999991));
#70767=CARTESIAN_POINT('Ctrl Pts',(0.22549026171249,-0.371025032773971,
-0.0250000000000013));
#70768=CARTESIAN_POINT('Ctrl Pts',(0.246351583123323,-0.35961031708094,
-0.0250000000000009));
#70769=CARTESIAN_POINT('Ctrl Pts',(0.259270215793116,-0.35254161245939,
-0.0250000000000007));
#70770=CARTESIAN_POINT('Ctrl Pts',(0.271842146168147,-0.344846493770231,
-0.0249999999999993));
#70771=CARTESIAN_POINT('Ctrl Pts',(0.284013996361614,-0.336546617664755,
-0.0249999999999994));
#70772=CARTESIAN_POINT('Ctrl Pts',(0.293911077818581,-0.32979788607564,
-0.0249999999999996));
#70773=CARTESIAN_POINT('Ctrl Pts',(0.303543649983073,-0.322649170726144,
-0.0249999999999999));
#70774=CARTESIAN_POINT('Ctrl Pts',(0.312881312926065,-0.315108752373828,
-0.025));
#70775=CARTESIAN_POINT('Ctrl Pts',(0.317290196363017,-0.311548458349062,
-0.025));
#70776=CARTESIAN_POINT('Ctrl Pts',(0.321632703673732,-0.307901054442145,
-0.0249999999999991));
#70777=CARTESIAN_POINT('Ctrl Pts',(0.325895512535387,-0.304176694866598,
-0.0249999999999992));
#70778=CARTESIAN_POINT('Ctrl Pts',(0.341087497923146,-0.290903658686291,
-0.0249999999999993));
#70779=CARTESIAN_POINT('Ctrl Pts',(0.355302925077213,-0.276627230860661,
-0.0250000000000004));
#70780=CARTESIAN_POINT('Ctrl Pts',(0.368414610711014,-0.261411535021156,
-0.0250000000000003));
#70781=CARTESIAN_POINT('Ctrl Pts',(0.38096744800188,-0.246844364981002,
-0.0250000000000003));
#70782=CARTESIAN_POINT('Ctrl Pts',(0.392509163584889,-0.231416085721514,
-0.0250000000000002));
#70783=CARTESIAN_POINT('Ctrl Pts',(0.403021877045189,-0.215260169684606,
-0.0250000000000003));
#70784=CARTESIAN_POINT('Ctrl Pts',(0.41029062462888,-0.204089573615468,
-0.0250000000000003));
#70785=CARTESIAN_POINT('Ctrl Pts',(0.417067159241788,-0.192570686603153,
-0.0249999999999998));
#70786=CARTESIAN_POINT('Ctrl Pts',(0.423341039846872,-0.180743491987121,
-0.0249999999999996));
#70787=CARTESIAN_POINT('Ctrl Pts',(0.426046091107006,-0.175644069522175,
-0.0249999999999995));
#70788=CARTESIAN_POINT('Ctrl Pts',(0.428657339542585,-0.170487505211596,
-0.0249999999999992));
#70789=CARTESIAN_POINT('Ctrl Pts',(0.431168090704968,-0.165289798304669,
-0.0249999999999992));
#70790=CARTESIAN_POINT('Ctrl Pts',(0.441952230009222,-0.142964688518082,
-0.0249999999999993));
#70791=CARTESIAN_POINT('Ctrl Pts',(0.450916595356233,-0.119826320055446,
-0.0249999999999978));
#70792=CARTESIAN_POINT('Ctrl Pts',(0.458031178347495,-0.0961506920430363,
-0.0249999999999986));
#70793=CARTESIAN_POINT('Ctrl Pts',(0.462087263293214,-0.0826530129127887,
-0.0249999999999991));
#70794=CARTESIAN_POINT('Ctrl Pts',(0.465541456021857,-0.0689799331539447,
-0.0249999999999998));
#70795=CARTESIAN_POINT('Ctrl Pts',(0.468382162239584,-0.0551781242986939,
-0.0249999999999996));
#70796=CARTESIAN_POINT('Ctrl Pts',(0.471104443522198,-0.0419516928999102,
-0.0249999999999995));
#70797=CARTESIAN_POINT('Ctrl Pts',(0.473263317184127,-0.0286069608577007,
-0.0249999999999989));
#70798=CARTESIAN_POINT('Ctrl Pts',(0.474858192805233,-0.0151757738305842,
-0.024999999999999));
#70799=CARTESIAN_POINT('Ctrl Pts',(0.475856795922803,-0.00676607400168343,
-0.0249999999999991));
#70800=CARTESIAN_POINT('Ctrl Pts',(0.476634321335288,0.0016835602057796,
-0.0250000000000001));
#70801=CARTESIAN_POINT('Ctrl Pts',(0.477188356191574,0.0101317298598468,
-0.0250000000000001));
#70802=CARTESIAN_POINT('Ctrl Pts',(0.478859492768636,0.0356139628961899,
-0.0250000000000002));
#70803=CARTESIAN_POINT('Ctrl Pts',(0.478509242868913,0.0611272410931792,
-0.0250000000000001));
#70804=CARTESIAN_POINT('Ctrl Pts',(0.476172029705562,0.0864508239821215,
-0.0249999999999998));
#70805=CARTESIAN_POINT('Ctrl Pts',(0.473839980058189,0.111718460444394,
-0.0249999999999995));
#70806=CARTESIAN_POINT('Ctrl Pts',(0.469529905743689,0.136798534533325,
-0.025));
#70807=CARTESIAN_POINT('Ctrl Pts',(0.46322590299162,0.161480326316489,-0.0250000000000002));
#70808=CARTESIAN_POINT('Ctrl Pts',(0.461339801487617,0.168864898696068,
-0.0250000000000003));
#70809=CARTESIAN_POINT('Ctrl Pts',(0.459274862212137,0.17621380430208,-0.0249999999999995));
#70810=CARTESIAN_POINT('Ctrl Pts',(0.457029747534529,0.183521279061925,
-0.0249999999999995));
#70811=CARTESIAN_POINT('',(-0.4925,-6.03138548580071E-17,-0.0249999999999999));
#70812=CARTESIAN_POINT('Origin',(0.,0.,-0.0249999999999999));
#70813=CARTESIAN_POINT('',(0.134559949224566,0.474484556402355,-0.0249999999999999));
#70814=CARTESIAN_POINT('Origin',(0.,0.,-0.0249999999999999));
#70815=CARTESIAN_POINT('Ctrl Pts',(0.134559949224566,0.474484556402355,
-0.0249999999999999));
#70816=CARTESIAN_POINT('Ctrl Pts',(0.123555094791079,0.476693790868335,
-0.025));
#70817=CARTESIAN_POINT('Ctrl Pts',(0.112488500107867,0.478496855056247,
-0.0250000000000006));
#70818=CARTESIAN_POINT('Ctrl Pts',(0.101375304595012,0.479878948430273,
-0.0250000000000004));
#70819=CARTESIAN_POINT('Ctrl Pts',(0.0820161039435544,0.482286556837401,
-0.0250000000000001));
#70820=CARTESIAN_POINT('Ctrl Pts',(0.0625152503388465,0.483417645176772,
-0.0249999999999985));
#70821=CARTESIAN_POINT('Ctrl Pts',(0.0429779460829366,0.483316943501375,
-0.0249999999999985));
#70822=CARTESIAN_POINT('Ctrl Pts',(0.0325576452803804,0.483263233852632,
-0.0249999999999985));
#70823=CARTESIAN_POINT('Ctrl Pts',(0.0221270158330046,0.482858819240042,
-0.0249999999999989));
#70824=CARTESIAN_POINT('Ctrl Pts',(0.0117026104786621,0.482108568565393,
-0.0249999999999988));
#70825=CARTESIAN_POINT('Ctrl Pts',(0.00498825037415073,0.481625332061534,
-0.0249999999999987));
#70826=CARTESIAN_POINT('Ctrl Pts',(-0.0017201083185829,0.480998723263594,
-0.0249999999999994));
#70827=CARTESIAN_POINT('Ctrl Pts',(-0.00840971123782733,0.480231503030802,
-0.0249999999999995));
#70828=CARTESIAN_POINT('Ctrl Pts',(-0.03375204596074,0.47732502977965,-0.0249999999999997));
#70829=CARTESIAN_POINT('Ctrl Pts',(-0.0588627694554139,0.472401938366701,
-0.0249999999999997));
#70830=CARTESIAN_POINT('Ctrl Pts',(-0.0835002259753155,0.465549384270615,
-0.0250000000000004));
#70831=CARTESIAN_POINT('Ctrl Pts',(-0.0924179898816985,0.463069036531178,
-0.0250000000000006));
#70832=CARTESIAN_POINT('Ctrl Pts',(-0.101273541185288,0.460335451608263,
-0.0250000000000007));
#70833=CARTESIAN_POINT('Ctrl Pts',(-0.110054517088707,0.457351333110056,
-0.0250000000000009));
#70834=CARTESIAN_POINT('Ctrl Pts',(-0.115349721097155,0.455551816016833,
-0.0250000000000009));
#70835=CARTESIAN_POINT('Ctrl Pts',(-0.120616282206451,0.453661581487259,
-0.0249999999999976));
#70836=CARTESIAN_POINT('Ctrl Pts',(-0.12584278956843,0.451684861751622,
-0.0249999999999977));
#70837=CARTESIAN_POINT('Ctrl Pts',(-0.149125860671454,0.442878960799412,
-0.0249999999999981));
#70838=CARTESIAN_POINT('Ctrl Pts',(-0.171665873862567,0.432343672613944,
-0.0249999999999992));
#70839=CARTESIAN_POINT('Ctrl Pts',(-0.193238606369979,0.42015887610055,
-0.0249999999999992));
#70840=CARTESIAN_POINT('Ctrl Pts',(-0.21426277833423,0.40828391973334,-0.0249999999999992));
#70841=CARTESIAN_POINT('Ctrl Pts',(-0.234369248412146,0.394841501860522,
-0.0249999999999994));
#70842=CARTESIAN_POINT('Ctrl Pts',(-0.253316286172159,0.379871074180984,
-0.0249999999999996));
#70843=CARTESIAN_POINT('Ctrl Pts',(-0.258074354348964,0.376111630808495,
-0.0249999999999996));
#70844=CARTESIAN_POINT('Ctrl Pts',(-0.262759091303972,0.372255683264206,
-0.0249999999999996));
#70845=CARTESIAN_POINT('Ctrl Pts',(-0.267366205423779,0.368303587897705,
-0.0249999999999997));
#70846=CARTESIAN_POINT('Ctrl Pts',(-0.272131127547925,0.364216120958777,
-0.0249999999999997));
#70847=CARTESIAN_POINT('Ctrl Pts',(-0.276807128535211,0.36003072093939,
-0.0249999999999994));
#70848=CARTESIAN_POINT('Ctrl Pts',(-0.281384804472264,0.35575357543162,
-0.0249999999999993));
#70849=CARTESIAN_POINT('Ctrl Pts',(-0.294787805690782,0.343230498822286,
-0.0249999999999992));
#70850=CARTESIAN_POINT('Ctrl Pts',(-0.307364443444733,0.329908587482838,
-0.0249999999999991));
#70851=CARTESIAN_POINT('Ctrl Pts',(-0.319013982928522,0.31581173345222,
-0.0249999999999992));
#70852=CARTESIAN_POINT('Ctrl Pts',(-0.332336765116745,0.299690124864134,
-0.0249999999999993));
#70853=CARTESIAN_POINT('Ctrl Pts',(-0.344447706547327,0.282554571833339,
-0.0249999999999993));
#70854=CARTESIAN_POINT('Ctrl Pts',(-0.355285026905852,0.264573570396947,
-0.024999999999999));
#70855=CARTESIAN_POINT('Ctrl Pts',(-0.36027217617748,0.256299021407897,
-0.0249999999999989));
#70856=CARTESIAN_POINT('Ctrl Pts',(-0.364989210369154,0.247845308384308,
-0.0250000000000001));
#70857=CARTESIAN_POINT('Ctrl Pts',(-0.369427973343093,0.239228558655422,
-0.0250000000000002));
#70858=CARTESIAN_POINT('Ctrl Pts',(-0.372691078878274,0.23289405422239,
-0.0250000000000002));
#70859=CARTESIAN_POINT('Ctrl Pts',(-0.375804878242441,0.226468396851928,
-0.0250000000000003));
#70860=CARTESIAN_POINT('Ctrl Pts',(-0.378755924034929,0.219981221274517,
-0.0250000000000002));
#70861=CARTESIAN_POINT('Ctrl Pts',(-0.388473620732812,0.198619165542392,
-0.0249999999999998));
#70862=CARTESIAN_POINT('Ctrl Pts',(-0.396457052544794,0.176542967218711,
-0.0250000000000005));
#70863=CARTESIAN_POINT('Ctrl Pts',(-0.402628366384551,0.153995847400014,
-0.025));
#70864=CARTESIAN_POINT('Ctrl Pts',(-0.405848553416808,0.142230776826689,
-0.0249999999999998));
#70865=CARTESIAN_POINT('Ctrl Pts',(-0.40857451584816,0.130337276741726,
-0.0249999999999988));
#70866=CARTESIAN_POINT('Ctrl Pts',(-0.410789527386875,0.118349752967864,
-0.0249999999999986));
#70867=CARTESIAN_POINT('Ctrl Pts',(-0.413173307917742,0.105448860450609,
-0.0249999999999984));
#70868=CARTESIAN_POINT('Ctrl Pts',(-0.414965336322946,0.0924389960516608,
-0.0249999999999991));
#70869=CARTESIAN_POINT('Ctrl Pts',(-0.416156410828275,0.0793583313213072,
-0.0249999999999989));
#70870=CARTESIAN_POINT('Ctrl Pts',(-0.41678540546089,0.0724505620175296,
-0.0249999999999988));
#70871=CARTESIAN_POINT('Ctrl Pts',(-0.417246607084851,0.0655199159985511,
-0.0250000000000001));
#70872=CARTESIAN_POINT('Ctrl Pts',(-0.417537811172664,0.0585969702267026,
-0.025));
#70873=CARTESIAN_POINT('Ctrl Pts',(-0.418493406177842,0.0358791146829457,
-0.0249999999999998));
#70874=CARTESIAN_POINT('Ctrl Pts',(-0.41762892133668,0.0131899923548943,
-0.0249999999999987));
#70875=CARTESIAN_POINT('Ctrl Pts',(-0.414931126870213,-0.00927360260191209,
-0.024999999999999));
#70876=CARTESIAN_POINT('Ctrl Pts',(-0.412300309655844,-0.0311795013067703,
-0.0249999999999994));
#70877=CARTESIAN_POINT('Ctrl Pts',(-0.407925720268869,-0.0528720434064392,
-0.0250000000000002));
#70878=CARTESIAN_POINT('Ctrl Pts',(-0.401749711262537,-0.0741500679289064,
-0.0250000000000002));
#70879=CARTESIAN_POINT('Ctrl Pts',(-0.400376913363202,-0.0788797286752727,
-0.0250000000000002));
#70880=CARTESIAN_POINT('Ctrl Pts',(-0.39891494101082,-0.0835887978684164,
-0.0249999999999999));
#70881=CARTESIAN_POINT('Ctrl Pts',(-0.39736287274916,-0.0882748540669144,
-0.0249999999999999));
#70882=CARTESIAN_POINT('Ctrl Pts',(-0.179217368492187,0.365473442716069,
-3.50683458050225));
#70883=CARTESIAN_POINT('Ctrl Pts',(-0.240065670223399,0.33563523495891,
-3.50285988349255));
#70884=CARTESIAN_POINT('Ctrl Pts',(-0.345646884548746,0.244990880907642,
-3.49491048947314));
#70885=CARTESIAN_POINT('Ctrl Pts',(-0.448647636125016,-0.0162619182297498,
-3.47901170143431));
#70886=CARTESIAN_POINT('Ctrl Pts',(-0.305996566448462,-0.371515294606295,
-3.45913821638579));
#70887=CARTESIAN_POINT('Ctrl Pts',(0.147593574246178,-0.458419355808066,
-3.43529003432755));
#70888=CARTESIAN_POINT('Ctrl Pts',(0.464962259161517,-0.123953347438615,
-3.41144185226931));
#70889=CARTESIAN_POINT('Ctrl Pts',(0.356070675898753,0.323893827689701,
-3.38759367021108));
#70890=CARTESIAN_POINT('Ctrl Pts',(-0.0797710380057583,0.474714264786181,
-3.36374548815284));
#70891=CARTESIAN_POINT('Ctrl Pts',(-0.44230355372976,0.189825171767689,
-3.33989730609462));
#70892=CARTESIAN_POINT('Ctrl Pts',(-0.399022082550972,-0.269202152090369,
-3.31604912403637));
#70893=CARTESIAN_POINT('Ctrl Pts',(0.0104433754015671,-0.481228201914669,
-3.29220094197814));
#70894=CARTESIAN_POINT('Ctrl Pts',(0.410310267884784,-0.251651262526424,
-3.26835275991991));
#70895=CARTESIAN_POINT('Ctrl Pts',(0.433672420198296,0.208841071520909,
-3.24450457786167));
#70896=CARTESIAN_POINT('Ctrl Pts',(0.0590798125780674,0.477698450045499,
-3.22065639580344));
#70897=CARTESIAN_POINT('Ctrl Pts',(-0.369723987360064,0.30820371761162,
-3.1968082137452));
#70898=CARTESIAN_POINT('Ctrl Pts',(-0.459259315099757,-0.144106794284832,
-3.17296003168697));
#70899=CARTESIAN_POINT('Ctrl Pts',(-0.12736418971267,-0.464181203311474,
-3.14911184962874));
#70900=CARTESIAN_POINT('Ctrl Pts',(0.321403754809788,-0.358309005302331,
-3.12526366757049));
#70901=CARTESIAN_POINT('Ctrl Pts',(0.475242318068355,0.0763579342497911,
-3.10141548551227));
#70902=CARTESIAN_POINT('Ctrl Pts',(0.192984463138943,0.440956661874455,
-3.07756730345403));
#70903=CARTESIAN_POINT('Ctrl Pts',(-0.266361569718098,0.400920542894828,
-3.0537191213958));
#70904=CARTESIAN_POINT('Ctrl Pts',(-0.481286411713864,-0.00701204226000944,
-3.02987093933756));
#70905=CARTESIAN_POINT('Ctrl Pts',(-0.2545686693589,-0.408510181769555,
-3.00602275727932));
#70906=CARTESIAN_POINT('Ctrl Pts',(0.205748768093235,-0.435147353171444,
-2.98217457522109));
#70907=CARTESIAN_POINT('Ctrl Pts',(0.477265085335348,-0.0624805126738404,
-2.95832639316285));
#70908=CARTESIAN_POINT('Ctrl Pts',(0.310828915823958,0.367520286150906,
-2.93447821110462));
#70909=CARTESIAN_POINT('Ctrl Pts',(-0.140833011620641,0.460273655915389,
-2.91063002904639));
#70910=CARTESIAN_POINT('Ctrl Pts',(-0.463262424270052,0.130666376597655,
-2.88678184698815));
#70911=CARTESIAN_POINT('Ctrl Pts',(-0.360588605408013,-0.318844214750719,
-2.86293366492992));
#70912=CARTESIAN_POINT('Ctrl Pts',(0.0729719274013494,-0.475773973046388,
-2.83908548287168));
#70913=CARTESIAN_POINT('Ctrl Pts',(0.439571272608378,-0.196119534836683,
-2.81523730081345));
#70914=CARTESIAN_POINT('Ctrl Pts',(0.402807084347494,0.263499959076195,
-2.79138911875521));
#70915=CARTESIAN_POINT('Ctrl Pts',(-0.00358473645388183,0.481324137455872,
-2.76754093669698));
#70916=CARTESIAN_POINT('Ctrl Pts',(-0.406687097619119,0.257471125113484,
-2.74369275463875));
#70917=CARTESIAN_POINT('Ctrl Pts',(-0.436601411880274,-0.202644967317561,
-2.71984457258051));
#70918=CARTESIAN_POINT('Ctrl Pts',(-0.0658774242972122,-0.476808075228433,
-2.69599639052228));
#70919=CARTESIAN_POINT('Ctrl Pts',(0.365297626161182,-0.313438063988078,
-2.67214820846404));
#70920=CARTESIAN_POINT('Ctrl Pts',(0.461264826549058,0.137551937187166,
-2.64830002640581));
#70921=CARTESIAN_POINT('Ctrl Pts',(0.133961850108581,0.462320233551161,
-2.62445184434757));
#70922=CARTESIAN_POINT('Ctrl Pts',(-0.316268461607078,0.362849880567804,
-2.60060366228934));
#70923=CARTESIAN_POINT('Ctrl Pts',(-0.47628152725319,-0.0695821991079605,
-2.5767554802311));
#70924=CARTESIAN_POINT('Ctrl Pts',(-0.199244649661891,-0.438163605536162,
-2.55290729817287));
#70925=CARTESIAN_POINT('Ctrl Pts',(0.260624980917576,-0.404673195253975,
-2.52905911611463));
#70926=CARTESIAN_POINT('Ctrl Pts',(0.481337460529596,0.000157245861404591,
-2.5052109340564));
#70927=CARTESIAN_POINT('Ctrl Pts',(0.260360523766897,0.404843393547639,
-2.48136275199817));
#70928=CARTESIAN_POINT('Ctrl Pts',(-0.199530890300541,0.438033331438621,
-2.45751456993993));
#70929=CARTESIAN_POINT('Ctrl Pts',(-0.476326888547635,0.0692709959641985,
-2.4336663878817));
#70930=CARTESIAN_POINT('Ctrl Pts',(-0.3160313186988,-0.363056443596366,
-2.40981820582346));
#70931=CARTESIAN_POINT('Ctrl Pts',(0.134263887909296,-0.462232608151807,
-2.38597002376523));
#70932=CARTESIAN_POINT('Ctrl Pts',(0.461354600469472,-0.137250531004422,
-2.36212184170699));
#70933=CARTESIAN_POINT('Ctrl Pts',(0.365092757010119,0.313676671772215,
-2.33827365964876));
#70934=CARTESIAN_POINT('Ctrl Pts',(-0.0661889425581167,0.476764931091184,
-2.31442547759052));
#70935=CARTESIAN_POINT('Ctrl Pts',(-0.436733720930171,0.202359661587554,
-2.29057729553229));
#70936=CARTESIAN_POINT('Ctrl Pts',(-0.40651878677836,-0.257736787501498,
-2.26672911347405));
#70937=CARTESIAN_POINT('Ctrl Pts',(-0.00327025270698847,-0.481326376882232,
-2.24288093141582));
#70938=CARTESIAN_POINT('Ctrl Pts',(0.402979161470327,-0.263236720569178,
-2.21903274935758));
#70939=CARTESIAN_POINT('Ctrl Pts',(0.4394430400586,0.196406695861922,-2.19518456729935));
#70940=CARTESIAN_POINT('Ctrl Pts',(0.0726610551733367,0.47582154921403,
-2.17133638524111));
#70941=CARTESIAN_POINT('Ctrl Pts',(-0.3607968518755,0.318608548711537,-2.14748820318288));
#70942=CARTESIAN_POINT('Ctrl Pts',(-0.463176951767192,-0.13096903064082,
-2.12364002112464));
#70943=CARTESIAN_POINT('Ctrl Pts',(-0.14053225246876,-0.460365573920769,
-2.09979183906641));
#70944=CARTESIAN_POINT('Ctrl Pts',(0.311068976634055,-0.367317121042818,
-2.07594365700817));
#70945=CARTESIAN_POINT('Ctrl Pts',(0.477224160065282,0.0627923298288068,
-2.05209547494994));
#70946=CARTESIAN_POINT('Ctrl Pts',(0.205464412655191,0.435281691284622,
-2.02824729289171));
#70947=CARTESIAN_POINT('Ctrl Pts',(-0.254835525272372,0.408343765342997,
-2.00439911083347));
#70948=CARTESIAN_POINT('Ctrl Pts',(-0.481290887078107,0.00669758545379794,
-1.98055092877524));
#70949=CARTESIAN_POINT('Ctrl Pts',(-0.266099569678556,-0.401094495913658,
-1.956702746717));
#70950=CARTESIAN_POINT('Ctrl Pts',(0.193272542416614,-0.440830466260172,
-1.93285456465877));
#70951=CARTESIAN_POINT('Ctrl Pts',(0.475292082851708,-0.0760474300277662,
-1.90900638260053));
#70952=CARTESIAN_POINT('Ctrl Pts',(0.321169623344976,0.358518965573356,
-1.8851582005423));
#70953=CARTESIAN_POINT('Ctrl Pts',(-0.127667532450826,0.464097809511379,
-1.86131001848406));
#70954=CARTESIAN_POINT('Ctrl Pts',(-0.459353204054721,0.143806848098432,
-1.83746183642583));
#70955=CARTESIAN_POINT('Ctrl Pts',(-0.369522859877177,-0.308445508418479,
-1.8136136543676));
#70956=CARTESIAN_POINT('Ctrl Pts',(0.0593925331488187,-0.477659190889811,
-1.78976547230936));
#70957=CARTESIAN_POINT('Ctrl Pts',(0.433807590226198,-0.208558745435148,
-1.76591729025113));
#70958=CARTESIAN_POINT('Ctrl Pts',(0.410148038410438,0.251921341341723,
-1.74206910819289));
#70959=CARTESIAN_POINT('Ctrl Pts',(0.0101245785925387,0.481230992916775,
-1.71822092613466));
#70960=CARTESIAN_POINT('Ctrl Pts',(-0.39918949244157,0.268948925931271,
-1.69437274407642));
#70961=CARTESIAN_POINT('Ctrl Pts',(-0.442195539692441,-0.190128588885139,
-1.67052456201819));
#70962=CARTESIAN_POINT('Ctrl Pts',(-0.0794299488178135,-0.474738516307812,
-1.64667637995995));
#70963=CARTESIAN_POINT('Ctrl Pts',(0.356222900192536,-0.323714412737155,
-1.62282819790172));
#70964=CARTESIAN_POINT('Ctrl Pts',(0.464995134691316,0.124359560745234,
-1.59898001584348));
#70965=CARTESIAN_POINT('Ctrl Pts',(0.147074151851645,0.458317542204598,
-1.57513183378525));
#70966=CARTESIAN_POINT('Ctrl Pts',(-0.305806400151182,0.371709861668907,
-1.55128365172701));
#70967=CARTESIAN_POINT('Ctrl Pts',(-0.478070001506081,-0.0559897249083942,
-1.52743546966878));
#70968=CARTESIAN_POINT('Ctrl Pts',(-0.211642503026044,-0.432311492500735,
-1.50358728761054));
#70969=CARTESIAN_POINT('Ctrl Pts',(0.24899438347629,-0.411931514493132,
-1.47973910555231));
#70970=CARTESIAN_POINT('Ctrl Pts',(0.481146697435232,-0.0135510583539467,
-1.45589092349407));
#70971=CARTESIAN_POINT('Ctrl Pts',(0.271784644847739,0.397264247649257,
-1.43204274143584));
#70972=CARTESIAN_POINT('Ctrl Pts',(-0.186974994684948,0.443538191137929,
-1.40819455937761));
#70973=CARTESIAN_POINT('Ctrl Pts',(-0.474160877651511,0.0828084400293316,
-1.38434637731937));
#70974=CARTESIAN_POINT('Ctrl Pts',(-0.32624278785187,-0.353908772157435,
-1.36049819526114));
#70975=CARTESIAN_POINT('Ctrl Pts',(0.121045283258203,-0.465868881807192,
-1.3366500132029));
#70976=CARTESIAN_POINT('Ctrl Pts',(0.457258640884715,-0.150333998056345,
-1.31280183114467));
#70977=CARTESIAN_POINT('Ctrl Pts',(0.373878015523797,0.303151785650903,
-1.28895364908643));
#70978=CARTESIAN_POINT('Ctrl Pts',(-0.0525840776504784,0.478456571083512,
-1.2651054670282));
#70979=CARTESIAN_POINT('Ctrl Pts',(-0.430793473969433,0.214715529062733,
-1.24125728496997));
#70980=CARTESIAN_POINT('Ctrl Pts',(-0.413694103158059,-0.246054800090533,
-1.21740910291173));
#70981=CARTESIAN_POINT('Ctrl Pts',(-0.0169768509947866,-0.481038004907766,
-1.19356092085349));
#70982=CARTESIAN_POINT('Ctrl Pts',(0.395318859158266,-0.274606582639873,
-1.16971273879526));
#70983=CARTESIAN_POINT('Ctrl Pts',(0.444858352516096,0.183811919722327,
-1.14586455673703));
#70984=CARTESIAN_POINT('Ctrl Pts',(0.0861827323523932,0.473559196172579,
-1.12201637467879));
#70985=CARTESIAN_POINT('Ctrl Pts',(-0.35157669880833,0.328754620485218,
-1.09816819262056));
#70986=CARTESIAN_POINT('Ctrl Pts',(-0.466719006554749,-0.117724868043632,
-1.07432001056232));
#70987=CARTESIAN_POINT('Ctrl Pts',(-0.153586221418629,-0.456176553787775,
-1.05047182850409));
#70988=CARTESIAN_POINT('Ctrl Pts',(0.300481799522643,-0.376027211503337,
-1.02662364644585));
#70989=CARTESIAN_POINT('Ctrl Pts',(0.478818880020692,0.0491757640619698,
-1.00277546438762));
#70990=CARTESIAN_POINT('Ctrl Pts',(0.217777667724211,0.429253611605008,
-0.978927282329384));
#70991=CARTESIAN_POINT('Ctrl Pts',(-0.243102740239076,0.415435715031318,
-0.955079100271148));
#70992=CARTESIAN_POINT('Ctrl Pts',(-0.480904920845782,0.0204017828066685,
-0.931230918212915));
#70993=CARTESIAN_POINT('Ctrl Pts',(-0.277414596218298,-0.393353425611565,
-0.907382736154679));
#70994=CARTESIAN_POINT('Ctrl Pts',(0.180639524384169,-0.446155956886755,
-0.883534554096447));
#70995=CARTESIAN_POINT('Ctrl Pts',(0.472933502380155,-0.0895526546900201,
-0.85968637203821));
#70996=CARTESIAN_POINT('Ctrl Pts',(0.331249783271615,0.34922679839552,-0.835838189979976));
#70997=CARTESIAN_POINT('Ctrl Pts',(-0.114398483465715,0.467545465827366,
-0.811990007921742));
#70998=CARTESIAN_POINT('Ctrl Pts',(-0.455071335783922,0.15683065703141,
-0.788141825863506));
#70999=CARTESIAN_POINT('Ctrl Pts',(-0.378157340626862,-0.29779657715142,
-0.764293643805273));
#71000=CARTESIAN_POINT('Ctrl Pts',(0.0457649569583762,-0.479156909945254,
-0.740445461747037));
#71001=CARTESIAN_POINT('Ctrl Pts',(0.427691983500448,-0.220828763743674,
-0.716597279688803));
#71002=CARTESIAN_POINT('Ctrl Pts',(0.417156261778369,0.240138353613306,
-0.692749097630569));
#71003=CARTESIAN_POINT('Ctrl Pts',(0.0238256801714527,0.480747451989572,
-0.668900915572333));
#71004=CARTESIAN_POINT('Ctrl Pts',(-0.391368046757949,0.28020854321486,
-0.6450527335141));
#71005=CARTESIAN_POINT('Ctrl Pts',(-0.447430938281907,-0.177457969559079,
-0.621204551455864));
#71006=CARTESIAN_POINT('Ctrl Pts',(-0.0929180364960938,-0.472283827945071,
-0.59735636939763));
#71007=CARTESIAN_POINT('Ctrl Pts',(0.346859190705059,-0.333728149797965,
-0.573508187339396));
#71008=CARTESIAN_POINT('Ctrl Pts',(0.468348216506024,0.11106629839706,-0.549660005281161));
#71009=CARTESIAN_POINT('Ctrl Pts',(0.160067142708905,0.453943042521375,
-0.525811823222927));
#71010=CARTESIAN_POINT('Ctrl Pts',(-0.29509625915887,0.380268295638099,
-0.501963641164692));
#71011=CARTESIAN_POINT('Ctrl Pts',(-0.479470635149994,-0.0423518307353366,
-0.478115459106457));
#71012=CARTESIAN_POINT('Ctrl Pts',(-0.223868678851143,-0.426108666062932,
-0.454267277048223));
#71013=CARTESIAN_POINT('Ctrl Pts',(0.23716182206986,-0.418855661485411,
-0.430419094989988));
#71014=CARTESIAN_POINT('Ctrl Pts',(0.48056554579435,-0.0272483592525269,
-0.406570912931754));
#71015=CARTESIAN_POINT('Ctrl Pts',(0.282988398107527,0.389362803648974,
-0.382722730873519));
#71016=CARTESIAN_POINT('Ctrl Pts',(-0.174267639443746,0.448683269698852,
-0.358874548815284));
#71017=CARTESIAN_POINT('Ctrl Pts',(-0.471609778146528,0.0962786348866224,
-0.33502636675705));
#71018=CARTESIAN_POINT('Ctrl Pts',(-0.336190415025481,-0.34447385717225,
-0.311178184698814));
#71019=CARTESIAN_POINT('Ctrl Pts',(0.107730056479299,-0.469127483873643,
-0.28733000264058));
#71020=CARTESIAN_POINT('Ctrl Pts',(0.452788709608233,-0.16329500394726,
-0.263481820582346));
#71021=CARTESIAN_POINT('Ctrl Pts',(0.382365767560564,0.292380003087804,
-0.239633638524111));
#71022=CARTESIAN_POINT('Ctrl Pts',(-0.0389476842058911,0.479761919026928,
-0.215785456465877));
#71023=CARTESIAN_POINT('Ctrl Pts',(-0.424482390454294,0.226893652782127,
-0.191937274407642));
#71024=CARTESIAN_POINT('Ctrl Pts',(-0.42057479669623,-0.234166376920184,
-0.168089092349408));
#71025=CARTESIAN_POINT('Ctrl Pts',(-0.0305910094676718,-0.480372488794092,
-0.144240910291172));
#71026=CARTESIAN_POINT('Ctrl Pts',(0.387186688863383,-0.285728547318658,
-0.120392728232938));
#71027=CARTESIAN_POINT('Ctrl Pts',(0.450204815655376,0.171019861124231,
-0.0965445461747034));
#71028=CARTESIAN_POINT('Ctrl Pts',(0.0990560712614088,0.471004678905531,
-0.0726963641164688));
#71029=CARTESIAN_POINT('Ctrl Pts',(-0.267488470034939,0.360553837565826,
-0.0528228790679404));
#71030=CARTESIAN_POINT('Ctrl Pts',(-0.407203348846865,0.116951841430801,
-0.0369240910291168));
#71031=CARTESIAN_POINT('Ctrl Pts',(-0.412059904948337,-0.022117226311166,
-0.0289746970097056));
#71032=CARTESIAN_POINT('Ctrl Pts',(-0.39736287274916,-0.0882748540669144,
-0.0249999999999999));
#71033=CARTESIAN_POINT('Ctrl Pts',(-0.191758108071809,0.391047455474607,
-3.49038972033484));
#71034=CARTESIAN_POINT('Ctrl Pts',(-0.256864271149238,0.359121318427148,
-3.48641502332513));
#71035=CARTESIAN_POINT('Ctrl Pts',(-0.36983353343274,0.262134123567069,
-3.47846562930572));
#71036=CARTESIAN_POINT('Ctrl Pts',(-0.480041765025547,-0.0173998463407366,
-3.46256684126689));
#71037=CARTESIAN_POINT('Ctrl Pts',(-0.327408683389887,-0.397512086093095,
-3.44269335621837));
#71038=CARTESIAN_POINT('Ctrl Pts',(0.157921438078905,-0.490497261023478,
-3.41884517416013));
#71039=CARTESIAN_POINT('Ctrl Pts',(0.497498004193129,-0.132626985843913,
-3.39499699210189));
#71040=CARTESIAN_POINT('Ctrl Pts',(0.380986729827876,0.346558305907843,
-3.37114881004367));
#71041=CARTESIAN_POINT('Ctrl Pts',(-0.0853530182682902,0.507932406640973,
-3.34730062798542));
#71042=CARTESIAN_POINT('Ctrl Pts',(-0.473253755315321,0.20310819263126,
-3.3234524459272));
#71043=CARTESIAN_POINT('Ctrl Pts',(-0.426943662171806,-0.288039579020821,
-3.29960426386895));
#71044=CARTESIAN_POINT('Ctrl Pts',(0.0111741508411632,-0.514902156673387,
-3.27575608181073));
#71045=CARTESIAN_POINT('Ctrl Pts',(0.439021738540113,-0.269260565546433,
-3.25190789975249));
#71046=CARTESIAN_POINT('Ctrl Pts',(0.464018658011788,0.223454730417408,
-3.22805971769425));
#71047=CARTESIAN_POINT('Ctrl Pts',(0.0632139238541575,0.51112541033407,
-3.20421153563602));
#71048=CARTESIAN_POINT('Ctrl Pts',(-0.395595432080138,0.329770280007651,
-3.18036335357778));
#71049=CARTESIAN_POINT('Ctrl Pts',(-0.491395996486379,-0.154190670607673,
-3.15651517151955));
#71050=CARTESIAN_POINT('Ctrl Pts',(-0.136276501886399,-0.496662293941589,
-3.13266698946132));
#71051=CARTESIAN_POINT('Ctrl Pts',(0.343893990119533,-0.383381686384168,
-3.10881880740308));
#71052=CARTESIAN_POINT('Ctrl Pts',(0.508497410464,0.0817010824966437,-3.08497062534485));
#71053=CARTESIAN_POINT('Ctrl Pts',(0.206488555490598,0.47181261467073,-3.06112244328661));
#71054=CARTESIAN_POINT('Ctrl Pts',(-0.285000226830173,0.428974967322919,
-3.03727426122838));
#71055=CARTESIAN_POINT('Ctrl Pts',(-0.514964439704652,-0.00750271008224029,
-3.01342607917014));
#71056=CARTESIAN_POINT('Ctrl Pts',(-0.272382117990696,-0.437095691356589,
-2.98957789711191));
#71057=CARTESIAN_POINT('Ctrl Pts',(0.22014604298458,-0.465596799454457,
-2.96572971505367));
#71058=CARTESIAN_POINT('Ctrl Pts',(0.510661720918123,-0.0668525880191949,
-2.94188153299544));
#71059=CARTESIAN_POINT('Ctrl Pts',(0.332579176526704,0.393237526826984,
-2.9180333509372));
#71060=CARTESIAN_POINT('Ctrl Pts',(-0.150687804924479,0.492481315824468,
-2.89418516887897));
#71061=CARTESIAN_POINT('Ctrl Pts',(-0.495679223315113,0.139809759376405,
-2.87033698682074));
#71062=CARTESIAN_POINT('Ctrl Pts',(-0.385820801560915,-0.34115534618457,
-2.8464888047625));
#71063=CARTESIAN_POINT('Ctrl Pts',(0.0780781397392639,-0.509066268011637,
-2.82264062270427));
#71064=CARTESIAN_POINT('Ctrl Pts',(0.470330282758143,-0.209843003904197,
-2.79879244064603));
#71065=CARTESIAN_POINT('Ctrl Pts',(0.430993519558152,0.281938374916232,
-2.7749442585878));
#71066=CARTESIAN_POINT('Ctrl Pts',(-0.00383557847163829,0.515004805306344,
-2.75109607652956));
#71067=CARTESIAN_POINT('Ctrl Pts',(-0.435145036849806,0.275487673155042,
-2.72724789447133));
#71068=CARTESIAN_POINT('Ctrl Pts',(-0.46715260595567,-0.216825053676554,
-2.70339971241309));
#71069=CARTESIAN_POINT('Ctrl Pts',(-0.0704871986133876,-0.510172731518216,
-2.67955153035486));
#71070=CARTESIAN_POINT('Ctrl Pts',(0.390859336152151,-0.335370899895037,
-2.65570334829662));
#71071=CARTESIAN_POINT('Ctrl Pts',(0.493541843646563,0.147177137230274,
-2.63185516623839));
#71072=CARTESIAN_POINT('Ctrl Pts',(0.143335833723845,0.494671102778485,
-2.60800698418016));
#71073=CARTESIAN_POINT('Ctrl Pts',(-0.338399354654062,0.38824030950325,
-2.58415880212192));
#71074=CARTESIAN_POINT('Ctrl Pts',(-0.509609338336009,-0.0744512151287393,
-2.56031062006369));
#71075=CARTESIAN_POINT('Ctrl Pts',(-0.213186798712875,-0.468824114149408,
-2.53646243800545));
#71076=CARTESIAN_POINT('Ctrl Pts',(0.278862220093275,-0.432990211619247,
-2.51261425594722));
#71077=CARTESIAN_POINT('Ctrl Pts',(0.515019060662466,0.000168249144257329,
-2.48876607388898));
#71078=CARTESIAN_POINT('Ctrl Pts',(0.278579257547253,0.433172319542517,
-2.46491789183075));
#71079=CARTESIAN_POINT('Ctrl Pts',(-0.213493069046952,0.468684724118824,
-2.44106970977251));
#71080=CARTESIAN_POINT('Ctrl Pts',(-0.509657873788101,0.0741182355376679,
-2.41722152771428));
#71081=CARTESIAN_POINT('Ctrl Pts',(-0.338145617665194,-0.388461326784597,
-2.39337334565604));
#71082=CARTESIAN_POINT('Ctrl Pts',(0.143659006626774,-0.494577345789749,
-2.36952516359781));
#71083=CARTESIAN_POINT('Ctrl Pts',(0.49363789949917,-0.146854640142799,
-2.34567698153957));
#71084=CARTESIAN_POINT('Ctrl Pts',(0.39064013127742,0.335626204264484,-2.32182879948134));
#71085=CARTESIAN_POINT('Ctrl Pts',(-0.0708205153719315,0.510126568368949,
-2.2979806174231));
#71086=CARTESIAN_POINT('Ctrl Pts',(-0.467294173334448,0.216519783671375,
-2.27413243536487));
#71087=CARTESIAN_POINT('Ctrl Pts',(-0.434964948454003,-0.27577192527491,
-2.25028425330663));
#71088=CARTESIAN_POINT('Ctrl Pts',(-0.00349908871715384,-0.515007201436616,
-2.2264360712484));
#71089=CARTESIAN_POINT('Ctrl Pts',(0.431177637781705,-0.28165671628849,
-2.20258788919016));
#71090=CARTESIAN_POINT('Ctrl Pts',(0.470193077132676,0.210150259028937,
-2.17873970713193));
#71091=CARTESIAN_POINT('Ctrl Pts',(0.0777455142197789,0.50911717332273,
-2.15489152507369));
#71092=CARTESIAN_POINT('Ctrl Pts',(-0.386043620079866,0.340903189408749,
-2.13104334301546));
#71093=CARTESIAN_POINT('Ctrl Pts',(-0.495587769871853,-0.140133591643364,
-2.10719516095723));
#71094=CARTESIAN_POINT('Ctrl Pts',(-0.150366000143867,-0.492579665794437,
-2.08334697889899));
#71095=CARTESIAN_POINT('Ctrl Pts',(0.332836035597638,-0.393020145235676,
-2.05949879684076));
#71096=CARTESIAN_POINT('Ctrl Pts',(0.51061793190132,0.0671862245869203,
-2.03565061478253));
#71097=CARTESIAN_POINT('Ctrl Pts',(0.219841789768066,0.465740537880266,
-2.01180243272429));
#71098=CARTESIAN_POINT('Ctrl Pts',(-0.272667647152995,0.436917629936666,
-1.98795425066605));
#71099=CARTESIAN_POINT('Ctrl Pts',(-0.514969228232612,0.00716624915361177,
-1.96410606860782));
#71100=CARTESIAN_POINT('Ctrl Pts',(-0.284719893331698,-0.429161092708335,
-1.94025788654958));
#71101=CARTESIAN_POINT('Ctrl Pts',(0.206796793122505,-0.471677588515368,
-1.91640970449135));
#71102=CARTESIAN_POINT('Ctrl Pts',(0.508550657539238,-0.0813688507343729,
-1.89256152243311));
#71103=CARTESIAN_POINT('Ctrl Pts',(0.34364347529996,0.383606338630098,-1.86871334037488));
#71104=CARTESIAN_POINT('Ctrl Pts',(-0.136601071039797,0.49657306465837,
-1.84486515831665));
#71105=CARTESIAN_POINT('Ctrl Pts',(-0.491496455323177,0.15386973567982,
-1.82101697625841));
#71106=CARTESIAN_POINT('Ctrl Pts',(-0.395380230696901,-0.330028990131912,
-1.79716879420018));
#71107=CARTESIAN_POINT('Ctrl Pts',(0.0635485270542077,-0.511083404018038,
-1.77332061214195));
#71108=CARTESIAN_POINT('Ctrl Pts',(0.464163286565573,-0.223152648557151,
-1.74947243008371));
#71109=CARTESIAN_POINT('Ctrl Pts',(0.438848157054481,0.269549543133189,
-1.72562424802547));
#71110=CARTESIAN_POINT('Ctrl Pts',(0.0108330462179193,0.514905142975932,
-1.70177606596724));
#71111=CARTESIAN_POINT('Ctrl Pts',(-0.427122786573439,0.287768633355279,
-1.677927883909));
#71112=CARTESIAN_POINT('Ctrl Pts',(-0.473138182993198,-0.203432841368646,
-1.65407970185077));
#71113=CARTESIAN_POINT('Ctrl Pts',(-0.0849880613563904,-0.507958355163401,
-1.63023151979254));
#71114=CARTESIAN_POINT('Ctrl Pts',(0.381149606020199,-0.346366336389769,
-1.6063833377343));
#71115=CARTESIAN_POINT('Ctrl Pts',(0.497533180188899,0.133061623936225,
-1.58253515567607));
#71116=CARTESIAN_POINT('Ctrl Pts',(0.157365669090087,0.490388323010709,
-1.55868697361783));
#71117=CARTESIAN_POINT('Ctrl Pts',(-0.327205210201477,0.397720267990497,
-1.53483879155959));
#71118=CARTESIAN_POINT('Ctrl Pts',(-0.511522961116853,-0.0599076072270458,
-1.51099060950136));
#71119=CARTESIAN_POINT('Ctrl Pts',(-0.226452192158073,-0.462562499366548,
-1.48714242744313));
#71120=CARTESIAN_POINT('Ctrl Pts',(0.266417771322213,-0.44075643191805,
-1.46329424538489));
#71121=CARTESIAN_POINT('Ctrl Pts',(0.514814948916082,-0.0144992939813027,
-1.43944606332666));
#71122=CARTESIAN_POINT('Ctrl Pts',(0.29080278176969,0.425062822731458,-1.41559788126842));
#71123=CARTESIAN_POINT('Ctrl Pts',(-0.200058574340051,0.474574786505194,
-1.39174969921019));
#71124=CARTESIAN_POINT('Ctrl Pts',(-0.507340296228526,0.0886029625699759,
-1.36790151715195));
#71125=CARTESIAN_POINT('Ctrl Pts',(-0.349071634612663,-0.37867354682136,
-1.34405333509372));
#71126=CARTESIAN_POINT('Ctrl Pts',(0.12951542980401,-0.49846806777978,-1.32020515303549));
#71127=CARTESIAN_POINT('Ctrl Pts',(0.489255325046037,-0.160853623109709,
-1.29635697097725));
#71128=CARTESIAN_POINT('Ctrl Pts',(0.400040138462428,0.324364838989042,
-1.27250878891902));
#71129=CARTESIAN_POINT('Ctrl Pts',(-0.0562636497220763,0.511936580909566,
-1.24866060686078));
#71130=CARTESIAN_POINT('Ctrl Pts',(-0.460938257452779,0.229740253264028,
-1.22481242480255));
#71131=CARTESIAN_POINT('Ctrl Pts',(-0.442642357766302,-0.263272490519829,
-1.20096424274431));
#71132=CARTESIAN_POINT('Ctrl Pts',(-0.0181648065428401,-0.514698650626448,
-1.17711606068608));
#71133=CARTESIAN_POINT('Ctrl Pts',(0.422981305635007,-0.293822184725266,
-1.15326787862784));
#71134=CARTESIAN_POINT('Ctrl Pts',(0.47598732620688,0.196674163132451,-1.12941969656961));
#71135=CARTESIAN_POINT('Ctrl Pts',(0.0922133710777856,0.50669651207394,
-1.10557151451137));
#71136=CARTESIAN_POINT('Ctrl Pts',(-0.376178286584747,0.351759232793667,
-1.08172333245314));
#71137=CARTESIAN_POINT('Ctrl Pts',(-0.499377680026562,-0.125962668456626,
-1.0578751503949));
#71138=CARTESIAN_POINT('Ctrl Pts',(-0.164333420878337,-0.488097518879012,
-1.03402696833667));
#71139=CARTESIAN_POINT('Ctrl Pts',(0.321508020518597,-0.402339724481236,
-1.01017878627844));
#71140=CARTESIAN_POINT('Ctrl Pts',(0.512324242423155,0.052616839309969,
-0.9863306042202));
#71141=CARTESIAN_POINT('Ctrl Pts',(0.233016665150436,0.459290643183149,
-0.962482422161966));
#71142=CARTESIAN_POINT('Ctrl Pts',(-0.260113860210765,0.444505838971396,
-0.938634240103731));
#71143=CARTESIAN_POINT('Ctrl Pts',(-0.514556254004094,0.0218293980388927,
-0.914786058045497));
#71144=CARTESIAN_POINT('Ctrl Pts',(-0.296826689119951,-0.420878340829603,
-0.890937875987262));
#71145=CARTESIAN_POINT('Ctrl Pts',(0.193279779355815,-0.477375730473926,
-0.867089693929028));
#71146=CARTESIAN_POINT('Ctrl Pts',(0.50602703534366,-0.0958191038103274,
-0.843241511870793));
#71147=CARTESIAN_POINT('Ctrl Pts',(0.354428994654787,0.373663951835225,
-0.819393329812559));
#71148=CARTESIAN_POINT('Ctrl Pts',(-0.122403520039554,0.500261970806237,
-0.795545147754323));
#71149=CARTESIAN_POINT('Ctrl Pts',(-0.48691496321932,0.167804885949508,
-0.77169696569609));
#71150=CARTESIAN_POINT('Ctrl Pts',(-0.40461890944033,-0.318634899648728,
-0.747848783637854));
#71151=CARTESIAN_POINT('Ctrl Pts',(0.0489673608989993,-0.512685925999647,
-0.72400060157962));
#71152=CARTESIAN_POINT('Ctrl Pts',(0.457619740115207,-0.236281261685694,
-0.700152419521385));
#71153=CARTESIAN_POINT('Ctrl Pts',(0.44634678101758,0.256942040561066,-0.67630423746315));
#71154=CARTESIAN_POINT('Ctrl Pts',(0.0254928827023883,0.514387766260962,
-0.652456055404916));
#71155=CARTESIAN_POINT('Ctrl Pts',(-0.418754035043963,0.299816142623377,
-0.628607873346681));
#71156=CARTESIAN_POINT('Ctrl Pts',(-0.478739928722221,-0.189875595156935,
-0.604759691288448));
#71157=CARTESIAN_POINT('Ctrl Pts',(-0.0994199782875138,-0.505331899924686,
-0.580911509230211));
#71158=CARTESIAN_POINT('Ctrl Pts',(0.371130670740883,-0.357080784937167,
-0.557063327171978));
#71159=CARTESIAN_POINT('Ctrl Pts',(0.501120893982533,0.11883816524227,-0.533215145113743));
#71160=CARTESIAN_POINT('Ctrl Pts',(0.171267844788483,0.485707717609162,
-0.509366963055509));
#71161=CARTESIAN_POINT('Ctrl Pts',(-0.315745626841075,0.406877578578177,
-0.485518780997274));
#71162=CARTESIAN_POINT('Ctrl Pts',(-0.513021604132975,-0.0453154010881461,
-0.461670598939039));
#71163=CARTESIAN_POINT('Ctrl Pts',(-0.239533894924378,-0.455925630002724,
-0.437822416880805));
#71164=CARTESIAN_POINT('Ctrl Pts',(0.253757226152789,-0.448165096259132,
-0.41397423482257));
#71165=CARTESIAN_POINT('Ctrl Pts',(0.514193131175447,-0.0291550638327419,
-0.390126052764336));
#71166=CARTESIAN_POINT('Ctrl Pts',(0.302790517927606,0.416608475001228,
-0.366277870706101));
#71167=CARTESIAN_POINT('Ctrl Pts',(-0.186462021616671,0.480079892059551,
-0.342429688647866));
#71168=CARTESIAN_POINT('Ctrl Pts',(-0.50461068347562,0.103015734629539,
-0.318581506589632));
#71169=CARTESIAN_POINT('Ctrl Pts',(-0.359715347231949,-0.368578423437957,
-0.294733324531397));
#71170=CARTESIAN_POINT('Ctrl Pts',(0.115268469717766,-0.501954690602548,
-0.270885142473162));
#71171=CARTESIAN_POINT('Ctrl Pts',(0.484472610223246,-0.174721575692987,
-0.247036960414928));
#71172=CARTESIAN_POINT('Ctrl Pts',(0.409121821147799,0.312839300687487,
-0.223188778356693));
#71173=CARTESIAN_POINT('Ctrl Pts',(-0.0416730493251578,0.513333270606055,
-0.199340596298459));
#71174=CARTESIAN_POINT('Ctrl Pts',(-0.454185555720083,0.242770541477401,
-0.175492414240224));
#71175=CARTESIAN_POINT('Ctrl Pts',(-0.450004527996802,-0.250552174658241,
-0.15164423218199));
#71176=CARTESIAN_POINT('Ctrl Pts',(-0.0327316160753884,-0.513986565007051,
-0.127796050123755));
#71177=CARTESIAN_POINT('Ctrl Pts',(0.414280086532281,-0.305722409144298,
-0.10394786806552));
#71178=CARTESIAN_POINT('Ctrl Pts',(0.481707908230206,0.182986979932784,
-0.0800996860072855));
#71179=CARTESIAN_POINT('Ctrl Pts',(0.105987522180041,0.503963242400988,
-0.0562515039490512));
#71180=CARTESIAN_POINT('Ctrl Pts',(-0.286205982023216,0.385783600838152,
-0.0363780189005224));
#71181=CARTESIAN_POINT('Ctrl Pts',(-0.435697412769368,0.125135549288363,
-0.020479230861699));
#71182=CARTESIAN_POINT('Ctrl Pts',(-0.44089380649838,-0.0236648797430034,
-0.0125298368422878));
#71183=CARTESIAN_POINT('Ctrl Pts',(-0.425168349125048,-0.0944518890585346,
-0.00855513983258212));
#71184=CARTESIAN_POINT('Ctrl Pts',(-0.204298847651432,0.416621468233145,
-3.47394486016742));
#71185=CARTESIAN_POINT('Ctrl Pts',(-0.273662872075077,0.382607401895386,
-3.46997016315771));
#71186=CARTESIAN_POINT('Ctrl Pts',(-0.394020182316735,0.279277366226496,
-3.4620207691383));
#71187=CARTESIAN_POINT('Ctrl Pts',(-0.511435893926076,-0.0185377744517229,
-3.44612198109947));
#71188=CARTESIAN_POINT('Ctrl Pts',(-0.348820800331314,-0.423508877579897,
-3.42624849605095));
#71189=CARTESIAN_POINT('Ctrl Pts',(0.168249301911632,-0.522575166238889,
-3.40240031399271));
#71190=CARTESIAN_POINT('Ctrl Pts',(0.530033749224739,-0.141300624249212,
-3.37855213193448));
#71191=CARTESIAN_POINT('Ctrl Pts',(0.405902783757,0.369222784125986,-3.35470394987624));
#71192=CARTESIAN_POINT('Ctrl Pts',(-0.0909349985308223,0.541150548495764,
-3.33085576781801));
#71193=CARTESIAN_POINT('Ctrl Pts',(-0.504203956900882,0.216391213494833,
-3.30700758575977));
#71194=CARTESIAN_POINT('Ctrl Pts',(-0.45486524179264,-0.306877005951273,
-3.28315940370154));
#71195=CARTESIAN_POINT('Ctrl Pts',(0.0119049262807596,-0.548576111432104,
-3.25931122164331));
#71196=CARTESIAN_POINT('Ctrl Pts',(0.467733209195441,-0.286869868566442,
-3.23546303958507));
#71197=CARTESIAN_POINT('Ctrl Pts',(0.494364895825279,0.238068389313909,
-3.21161485752684));
#71198=CARTESIAN_POINT('Ctrl Pts',(0.067348035130247,0.54455237062264,-3.1877666754686));
#71199=CARTESIAN_POINT('Ctrl Pts',(-0.42146687680021,0.351336842403683,
-3.16391849341037));
#71200=CARTESIAN_POINT('Ctrl Pts',(-0.523532677873002,-0.164274546930515,
-3.14007031135213));
#71201=CARTESIAN_POINT('Ctrl Pts',(-0.145188814060127,-0.529143384571705,
-3.1162221292939));
#71202=CARTESIAN_POINT('Ctrl Pts',(0.366384225429279,-0.408454367466004,
-3.09237394723566));
#71203=CARTESIAN_POINT('Ctrl Pts',(0.541752502859644,0.0870442307434959,
-3.06852576517743));
#71204=CARTESIAN_POINT('Ctrl Pts',(0.219992647842253,0.502668567467005,
-3.04467758311919));
#71205=CARTESIAN_POINT('Ctrl Pts',(-0.303638883942248,0.457029391751011,
-3.02082940106096));
#71206=CARTESIAN_POINT('Ctrl Pts',(-0.548642467695438,-0.00799337790447078,
-2.99698121900273));
#71207=CARTESIAN_POINT('Ctrl Pts',(-0.290195566622494,-0.465681200943625,
-2.97313303694449));
#71208=CARTESIAN_POINT('Ctrl Pts',(0.234543317875925,-0.496046245737469,
-2.94928485488626));
#71209=CARTESIAN_POINT('Ctrl Pts',(0.544058356500897,-0.0712246633645508,
-2.92543667282802));
#71210=CARTESIAN_POINT('Ctrl Pts',(0.35432943722945,0.418954767503064,-2.90158849076979));
#71211=CARTESIAN_POINT('Ctrl Pts',(-0.160542598228318,0.524688975733545,
-2.87774030871155));
#71212=CARTESIAN_POINT('Ctrl Pts',(-0.528096022360174,0.148953142155155,
-2.85389212665332));
#71213=CARTESIAN_POINT('Ctrl Pts',(-0.411052997713816,-0.363466477618423,
-2.83004394459508));
#71214=CARTESIAN_POINT('Ctrl Pts',(0.0831843520771779,-0.542358562976886,
-2.80619576253685));
#71215=CARTESIAN_POINT('Ctrl Pts',(0.501089292907908,-0.223566472971712,
-2.78234758047861));
#71216=CARTESIAN_POINT('Ctrl Pts',(0.459179954768808,0.300376790756268,
-2.75849939842038));
#71217=CARTESIAN_POINT('Ctrl Pts',(-0.00408642048939399,0.548685473156816,
-2.73465121636214));
#71218=CARTESIAN_POINT('Ctrl Pts',(-0.463602976080494,0.2935042211966,-2.71080303430391));
#71219=CARTESIAN_POINT('Ctrl Pts',(-0.497703800031065,-0.231005140035548,
-2.68695485224567));
#71220=CARTESIAN_POINT('Ctrl Pts',(-0.0750969729295639,-0.543537387808,
-2.66310667018744));
#71221=CARTESIAN_POINT('Ctrl Pts',(0.416421046143122,-0.357303735801995,
-2.63925848812921));
#71222=CARTESIAN_POINT('Ctrl Pts',(0.525818860744067,0.156802337273383,
-2.61541030607097));
#71223=CARTESIAN_POINT('Ctrl Pts',(0.152709817339109,0.527021972005809,
-2.59156212401274));
#71224=CARTESIAN_POINT('Ctrl Pts',(-0.360530247701046,0.413630738438696,
-2.5677139419545));
#71225=CARTESIAN_POINT('Ctrl Pts',(-0.542937149418829,-0.0793202311495182,
-2.54386575989627));
#71226=CARTESIAN_POINT('Ctrl Pts',(-0.227128947763859,-0.499484622762653,
-2.52001757783803));
#71227=CARTESIAN_POINT('Ctrl Pts',(0.297099459268975,-0.46130722798452,
-2.4961693957798));
#71228=CARTESIAN_POINT('Ctrl Pts',(0.548700660795336,0.000179252427110567,
-2.47232121372157));
#71229=CARTESIAN_POINT('Ctrl Pts',(0.296797991327609,0.461501245537395,
-2.44847303166333));
#71230=CARTESIAN_POINT('Ctrl Pts',(-0.227455247793364,0.499336116799028,
-2.4246248496051));
#71231=CARTESIAN_POINT('Ctrl Pts',(-0.542988859028567,0.078965475111137,
-2.40077666754686));
#71232=CARTESIAN_POINT('Ctrl Pts',(-0.36025991663159,-0.413866209972829,
-2.37692848548863));
#71233=CARTESIAN_POINT('Ctrl Pts',(0.153054125344252,-0.52692208342769,
-2.35308030343039));
#71234=CARTESIAN_POINT('Ctrl Pts',(0.525921198528869,-0.156458749281175,
-2.32923212137215));
#71235=CARTESIAN_POINT('Ctrl Pts',(0.416187505544722,0.357575736756754,
-2.30538393931392));
#71236=CARTESIAN_POINT('Ctrl Pts',(-0.0754520881857466,0.543488205646713,
-2.28153575725568));
#71237=CARTESIAN_POINT('Ctrl Pts',(-0.497854625738724,0.230679905755195,
-2.25768757519746));
#71238=CARTESIAN_POINT('Ctrl Pts',(-0.463411110129646,-0.293807063048322,
-2.23383939313921));
#71239=CARTESIAN_POINT('Ctrl Pts',(-0.0037279247273187,-0.548688025991,
-2.20999121108099));
#71240=CARTESIAN_POINT('Ctrl Pts',(0.459376114093082,-0.300076712007801,
-2.18614302902275));
#71241=CARTESIAN_POINT('Ctrl Pts',(0.500943114206752,0.223893822195952,
-2.16229484696451));
#71242=CARTESIAN_POINT('Ctrl Pts',(0.0828299732662211,0.542412797431429,
-2.13844666490628));
#71243=CARTESIAN_POINT('Ctrl Pts',(-0.411290388284232,0.363197830105963,
-2.11459848284804));
#71244=CARTESIAN_POINT('Ctrl Pts',(-0.527998587976513,-0.149298152645908,
-2.09075030078981));
#71245=CARTESIAN_POINT('Ctrl Pts',(-0.160199747818974,-0.524793757668104,
-2.06690211873158));
#71246=CARTESIAN_POINT('Ctrl Pts',(0.354603094561221,-0.418723169428535,
-2.04305393667334));
#71247=CARTESIAN_POINT('Ctrl Pts',(0.544011703737359,0.0715801193450341,
-2.01920575461511));
#71248=CARTESIAN_POINT('Ctrl Pts',(0.234219166880941,0.496199384475909,
-1.99535757255687));
#71249=CARTESIAN_POINT('Ctrl Pts',(-0.290499769033619,0.465491494530337,
-1.97150939049864));
#71250=CARTESIAN_POINT('Ctrl Pts',(-0.548647569387118,0.00763491285342533,
-1.9476612084404));
#71251=CARTESIAN_POINT('Ctrl Pts',(-0.303340216984838,-0.457227689503013,
-1.92381302638217));
#71252=CARTESIAN_POINT('Ctrl Pts',(0.220321043828396,-0.502524710770565,
-1.89996484432393));
#71253=CARTESIAN_POINT('Ctrl Pts',(0.54180923222677,-0.0866902714409802,
-1.8761166622657));
#71254=CARTESIAN_POINT('Ctrl Pts',(0.366117327254944,0.408693711686842,
-1.85226848020746));
#71255=CARTESIAN_POINT('Ctrl Pts',(-0.145534609628768,0.529048319805361,
-1.82842029814923));
#71256=CARTESIAN_POINT('Ctrl Pts',(-0.523639706591634,0.163932623261208,
-1.804572116091));
#71257=CARTESIAN_POINT('Ctrl Pts',(-0.421237601516625,-0.351612471845344,
-1.78072393403276));
#71258=CARTESIAN_POINT('Ctrl Pts',(0.0677045209595963,-0.544507617146265,
-1.75687575197453));
#71259=CARTESIAN_POINT('Ctrl Pts',(0.494518982904948,-0.237746551679154,
-1.73302756991629));
#71260=CARTESIAN_POINT('Ctrl Pts',(0.467548275698523,0.287177744924656,
-1.70917938785805));
#71261=CARTESIAN_POINT('Ctrl Pts',(0.0115415138432998,0.548579293035088,
-1.68533120579982));
#71262=CARTESIAN_POINT('Ctrl Pts',(-0.455056080705307,0.306588340779288,
-1.66148302374159));
#71263=CARTESIAN_POINT('Ctrl Pts',(-0.504080826293955,-0.216737093852153,
-1.63763484168335));
#71264=CARTESIAN_POINT('Ctrl Pts',(-0.0905461738949672,-0.541178194018989,
-1.61378665962512));
#71265=CARTESIAN_POINT('Ctrl Pts',(0.406076311847863,-0.369018260042385,
-1.58993847756688));
#71266=CARTESIAN_POINT('Ctrl Pts',(0.530071225686482,0.141763687127217,
-1.56609029550865));
#71267=CARTESIAN_POINT('Ctrl Pts',(0.167657186328529,0.522459103816819,
-1.54224211345041));
#71268=CARTESIAN_POINT('Ctrl Pts',(-0.348604020251771,0.423730674312086,
-1.51839393139218));
#71269=CARTESIAN_POINT('Ctrl Pts',(-0.544975920727627,-0.0638254895456974,
-1.49454574933394));
#71270=CARTESIAN_POINT('Ctrl Pts',(-0.241261881290101,-0.49281350623236,
-1.47069756727571));
#71271=CARTESIAN_POINT('Ctrl Pts',(0.283841159168135,-0.469581349342968,
-1.44684938521748));
#71272=CARTESIAN_POINT('Ctrl Pts',(0.548483200396933,-0.0154475296086586,
-1.42300120315924));
#71273=CARTESIAN_POINT('Ctrl Pts',(0.309820918691641,0.452861397813657,
-1.39915302110101));
#71274=CARTESIAN_POINT('Ctrl Pts',(-0.213142153995152,0.50561138187246,
-1.37530483904277));
#71275=CARTESIAN_POINT('Ctrl Pts',(-0.540519714805541,0.0943974851106201,
-1.35145665698454));
#71276=CARTESIAN_POINT('Ctrl Pts',(-0.371900481373456,-0.403438321485286,
-1.3276084749263));
#71277=CARTESIAN_POINT('Ctrl Pts',(0.137985576349817,-0.531067253752366,
-1.30376029286807));
#71278=CARTESIAN_POINT('Ctrl Pts',(0.521252009207359,-0.171373248163074,
-1.27991211080983));
#71279=CARTESIAN_POINT('Ctrl Pts',(0.426202261401058,0.345577892327182,
-1.2560639287516));
#71280=CARTESIAN_POINT('Ctrl Pts',(-0.0599432217936751,0.54541659073562,
-1.23221574669336));
#71281=CARTESIAN_POINT('Ctrl Pts',(-0.491083040936125,0.244764977465323,
-1.20836756463513));
#71282=CARTESIAN_POINT('Ctrl Pts',(-0.471590612374546,-0.280490180949125,
-1.18451938257689));
#71283=CARTESIAN_POINT('Ctrl Pts',(-0.0193527620908934,-0.54835929634513,
-1.16067120051866));
#71284=CARTESIAN_POINT('Ctrl Pts',(0.450643752111749,-0.31303778681066,
-1.13682301846043));
#71285=CARTESIAN_POINT('Ctrl Pts',(0.507116299897664,0.209536406542574,
-1.11297483640219));
#71286=CARTESIAN_POINT('Ctrl Pts',(0.0982440098031782,0.539833827975301,
-1.08912665434396));
#71287=CARTESIAN_POINT('Ctrl Pts',(-0.400779874361163,0.374763845102116,
-1.06527847228572));
#71288=CARTESIAN_POINT('Ctrl Pts',(-0.532036353498374,-0.134200468869619,
-1.04143029022749));
#71289=CARTESIAN_POINT('Ctrl Pts',(-0.175080620338046,-0.52001848397025,
-1.01758210816925));
#71290=CARTESIAN_POINT('Ctrl Pts',(0.342534241514551,-0.428652237459134,
-0.993733926111017));
#71291=CARTESIAN_POINT('Ctrl Pts',(0.545829604825618,0.056057914557968,
-0.969885744052783));
#71292=CARTESIAN_POINT('Ctrl Pts',(0.248255662576661,0.489327674761291,
-0.946037561994548));
#71293=CARTESIAN_POINT('Ctrl Pts',(-0.277124980182455,0.473575962911475,
-0.922189379936314));
#71294=CARTESIAN_POINT('Ctrl Pts',(-0.548207587162405,0.023257013271117,
-0.898341197878079));
#71295=CARTESIAN_POINT('Ctrl Pts',(-0.316238782021605,-0.448403256047641,
-0.874493015819845));
#71296=CARTESIAN_POINT('Ctrl Pts',(0.205920034327462,-0.508595504061096,
-0.850644833761609));
#71297=CARTESIAN_POINT('Ctrl Pts',(0.539120568307165,-0.102085552930635,
-0.826796651703376));
#71298=CARTESIAN_POINT('Ctrl Pts',(0.377608206037959,0.398101105274931,
-0.80294846964514));
#71299=CARTESIAN_POINT('Ctrl Pts',(-0.130408556613393,0.532978475785109,
-0.779100287586906));
#71300=CARTESIAN_POINT('Ctrl Pts',(-0.518758590654718,0.178779114867606,
-0.755252105528672));
#71301=CARTESIAN_POINT('Ctrl Pts',(-0.431080478253797,-0.339473222146037,
-0.731403923470437));
#71302=CARTESIAN_POINT('Ctrl Pts',(0.0521697648396222,-0.54621494205404,
-0.707555741412202));
#71303=CARTESIAN_POINT('Ctrl Pts',(0.487547496729966,-0.251733759627714,
-0.683707559353968));
#71304=CARTESIAN_POINT('Ctrl Pts',(0.47553730025679,0.273745727508825,-0.659859377295733));
#71305=CARTESIAN_POINT('Ctrl Pts',(0.027160085233324,0.548028080532353,
-0.636011195237498));
#71306=CARTESIAN_POINT('Ctrl Pts',(-0.446140023329977,0.319423742031895,
-0.612163013179265));
#71307=CARTESIAN_POINT('Ctrl Pts',(-0.510048919162534,-0.202293220754791,
-0.588314831121028));
#71308=CARTESIAN_POINT('Ctrl Pts',(-0.105921920078934,-0.5383799719043,
-0.564466649062795));
#71309=CARTESIAN_POINT('Ctrl Pts',(0.395402150776707,-0.38043342007637,
-0.540618467004559));
#71310=CARTESIAN_POINT('Ctrl Pts',(0.533893571459043,0.126610032087479,
-0.516770284946326));
#71311=CARTESIAN_POINT('Ctrl Pts',(0.182468546868062,0.51747239269695,-0.492922102888091));
#71312=CARTESIAN_POINT('Ctrl Pts',(-0.336394994523279,0.433486861518255,
-0.469073920829856));
#71313=CARTESIAN_POINT('Ctrl Pts',(-0.546572573115956,-0.048278971440956,
-0.445225738771622));
#71314=CARTESIAN_POINT('Ctrl Pts',(-0.255199110997613,-0.485742593942516,
-0.421377556713387));
#71315=CARTESIAN_POINT('Ctrl Pts',(0.270352630235717,-0.477474531032853,
-0.397529374655153));
#71316=CARTESIAN_POINT('Ctrl Pts',(0.547820716556546,-0.0310617684129566,
-0.373681192596918));
#71317=CARTESIAN_POINT('Ctrl Pts',(0.322592637747684,0.443854146353481,
-0.349833010538683));
#71318=CARTESIAN_POINT('Ctrl Pts',(-0.198656403789595,0.51147651442025,
-0.325984828480449));
#71319=CARTESIAN_POINT('Ctrl Pts',(-0.537611588804712,0.109752834372456,
-0.302136646422214));
#71320=CARTESIAN_POINT('Ctrl Pts',(-0.383240279438416,-0.392682989703664,
-0.278288464363979));
#71321=CARTESIAN_POINT('Ctrl Pts',(0.122806882956234,-0.534781897331454,
-0.254440282305745));
#71322=CARTESIAN_POINT('Ctrl Pts',(0.516156510838259,-0.186148147438714,
-0.23059210024751));
#71323=CARTESIAN_POINT('Ctrl Pts',(0.435877874735032,0.333298598287169,
-0.206743918189276));
#71324=CARTESIAN_POINT('Ctrl Pts',(-0.0443984144444239,0.546904622185182,
-0.182895736131041));
#71325=CARTESIAN_POINT('Ctrl Pts',(-0.483888720985873,0.258647430172675,
-0.159047554072806));
#71326=CARTESIAN_POINT('Ctrl Pts',(-0.479434259297373,-0.266937972396299,
-0.135199372014572));
#71327=CARTESIAN_POINT('Ctrl Pts',(-0.0348722226831059,-0.54760064122001,
-0.111351189956337));
#71328=CARTESIAN_POINT('Ctrl Pts',(0.441373484201181,-0.325716270969938,
-0.0875030078981022));
#71329=CARTESIAN_POINT('Ctrl Pts',(0.513211000805034,0.194954098741337,
-0.0636548258398677));
#71330=CARTESIAN_POINT('Ctrl Pts',(0.112918973098675,0.536921805896445,
-0.0398066437816333));
#71331=CARTESIAN_POINT('Ctrl Pts',(-0.304923494011494,0.411013364110478,
-0.0199331587331047));
#71332=CARTESIAN_POINT('Ctrl Pts',(-0.464191476691871,0.133319257145926,
-0.00403437069428121));
#71333=CARTESIAN_POINT('Ctrl Pts',(-0.469727708048424,-0.0252125331748408,
0.00391502332512999));
#71334=CARTESIAN_POINT('Ctrl Pts',(-0.452973825500936,-0.100628924050155,
0.00788972033483567));
#71335=CARTESIAN_POINT('Ctrl Pts',(-0.216839587231055,0.442195480991683,
-3.4575));
#71336=CARTESIAN_POINT('Ctrl Pts',(-0.290461473000917,0.406093485363625,
-3.45352530299029));
#71337=CARTESIAN_POINT('Ctrl Pts',(-0.418206831200729,0.296420608885922,
-3.44557590897088));
#71338=CARTESIAN_POINT('Ctrl Pts',(-0.542830022826607,-0.0196757025627097,
-3.42967712093206));
#71339=CARTESIAN_POINT('Ctrl Pts',(-0.370232917272739,-0.449505669066697,
-3.40980363588353));
#71340=CARTESIAN_POINT('Ctrl Pts',(0.178577165744359,-0.554653071454301,
-3.3859554538253));
#71341=CARTESIAN_POINT('Ctrl Pts',(0.56256949425635,-0.149974262654511,
-3.36210727176706));
#71342=CARTESIAN_POINT('Ctrl Pts',(0.430818837686123,0.391887262344127,
-3.33825908970883));
#71343=CARTESIAN_POINT('Ctrl Pts',(-0.0965169787933541,0.574368690350557,
-3.31441090765059));
#71344=CARTESIAN_POINT('Ctrl Pts',(-0.535154158486442,0.229674234358403,
-3.29056272559236));
#71345=CARTESIAN_POINT('Ctrl Pts',(-0.482786821413474,-0.325714432881724,
-3.26671454353412));
#71346=CARTESIAN_POINT('Ctrl Pts',(0.012635701720356,-0.582250066190823,
-3.24286636147589));
#71347=CARTESIAN_POINT('Ctrl Pts',(0.496444679850769,-0.30447917158645,
-3.21901817941765));
#71348=CARTESIAN_POINT('Ctrl Pts',(0.524711133638771,0.252682048210408,
-3.19516999735942));
#71349=CARTESIAN_POINT('Ctrl Pts',(0.0714821464063366,0.577979330911211,
-3.17132181530119));
#71350=CARTESIAN_POINT('Ctrl Pts',(-0.447338321520283,0.372903404799714,
-3.14747363324295));
#71351=CARTESIAN_POINT('Ctrl Pts',(-0.555669359259625,-0.174358423253356,
-3.12362545118472));
#71352=CARTESIAN_POINT('Ctrl Pts',(-0.154101126233856,-0.56162447520182,
-3.09977726912648));
#71353=CARTESIAN_POINT('Ctrl Pts',(0.388874460739024,-0.43352704854784,
-3.07592908706825));
#71354=CARTESIAN_POINT('Ctrl Pts',(0.575007595255289,0.0923873789903477,
-3.05208090501001));
#71355=CARTESIAN_POINT('Ctrl Pts',(0.233496740193908,0.533524520263281,
-3.02823272295177));
#71356=CARTESIAN_POINT('Ctrl Pts',(-0.322277541054323,0.485083816179102,
-3.00438454089354));
#71357=CARTESIAN_POINT('Ctrl Pts',(-0.582320495686226,-0.00848404572670107,
-2.9805363588353));
#71358=CARTESIAN_POINT('Ctrl Pts',(-0.308009015254291,-0.49426671053066,
-2.95668817677707));
#71359=CARTESIAN_POINT('Ctrl Pts',(0.24894059276727,-0.526495692020481,
-2.93283999471884));
#71360=CARTESIAN_POINT('Ctrl Pts',(0.577454992083672,-0.0755967387099062,
-2.9089918126606));
#71361=CARTESIAN_POINT('Ctrl Pts',(0.376079697932196,0.444672008179143,
-2.88514363060237));
#71362=CARTESIAN_POINT('Ctrl Pts',(-0.170397391532157,0.556896635642623,
-2.86129544854414));
#71363=CARTESIAN_POINT('Ctrl Pts',(-0.560512821405234,0.158096524933905,
-2.8374472664859));
#71364=CARTESIAN_POINT('Ctrl Pts',(-0.436285193866717,-0.385777609052274,
-2.81359908442767));
#71365=CARTESIAN_POINT('Ctrl Pts',(0.0882905644150925,-0.575650857942135,
-2.78975090236943));
#71366=CARTESIAN_POINT('Ctrl Pts',(0.531848303057673,-0.237289942039227,
-2.76590272031119));
#71367=CARTESIAN_POINT('Ctrl Pts',(0.487366389979465,0.318815206596304,
-2.74205453825296));
#71368=CARTESIAN_POINT('Ctrl Pts',(-0.00433726250715015,0.582366141007289,
-2.71820635619472));
#71369=CARTESIAN_POINT('Ctrl Pts',(-0.492060915311181,0.311520769238158,
-2.69435817413649));
#71370=CARTESIAN_POINT('Ctrl Pts',(-0.528254994106461,-0.245185226394541,
-2.67050999207826));
#71371=CARTESIAN_POINT('Ctrl Pts',(-0.0797067472457391,-0.576902044097784,
-2.64666181002002));
#71372=CARTESIAN_POINT('Ctrl Pts',(0.44198275613409,-0.379236571708953,
-2.62281362796179));
#71373=CARTESIAN_POINT('Ctrl Pts',(0.558095877841571,0.166427537316492,
-2.59896544590355));
#71374=CARTESIAN_POINT('Ctrl Pts',(0.162083800954373,0.559372841233132,
-2.57511726384532));
#71375=CARTESIAN_POINT('Ctrl Pts',(-0.382661140748029,0.439021167374142,
-2.55126908178708));
#71376=CARTESIAN_POINT('Ctrl Pts',(-0.576264960501648,-0.0841892471702974,
-2.52742089972885));
#71377=CARTESIAN_POINT('Ctrl Pts',(-0.241071096814844,-0.530145131375898,
-2.50357271767062));
#71378=CARTESIAN_POINT('Ctrl Pts',(0.315336698444676,-0.489624244349793,
-2.47972453561237));
#71379=CARTESIAN_POINT('Ctrl Pts',(0.582382260928205,0.000190255709963338,
-2.45587635355415));
#71380=CARTESIAN_POINT('Ctrl Pts',(0.315016725107966,0.489830171532273,
-2.43202817149591));
#71381=CARTESIAN_POINT('Ctrl Pts',(-0.241417426539775,0.529987509479231,
-2.40817998943768));
#71382=CARTESIAN_POINT('Ctrl Pts',(-0.576319844269034,0.0838127146846064,
-2.38433180737944));
#71383=CARTESIAN_POINT('Ctrl Pts',(-0.382374215597984,-0.439271093161061,
-2.36048362532121));
#71384=CARTESIAN_POINT('Ctrl Pts',(0.16244924406173,-0.559266821065631,
-2.33663544326297));
#71385=CARTESIAN_POINT('Ctrl Pts',(0.558204497558567,-0.166062858419552,
-2.31278726120474));
#71386=CARTESIAN_POINT('Ctrl Pts',(0.441734879812023,0.379525269249024,
-2.2889390791465));
#71387=CARTESIAN_POINT('Ctrl Pts',(-0.0800836609995613,0.576849842924477,
-2.26509089708827));
#71388=CARTESIAN_POINT('Ctrl Pts',(-0.528415078143001,0.244840027839016,
-2.24124271503004));
#71389=CARTESIAN_POINT('Ctrl Pts',(-0.491857271805289,-0.311842200821734,
-2.2173945329718));
#71390=CARTESIAN_POINT('Ctrl Pts',(-0.00395676073748407,-0.582368850545385,
-2.19354635091357));
#71391=CARTESIAN_POINT('Ctrl Pts',(0.48757459040446,-0.318496707727113,
-2.16969816885533));
#71392=CARTESIAN_POINT('Ctrl Pts',(0.531693151280828,0.237637385362967,
-2.1458499867971));
#71393=CARTESIAN_POINT('Ctrl Pts',(0.0879144323126632,0.575708421540129,
-2.12200180473886));
#71394=CARTESIAN_POINT('Ctrl Pts',(-0.436537156488597,0.385492470803176,
-2.09815362268063));
#71395=CARTESIAN_POINT('Ctrl Pts',(-0.560409406081175,-0.158462713648453,
-2.07430544062239));
#71396=CARTESIAN_POINT('Ctrl Pts',(-0.17003349549408,-0.557007849541772,
-2.05045725856416));
#71397=CARTESIAN_POINT('Ctrl Pts',(0.376370153524803,-0.444426193621394,
-2.02660907650592));
#71398=CARTESIAN_POINT('Ctrl Pts',(0.577405475573398,0.0759740141031477,
-2.00276089444769));
#71399=CARTESIAN_POINT('Ctrl Pts',(0.248596543993815,0.526658231071553,
-1.97891271238945));
#71400=CARTESIAN_POINT('Ctrl Pts',(-0.308331890914242,0.494065359124006,
-1.95506453033122));
#71401=CARTESIAN_POINT('Ctrl Pts',(-0.582325910541624,0.00810357655323996,
-1.93121634827298));
#71402=CARTESIAN_POINT('Ctrl Pts',(-0.321960540637979,-0.485294286297692,
-1.90736816621475));
#71403=CARTESIAN_POINT('Ctrl Pts',(0.233845294534286,-0.53337183302576,
-1.88351998415651));
#71404=CARTESIAN_POINT('Ctrl Pts',(0.5750678069143,-0.0920116921475879,
-1.85967180209828));
#71405=CARTESIAN_POINT('Ctrl Pts',(0.388591179209928,0.433781084743586,
-1.83582362004004));
#71406=CARTESIAN_POINT('Ctrl Pts',(-0.154468148217739,0.561523574952351,
-1.81197543798181));
#71407=CARTESIAN_POINT('Ctrl Pts',(-0.55578295786009,0.173995510842596,
-1.78812725592357));
#71408=CARTESIAN_POINT('Ctrl Pts',(-0.447094972336349,-0.373195953558777,
-1.76427907386534));
#71409=CARTESIAN_POINT('Ctrl Pts',(0.0718605148649851,-0.577931830274492,
-1.74043089180711));
#71410=CARTESIAN_POINT('Ctrl Pts',(0.524874679244323,-0.252340454801157,
-1.71658270974887));
#71411=CARTESIAN_POINT('Ctrl Pts',(0.496248394342566,0.304805946716122,
-1.69273452769064));
#71412=CARTESIAN_POINT('Ctrl Pts',(0.0122499814686803,0.582253443094244,
-1.6688863456324));
#71413=CARTESIAN_POINT('Ctrl Pts',(-0.482989374837176,0.325408048203296,
-1.64503816357417));
#71414=CARTESIAN_POINT('Ctrl Pts',(-0.535023469594712,-0.230041346335659,
-1.62118998151593));
#71415=CARTESIAN_POINT('Ctrl Pts',(-0.0961042864335442,-0.574398032874579,
-1.5973417994577));
#71416=CARTESIAN_POINT('Ctrl Pts',(0.431003017675527,-0.391670183695,-1.57349361739947));
#71417=CARTESIAN_POINT('Ctrl Pts',(0.562609271184064,0.150465750318208,
-1.54964543534123));
#71418=CARTESIAN_POINT('Ctrl Pts',(0.177948703566972,0.55452988462293,-1.525797253283));
#71419=CARTESIAN_POINT('Ctrl Pts',(-0.370002830302066,0.449741080633676,
-1.50194907122476));
#71420=CARTESIAN_POINT('Ctrl Pts',(-0.578428880338399,-0.0677433718643487,
-1.47810088916653));
#71421=CARTESIAN_POINT('Ctrl Pts',(-0.256071570422129,-0.523064513098173,
-1.45425270710829));
#71422=CARTESIAN_POINT('Ctrl Pts',(0.301264547014057,-0.498406266767886,
-1.43040452505006));
#71423=CARTESIAN_POINT('Ctrl Pts',(0.582151451877784,-0.0163957652360146,
-1.40655634299182));
#71424=CARTESIAN_POINT('Ctrl Pts',(0.328839055613591,0.480659972895857,
-1.38270816093359));
#71425=CARTESIAN_POINT('Ctrl Pts',(-0.226225733650254,0.536647977239726,
-1.35885997887535));
#71426=CARTESIAN_POINT('Ctrl Pts',(-0.573699133382556,0.100192007651264,
-1.33501179681712));
#71427=CARTESIAN_POINT('Ctrl Pts',(-0.39472932813425,-0.42820309614921,
-1.31116361475888));
#71428=CARTESIAN_POINT('Ctrl Pts',(0.146455722895625,-0.563666439724954,
-1.28731543270065));
#71429=CARTESIAN_POINT('Ctrl Pts',(0.553248693368682,-0.181892873216438,
-1.26346725064242));
#71430=CARTESIAN_POINT('Ctrl Pts',(0.452364384339689,0.366790945665321,
-1.23961906858418));
#71431=CARTESIAN_POINT('Ctrl Pts',(-0.0636227938652733,0.578896600561675,
-1.21577088652595));
#71432=CARTESIAN_POINT('Ctrl Pts',(-0.52122782441947,0.259789701666618,
-1.19192270446771));
#71433=CARTESIAN_POINT('Ctrl Pts',(-0.500538866982789,-0.297707871378421,
-1.16807452240948));
#71434=CARTESIAN_POINT('Ctrl Pts',(-0.0205407176389471,-0.582019942063812,
-1.14422634035124));
#71435=CARTESIAN_POINT('Ctrl Pts',(0.478306198588491,-0.332253388896053,
-1.12037815829301));
#71436=CARTESIAN_POINT('Ctrl Pts',(0.538245273588447,0.222398649952697,
-1.09652997623477));
#71437=CARTESIAN_POINT('Ctrl Pts',(0.104274648528571,0.572971143876661,
-1.07268179417654));
#71438=CARTESIAN_POINT('Ctrl Pts',(-0.42538146213758,0.397768457410565,
-1.0488336121183));
#71439=CARTESIAN_POINT('Ctrl Pts',(-0.564695026970186,-0.142438269282613,
-1.02498543006007));
#71440=CARTESIAN_POINT('Ctrl Pts',(-0.185827819797754,-0.551939449061487,
-1.00113724800184));
#71441=CARTESIAN_POINT('Ctrl Pts',(0.363560462510505,-0.454964750437033,
-0.977289065943598));
#71442=CARTESIAN_POINT('Ctrl Pts',(0.579334967228081,0.0594989898059677,
-0.953440883885366));
#71443=CARTESIAN_POINT('Ctrl Pts',(0.263494660002887,0.519364706339432,
-0.92959270182713));
#71444=CARTESIAN_POINT('Ctrl Pts',(-0.294136100154144,0.502646086851553,
-0.905744519768896));
#71445=CARTESIAN_POINT('Ctrl Pts',(-0.581858920320716,0.0246846285033414,
-0.881896337710661));
#71446=CARTESIAN_POINT('Ctrl Pts',(-0.335650874923259,-0.47592817126568,
-0.858048155652427));
#71447=CARTESIAN_POINT('Ctrl Pts',(0.218560289299109,-0.539815277648267,
-0.834199973594192));
#71448=CARTESIAN_POINT('Ctrl Pts',(0.572214101270669,-0.108352002050942,
-0.810351791535958));
#71449=CARTESIAN_POINT('Ctrl Pts',(0.400787417421131,0.422538258714637,
-0.786503609477722));
#71450=CARTESIAN_POINT('Ctrl Pts',(-0.138413593187233,0.56569498076398,
-0.762655427419489));
#71451=CARTESIAN_POINT('Ctrl Pts',(-0.550602218090115,0.189753343785704,
-0.738807245361253));
#71452=CARTESIAN_POINT('Ctrl Pts',(-0.457542047067265,-0.360311544643345,
-0.714959063303019));
#71453=CARTESIAN_POINT('Ctrl Pts',(0.055372168780246,-0.579743958108433,
-0.691110881244784));
#71454=CARTESIAN_POINT('Ctrl Pts',(0.517475253344724,-0.267186257569734,
-0.66726269918655));
#71455=CARTESIAN_POINT('Ctrl Pts',(0.504727819496001,0.290549414456584,
-0.643414517128314));
#71456=CARTESIAN_POINT('Ctrl Pts',(0.0288272877642591,0.581668394803744,
-0.619566335070081));
#71457=CARTESIAN_POINT('Ctrl Pts',(-0.473526011615991,0.339031341440412,
-0.595718153011845));
#71458=CARTESIAN_POINT('Ctrl Pts',(-0.541357909602848,-0.214710846352648,
-0.571869970953612));
#71459=CARTESIAN_POINT('Ctrl Pts',(-0.112423861870353,-0.571428043883915,
-0.548021788895377));
#71460=CARTESIAN_POINT('Ctrl Pts',(0.419673630812531,-0.403786055215572,
-0.524173606837142));
#71461=CARTESIAN_POINT('Ctrl Pts',(0.566666248935553,0.134381898932689,
-0.500325424778908));
#71462=CARTESIAN_POINT('Ctrl Pts',(0.19366924894764,0.549237067784737,-0.476477242720673));
#71463=CARTESIAN_POINT('Ctrl Pts',(-0.357044362205485,0.460096144458333,
-0.452629060662439));
#71464=CARTESIAN_POINT('Ctrl Pts',(-0.580123542098937,-0.0512425417937655,
-0.428780878604203));
#71465=CARTESIAN_POINT('Ctrl Pts',(-0.270864327070848,-0.515559557882308,
-0.404932696545969));
#71466=CARTESIAN_POINT('Ctrl Pts',(0.286948034318646,-0.506783965806573,
-0.381084514487735));
#71467=CARTESIAN_POINT('Ctrl Pts',(0.581448301937643,-0.0329684729931716,
-0.3572363324295));
#71468=CARTESIAN_POINT('Ctrl Pts',(0.342394757567763,0.471099817705734,
-0.333388150371265));
#71469=CARTESIAN_POINT('Ctrl Pts',(-0.21085078596252,0.542873136780949,
-0.309539968313031));
#71470=CARTESIAN_POINT('Ctrl Pts',(-0.570612494133804,0.116489934115373,
-0.285691786254796));
#71471=CARTESIAN_POINT('Ctrl Pts',(-0.406765211644884,-0.416787555969371,
-0.261843604196561));
#71472=CARTESIAN_POINT('Ctrl Pts',(0.130345296194702,-0.56760910406036,
-0.237995422138327));
#71473=CARTESIAN_POINT('Ctrl Pts',(0.547840411453272,-0.197574719184441,
-0.214147240080093));
#71474=CARTESIAN_POINT('Ctrl Pts',(0.462633928322266,0.353757895886852,
-0.190299058021858));
#71475=CARTESIAN_POINT('Ctrl Pts',(-0.0471237795636909,0.580475973764309,
-0.166450875963623));
#71476=CARTESIAN_POINT('Ctrl Pts',(-0.513591886251662,0.274524318867949,
-0.142602693905388));
#71477=CARTESIAN_POINT('Ctrl Pts',(-0.508863990597946,-0.283323770134356,
-0.118754511847154));
#71478=CARTESIAN_POINT('Ctrl Pts',(-0.0370128292908223,-0.581214717432969,
-0.0949063297889191));
#71479=CARTESIAN_POINT('Ctrl Pts',(0.468466881870079,-0.345710132795577,
-0.0710581477306844));
#71480=CARTESIAN_POINT('Ctrl Pts',(0.544714093379863,0.20692121754989,-0.0472099656724499));
#71481=CARTESIAN_POINT('Ctrl Pts',(0.119850424017307,0.569880369391903,
-0.0233617836142156));
#71482=CARTESIAN_POINT('Ctrl Pts',(-0.32364100599977,0.436243127382803,
-0.00348829856568689));
#71483=CARTESIAN_POINT('Ctrl Pts',(-0.492685540614374,0.141502965003489,
0.0124104894731366));
#71484=CARTESIAN_POINT('Ctrl Pts',(-0.498561609598467,-0.0267601866066781,
0.0203598834925478));
#71485=CARTESIAN_POINT('Ctrl Pts',(-0.480779301876824,-0.106805959041775,
0.0243345805022535));
#71486=CARTESIAN_POINT('Ctrl Pts',(-0.491698555522654,2.49815306513942E-5,
-0.130884152590357));
#71487=CARTESIAN_POINT('Ctrl Pts',(-0.49166889938861,-0.0837076434631148,
-0.12684093900929));
#71488=CARTESIAN_POINT('Ctrl Pts',(-0.471409647654858,-0.167456711012418,
-0.122797725428222));
#71489=CARTESIAN_POINT('Ctrl Pts',(-0.431010112989045,-0.239997579850407,
-0.118754511847154));
#71490=CARTESIAN_POINT('Ctrl Pts',(-0.351580270162238,-0.382620752567228,
-0.110805117827742));
#71491=CARTESIAN_POINT('Ctrl Pts',(-0.194296549726532,-0.481917735000098,
-0.102855723808331));
#71492=CARTESIAN_POINT('Ctrl Pts',(-0.0314080709818594,-0.492315462110302,
-0.0949063297889192));
#71493=CARTESIAN_POINT('Ctrl Pts',(0.131480407762813,-0.502713189220506,
-0.0869569357695075));
#71494=CARTESIAN_POINT('Ctrl Pts',(0.299973644816456,-0.424211661008035,
-0.0790075417500954));
#71495=CARTESIAN_POINT('Ctrl Pts',(0.396928131928234,-0.292855671844219,
-0.0710581477306837));
#71496=CARTESIAN_POINT('Ctrl Pts',(0.49388261904001,-0.161499682680408,
-0.0631087537112723));
#71497=CARTESIAN_POINT('Ctrl Pts',(0.519298356209934,0.0227107674347409,
-0.0551593596918611));
#71498=CARTESIAN_POINT('Ctrl Pts',(0.461195613234472,0.175309184465985,
-0.0472099656724497));
#71499=CARTESIAN_POINT('Ctrl Pts',(0.407084154180315,0.317425073872489,
-0.0398066437816331));
#71500=CARTESIAN_POINT('Ctrl Pts',(0.280534470088716,0.432122845008194,
-0.0324033218908166));
#71501=CARTESIAN_POINT('Ctrl Pts',(0.134559949224566,0.474484556402355,
-0.0249999999999999));
#71502=CARTESIAN_POINT('',(-0.236230756092323,-0.331488661006752,-3.4575));
#71503=CARTESIAN_POINT('Ctrl Pts',(-0.236825839292543,-0.331770464644072,
-3.4575));
#71504=CARTESIAN_POINT('Ctrl Pts',(-0.24498592505692,-0.327184164044185,
-3.4575));
#71505=CARTESIAN_POINT('Ctrl Pts',(-0.252961058460668,-0.322307537184471,
-3.4575));
#71506=CARTESIAN_POINT('Ctrl Pts',(-0.2607333681375,-0.317144081077849,
-3.4575));
#71507=CARTESIAN_POINT('Ctrl Pts',(-0.275646574082145,-0.307236642040296,
-3.4575));
#71508=CARTESIAN_POINT('Ctrl Pts',(-0.289813760355341,-0.296274605501924,
-3.4575));
#71509=CARTESIAN_POINT('Ctrl Pts',(-0.303204978700601,-0.284381130110945,
-3.4575));
#71510=CARTESIAN_POINT('Ctrl Pts',(-0.30899969474596,-0.279234525007043,
-3.4575));
#71511=CARTESIAN_POINT('Ctrl Pts',(-0.314648992460393,-0.273913228093762,
-3.4575));
#71512=CARTESIAN_POINT('Ctrl Pts',(-0.320149827110806,-0.268426052542454,
-3.4575));
#71513=CARTESIAN_POINT('Ctrl Pts',(-0.325348715088508,-0.26324007390136,
-3.4575));
#71514=CARTESIAN_POINT('Ctrl Pts',(-0.330409414487503,-0.257911292679725,
-3.4575));
#71515=CARTESIAN_POINT('Ctrl Pts',(-0.335324960153577,-0.252453580040169,
-3.4575));
#71516=CARTESIAN_POINT('Ctrl Pts',(-0.345907619881657,-0.240703691079382,
-3.4575));
#71517=CARTESIAN_POINT('Ctrl Pts',(-0.355825502531319,-0.228349378127429,
-3.4575));
#71518=CARTESIAN_POINT('Ctrl Pts',(-0.365056952902446,-0.215469067942917,
-3.4575));
#71519=CARTESIAN_POINT('Ctrl Pts',(-0.371061713935393,-0.207090841166103,
-3.4575));
#71520=CARTESIAN_POINT('Ctrl Pts',(-0.376775924245827,-0.198489825135662,
-3.4575));
#71521=CARTESIAN_POINT('Ctrl Pts',(-0.382192007793225,-0.189685455619147,
-3.4575));
#71522=CARTESIAN_POINT('Ctrl Pts',(-0.386628891731828,-0.182472870112388,
-3.4575));
#71523=CARTESIAN_POINT('Ctrl Pts',(-0.39086776775683,-0.175119290841785,
-3.4575));
#71524=CARTESIAN_POINT('Ctrl Pts',(-0.394890010680429,-0.16766200827966,
-3.4575));
#71525=CARTESIAN_POINT('Ctrl Pts',(-0.40620807148356,-0.146678199228982,
-3.4575));
#71526=CARTESIAN_POINT('Ctrl Pts',(-0.415836408714529,-0.124843045338353,
-3.4575));
#71527=CARTESIAN_POINT('Ctrl Pts',(-0.423701483345752,-0.10240131787515,
-3.4575));
#71528=CARTESIAN_POINT('Ctrl Pts',(-0.428572017874585,-0.088504029721993,
-3.4575));
#71529=CARTESIAN_POINT('Ctrl Pts',(-0.432765748438528,-0.0743732157083639,
-3.4575));
#71530=CARTESIAN_POINT('Ctrl Pts',(-0.436257497594041,-0.0600606864200386,
-3.4575));
#71531=CARTESIAN_POINT('Ctrl Pts',(-0.439096686594963,-0.0484229730789673,
-3.4575));
#71532=CARTESIAN_POINT('Ctrl Pts',(-0.441471662517333,-0.0366650055184638,
-3.4575));
#71533=CARTESIAN_POINT('Ctrl Pts',(-0.443365374066457,-0.0248132790866735,
-3.4575));
#71534=CARTESIAN_POINT('Ctrl Pts',(-0.444259517728958,-0.0192173127508425,
-3.4575));
#71535=CARTESIAN_POINT('Ctrl Pts',(-0.44504604416487,-0.0136010248224324,
-3.4575));
#71536=CARTESIAN_POINT('Ctrl Pts',(-0.445721847253133,-0.00798087641735873,
-3.4575));
#71537=CARTESIAN_POINT('Ctrl Pts',(-0.448130298890454,0.0120484129766512,
-3.4575));
#71538=CARTESIAN_POINT('Ctrl Pts',(-0.449141601140773,0.0321699224781787,
-3.4575));
#71539=CARTESIAN_POINT('Ctrl Pts',(-0.448704141806069,0.0522508947148586,
-3.4575));
#71540=CARTESIAN_POINT('Ctrl Pts',(-0.448285329643317,0.0714758940357306,
-3.4575));
#71541=CARTESIAN_POINT('Ctrl Pts',(-0.446538897531985,0.0906642480359715,
-3.4575));
#71542=CARTESIAN_POINT('Ctrl Pts',(-0.443540878719968,0.109704804163937,
-3.4575));
#71543=CARTESIAN_POINT('Ctrl Pts',(-0.441467971943461,0.122869930969648,
-3.4575));
#71544=CARTESIAN_POINT('Ctrl Pts',(-0.438796223272655,0.135964533139785,
-3.4575));
#71545=CARTESIAN_POINT('Ctrl Pts',(-0.435544631086097,0.14895191104839,
-3.4575));
#71546=CARTESIAN_POINT('Ctrl Pts',(-0.434142676634257,0.154551540778085,
-3.4575));
#71547=CARTESIAN_POINT('Ctrl Pts',(-0.432632778326946,0.160130868848963,
-3.4575));
#71548=CARTESIAN_POINT('Ctrl Pts',(-0.43102066709347,0.165673526206262,
-3.4575));
#71549=CARTESIAN_POINT('Ctrl Pts',(-0.424096345244513,0.189480285096999,
-3.4575));
#71550=CARTESIAN_POINT('Ctrl Pts',(-0.415275503745151,0.212673748338969,
-3.4575));
#71551=CARTESIAN_POINT('Ctrl Pts',(-0.404720542116381,0.235028731869538,
-3.4575));
#71552=CARTESIAN_POINT('Ctrl Pts',(-0.398703059276772,0.247773518113789,
-3.4575));
#71553=CARTESIAN_POINT('Ctrl Pts',(-0.392120926506971,0.260245908659614,
-3.4575));
#71554=CARTESIAN_POINT('Ctrl Pts',(-0.384996760852124,0.272403462043344,
-3.4575));
#71555=CARTESIAN_POINT('Ctrl Pts',(-0.378169594196076,0.284054179769713,
-3.4575));
#71556=CARTESIAN_POINT('Ctrl Pts',(-0.370844587868519,0.295415819953137,
-3.4575));
#71557=CARTESIAN_POINT('Ctrl Pts',(-0.36304260791885,0.306464321135028,
-3.4575));
#71558=CARTESIAN_POINT('Ctrl Pts',(-0.358157538916131,0.313382140842121,
-3.4575));
#71559=CARTESIAN_POINT('Ctrl Pts',(-0.353081459306764,0.320181708144073,
-3.4575));
#71560=CARTESIAN_POINT('Ctrl Pts',(-0.347840276198119,0.326830643032922,
-3.4575));
#71561=CARTESIAN_POINT('Ctrl Pts',(-0.332031181725627,0.346885969782693,
-3.4575));
#71562=CARTESIAN_POINT('Ctrl Pts',(-0.314699132938717,0.36561178190024,
-3.4575));
#71563=CARTESIAN_POINT('Ctrl Pts',(-0.296017391187458,0.382867065282375,
-3.4575));
#71564=CARTESIAN_POINT('Ctrl Pts',(-0.277377076349629,0.400084084934052,
-3.4575));
#71565=CARTESIAN_POINT('Ctrl Pts',(-0.257392306372362,0.415838166281252,
-3.4575));
#71566=CARTESIAN_POINT('Ctrl Pts',(-0.236192234025625,0.429962070234951,
-3.4575));
#71567=CARTESIAN_POINT('Ctrl Pts',(-0.229849434346378,0.434187767770413,
-3.4575));
#71568=CARTESIAN_POINT('Ctrl Pts',(-0.223397598075027,0.438267297508737,
-3.4575));
#71569=CARTESIAN_POINT('Ctrl Pts',(-0.216839587231055,0.442195480991683,
-3.4575));
#71570=CARTESIAN_POINT('Ctrl Pts',(-0.236825839292548,-0.331770464644068,
-3.4575));
#71571=CARTESIAN_POINT('Ctrl Pts',(-0.134134507353825,-0.404131753741505,
-3.45009667810918));
#71572=CARTESIAN_POINT('Ctrl Pts',(0.154860635227925,-0.45076080285477,
-3.43474396219895));
#71573=CARTESIAN_POINT('Ctrl Pts',(0.464962259161517,-0.123953347438615,
-3.41144185226931));
#71574=CARTESIAN_POINT('Ctrl Pts',(0.356070675898753,0.323893827689701,
-3.38759367021108));
#71575=CARTESIAN_POINT('Ctrl Pts',(-0.0797710380057583,0.474714264786181,
-3.36374548815284));
#71576=CARTESIAN_POINT('Ctrl Pts',(-0.370502916327729,0.246248299571174,
-3.34462050911336));
#71577=CARTESIAN_POINT('Ctrl Pts',(-0.406716221540625,0.0553845436928955,
-3.33344492409328));
#71578=CARTESIAN_POINT('Ctrl Pts',(-0.406471795258815,0.00019713841655692,
-3.33021873309261));
#71579=CARTESIAN_POINT('Origin',(-4.52129938221115E-17,0.,-3.4575));
#71580=CARTESIAN_POINT('',(-0.4925,-6.03138548580071E-17,-3.4575));
#71581=CARTESIAN_POINT('Origin',(0.,0.,-3.4575));
#71582=CARTESIAN_POINT('Origin',(0.,0.,-3.4575));
#71583=CARTESIAN_POINT('',(0.23623075609233,-0.331488661006747,-3.4575));
#71584=CARTESIAN_POINT('Ctrl Pts',(0.217494704229604,0.442648936192906,
-3.4575));
#71585=CARTESIAN_POINT('Ctrl Pts',(0.227151161842225,0.436927031618297,
-3.4575));
#71586=CARTESIAN_POINT('Ctrl Pts',(0.236581718719849,0.430861971334928,
-3.4575));
#71587=CARTESIAN_POINT('Ctrl Pts',(0.245765220410661,0.424452886643136,
-3.4575));
#71588=CARTESIAN_POINT('Ctrl Pts',(0.261762891981356,0.41328825299684,-3.4575));
#71589=CARTESIAN_POINT('Ctrl Pts',(0.277011667809708,0.401080195483046,
-3.4575));
#71590=CARTESIAN_POINT('Ctrl Pts',(0.291463300048419,0.38793234921563,-3.4575));
#71591=CARTESIAN_POINT('Ctrl Pts',(0.299171148542744,0.380919881323978,
-3.4575));
#71592=CARTESIAN_POINT('Ctrl Pts',(0.306652003669299,0.373639876799799,
-3.4575));
#71593=CARTESIAN_POINT('Ctrl Pts',(0.313896822610377,0.366107029970977,
-3.4575));
#71594=CARTESIAN_POINT('Ctrl Pts',(0.318563214856714,0.361255118788553,
-3.4575));
#71595=CARTESIAN_POINT('Ctrl Pts',(0.323129211638469,0.35630067653166,-3.4575));
#71596=CARTESIAN_POINT('Ctrl Pts',(0.327587182139254,0.351254289248762,
-3.4575));
#71597=CARTESIAN_POINT('Ctrl Pts',(0.344475362309805,0.332137003113971,
-3.4575));
#71598=CARTESIAN_POINT('Ctrl Pts',(0.35984203627762,0.311676053598004,-3.4575));
#71599=CARTESIAN_POINT('Ctrl Pts',(0.37356594240373,0.290097909978538,-3.4575));
#71600=CARTESIAN_POINT('Ctrl Pts',(0.378533439188415,0.282287498127555,
-3.4575));
#71601=CARTESIAN_POINT('Ctrl Pts',(0.383285254569069,0.274330522722929,
-3.4575));
#71602=CARTESIAN_POINT('Ctrl Pts',(0.387814010524765,0.266237265287823,
-3.4575));
#71603=CARTESIAN_POINT('Ctrl Pts',(0.390544998544752,0.261356766246991,
-3.4575));
#71604=CARTESIAN_POINT('Ctrl Pts',(0.39319399866812,0.25642801685015,-3.4575));
#71605=CARTESIAN_POINT('Ctrl Pts',(0.395755363081162,0.251461797430097,
-3.4575));
#71606=CARTESIAN_POINT('Ctrl Pts',(0.407165733601745,0.229338274755702,
-3.4575));
#71607=CARTESIAN_POINT('Ctrl Pts',(0.416866719135654,0.20642676787138,-3.4575));
#71608=CARTESIAN_POINT('Ctrl Pts',(0.424745143572822,0.182936674070674,
-3.4575));
#71609=CARTESIAN_POINT('Ctrl Pts',(0.432423237211658,0.160043881073128,
-3.4575));
#71610=CARTESIAN_POINT('Ctrl Pts',(0.438370511455948,0.13660029841765,-3.4575));
#71611=CARTESIAN_POINT('Ctrl Pts',(0.442433727764424,0.112796995411841,
-3.4575));
#71612=CARTESIAN_POINT('Ctrl Pts',(0.443454271781346,0.106818401947623,
-3.4575));
#71613=CARTESIAN_POINT('Ctrl Pts',(0.444355706852267,0.100817152549543,
-3.4575));
#71614=CARTESIAN_POINT('Ctrl Pts',(0.445135080697175,0.0947963852933782,
-3.4575));
#71615=CARTESIAN_POINT('Ctrl Pts',(0.445940883140782,0.088571453575303,
-3.4575));
#71616=CARTESIAN_POINT('Ctrl Pts',(0.44661511688423,0.0823332556971779,
-3.4575));
#71617=CARTESIAN_POINT('Ctrl Pts',(0.447154936518576,0.0760926679104064,
-3.4575));
#71618=CARTESIAN_POINT('Ctrl Pts',(0.448735717878663,0.0578180364934373,
-3.4575));
#71619=CARTESIAN_POINT('Ctrl Pts',(0.449167900960623,0.0395027025829728,
-3.4575));
#71620=CARTESIAN_POINT('Ctrl Pts',(0.448392616133184,0.021231823691261,
-3.4575));
#71621=CARTESIAN_POINT('Ctrl Pts',(0.447505993275466,0.000337078582567013,
-3.4575));
#71622=CARTESIAN_POINT('Ctrl Pts',(0.445040447967601,-0.020500296725011,
-3.4575));
#71623=CARTESIAN_POINT('Ctrl Pts',(0.4410627946643,-0.0411137620726926,
-3.4575));
#71624=CARTESIAN_POINT('Ctrl Pts',(0.439232335579409,-0.0505997836134454,
-3.4575));
#71625=CARTESIAN_POINT('Ctrl Pts',(0.437081273421581,-0.06003821102663,
-3.4575));
#71626=CARTESIAN_POINT('Ctrl Pts',(0.434614336619626,-0.069411603243447,
-3.4575));
#71627=CARTESIAN_POINT('Ctrl Pts',(0.432800575766688,-0.0763031830555531,
-3.4575));
#71628=CARTESIAN_POINT('Ctrl Pts',(0.430814830929698,-0.0831625935919254,
-3.4575));
#71629=CARTESIAN_POINT('Ctrl Pts',(0.428666939775117,-0.0899588063351191,
-3.4575));
#71630=CARTESIAN_POINT('Ctrl Pts',(0.421594724438486,-0.112336234488735,
-3.4575));
#71631=CARTESIAN_POINT('Ctrl Pts',(0.412755846768818,-0.13408393119108,
-3.4575));
#71632=CARTESIAN_POINT('Ctrl Pts',(0.402255176200046,-0.154969058094331,
-3.4575));
#71633=CARTESIAN_POINT('Ctrl Pts',(0.396775801082079,-0.165867166357014,
-3.4575));
#71634=CARTESIAN_POINT('Ctrl Pts',(0.390843182289698,-0.176530007122764,
-3.4575));
#71635=CARTESIAN_POINT('Ctrl Pts',(0.384467909415291,-0.186920817753301,
-3.4575));
#71636=CARTESIAN_POINT('Ctrl Pts',(0.377607033364656,-0.198103094215212,
-3.4575));
#71637=CARTESIAN_POINT('Ctrl Pts',(0.37023347161565,-0.208970394721843,
-3.4575));
#71638=CARTESIAN_POINT('Ctrl Pts',(0.362365932264957,-0.21948819497612,
-3.4575));
#71639=CARTESIAN_POINT('Ctrl Pts',(0.358211148066264,-0.225042560623827,
-3.4575));
#71640=CARTESIAN_POINT('Ctrl Pts',(0.353916358841732,-0.230501651312997,
-3.4575));
#71641=CARTESIAN_POINT('Ctrl Pts',(0.349500387143519,-0.235841268640749,
-3.4575));
#71642=CARTESIAN_POINT('Ctrl Pts',(0.335009267560686,-0.253363354041415,
-3.4575));
#71643=CARTESIAN_POINT('Ctrl Pts',(0.319184772663791,-0.26964621528388,
-3.4575));
#71644=CARTESIAN_POINT('Ctrl Pts',(0.302148777404973,-0.284534751709626,
-3.4575));
#71645=CARTESIAN_POINT('Ctrl Pts',(0.285535708385829,-0.299053673526473,
-3.4575));
#71646=CARTESIAN_POINT('Ctrl Pts',(0.267769531136388,-0.312247224204637,
-3.4575));
#71647=CARTESIAN_POINT('Ctrl Pts',(0.248942033157039,-0.323927335938675,
-3.4575));
#71648=CARTESIAN_POINT('Ctrl Pts',(0.24475711745839,-0.326523553609836,
-3.4575));
#71649=CARTESIAN_POINT('Ctrl Pts',(0.240519713189094,-0.329044800635418,
-3.4575));
#71650=CARTESIAN_POINT('Ctrl Pts',(0.236230756092332,-0.331488661006746,
-3.4575));
#71651=CARTESIAN_POINT('Origin',(0.,0.,-3.4575));
#71652=CARTESIAN_POINT('Origin',(0.,0.,-3.73478126690739));
#71653=CARTESIAN_POINT('Ctrl Pts',(0.236230756092329,-0.331488661006748,
-3.4575));
#71654=CARTESIAN_POINT('Ctrl Pts',(0.291420873096492,-0.292158196341315,
-3.45352530299029));
#71655=CARTESIAN_POINT('Ctrl Pts',(0.380867829859202,-0.185560026793827,
-3.44557590897088));
#71656=CARTESIAN_POINT('Ctrl Pts',(0.440039431000898,0.0889589528409691,
-3.42967712093207));
#71657=CARTESIAN_POINT('Ctrl Pts',(0.241551031548769,0.416306162933455,
-3.40980363588352));
#71658=CARTESIAN_POINT('Ctrl Pts',(-0.22013291818294,0.428338358383622,
-3.3859554538253));
#71659=CARTESIAN_POINT('Ctrl Pts',(-0.401074963635459,0.16153375529599,
-3.36928133083325));
#71660=CARTESIAN_POINT('Ctrl Pts',(-0.407613746698895,0.0133760251655175,
-3.36055660186061));
#71661=CARTESIAN_POINT('Ctrl Pts',(-0.407524236888043,0.000202371512057618,
-3.35978126690739));
#71662=CARTESIAN_POINT('Ctrl Pts',(0.285821514250022,-0.401076441581682,
-3.50683458050225));
#71663=CARTESIAN_POINT('Ctrl Pts',(0.35259742046437,-0.353489526343442,
-3.50285988349255));
#71664=CARTESIAN_POINT('Ctrl Pts',(0.460821535943143,-0.224513728524654,
-3.49491048947313));
#71665=CARTESIAN_POINT('Ctrl Pts',(0.532414739633811,0.10763366729929,-3.47901170143431));
#71666=CARTESIAN_POINT('Ctrl Pts',(0.292258648907431,0.503699263591024,
-3.45913821638578));
#71667=CARTESIAN_POINT('Ctrl Pts',(-0.266344336580512,0.518257318520905,
-3.43529003432755));
#71668=CARTESIAN_POINT('Ctrl Pts',(-0.579463933371572,0.0565528565653229,
-3.41144185226931));
#71669=CARTESIAN_POINT('Ctrl Pts',(-0.36140270524706,-0.456693171189222,
-3.38759367021108));
#71670=CARTESIAN_POINT('Ctrl Pts',(0.188579049697867,-0.551047079719571,
-3.36374548815284));
#71671=CARTESIAN_POINT('Ctrl Pts',(0.565365809375224,-0.139648741035217,
-3.33989730609461));
#71672=CARTESIAN_POINT('Ctrl Pts',(0.42343405354387,0.39984578150713,-3.31604912403638));
#71673=CARTESIAN_POINT('Ctrl Pts',(-0.107093777855668,0.572455898084804,
-3.29220094197814));
#71674=CARTESIAN_POINT('Ctrl Pts',(-0.539328090055823,0.219750171019256,
-3.26835275991991));
#71675=CARTESIAN_POINT('Ctrl Pts',(-0.476670081241653,-0.334597761312887,
-3.24450457786167));
#71676=CARTESIAN_POINT('Ctrl Pts',(0.0234001526480324,-0.58191259930159,
-3.22065639580343));
#71677=CARTESIAN_POINT('Ctrl Pts',(0.501994730637598,-0.295245409122807,
-3.19680821374521));
#71678=CARTESIAN_POINT('Ctrl Pts',(0.519945729935783,0.262346662895907,
-3.17296003168696));
#71679=CARTESIAN_POINT('Ctrl Pts',(0.0607784178287687,0.579202235152385,
-3.14911184962874));
#71680=CARTESIAN_POINT('Ctrl Pts',(-0.454160536196269,0.364564524813034,
-3.1252636675705));
#71681=CARTESIAN_POINT('Ctrl Pts',(-0.552348639443532,-0.184608179799961,
-3.10141548551227));
#71682=CARTESIAN_POINT('Ctrl Pts',(-0.143685264422752,-0.564379059995498,
-3.07756730345403));
#71683=CARTESIAN_POINT('Ctrl Pts',(0.396827877163523,-0.426259070653351,
-3.0537191213958));
#71684=CARTESIAN_POINT('Ctrl Pts',(0.573200113780989,0.103008764053386,
-3.02987093933756));
#71685=CARTESIAN_POINT('Ctrl Pts',(0.223587044257181,0.537752736345724,
-3.00602275727933));
#71686=CARTESIAN_POINT('Ctrl Pts',(-0.331196067315227,0.479038969850997,
-2.98217457522109));
#71687=CARTESIAN_POINT('Ctrl Pts',(-0.582063927005535,-0.0192550475321526,
-2.95832639316286));
#71688=CARTESIAN_POINT('Ctrl Pts',(-0.298812798670071,-0.499880068214747,
-2.93447821110462));
#71689=CARTESIAN_POINT('Ctrl Pts',(0.258637744622312,-0.521800429360905,
-2.91063002904639));
#71690=CARTESIAN_POINT('Ctrl Pts',(0.578754684066404,-0.0649013637714588,
-2.88678184698815));
#71691=CARTESIAN_POINT('Ctrl Pts',(0.367789296146031,0.451553103041694,
-2.86293366492992));
#71692=CARTESIAN_POINT('Ctrl Pts',(-0.1806703713665,0.553649156160662,-2.83908548287168));
#71693=CARTESIAN_POINT('Ctrl Pts',(-0.563341590261651,0.147700453392908,
-2.81523730081345));
#71694=CARTESIAN_POINT('Ctrl Pts',(-0.429073990452302,-0.393782531289495,
-2.79138911875521));
#71695=CARTESIAN_POINT('Ctrl Pts',(0.0989245277950369,-0.573919078817807,
-2.76754093669698));
#71696=CARTESIAN_POINT('Ctrl Pts',(0.536146988652502,-0.227410592970535,
-2.74369275463874));
#71697=CARTESIAN_POINT('Ctrl Pts',(0.48138519743957,0.327776544187327,-2.71984457258051));
#71698=CARTESIAN_POINT('Ctrl Pts',(-0.0151098149378764,0.582186280090831,
-2.69599639052227));
#71699=CARTESIAN_POINT('Ctrl Pts',(-0.497739616547707,0.302364755474486,
-2.67214820846404));
#71700=CARTESIAN_POINT('Ctrl Pts',(-0.523628900812201,-0.254915565370088,
-2.6483000264058));
#71701=CARTESIAN_POINT('Ctrl Pts',(-0.0690208987404531,-0.578277862943811,
-2.62445184434757));
#71702=CARTESIAN_POINT('Ctrl Pts',(0.448922710846462,-0.370995378569811,
-2.60060366228934));
#71703=CARTESIAN_POINT('Ctrl Pts',(0.55492163212046,0.176723381131619,-2.5767554802311));
#71704=CARTESIAN_POINT('Ctrl Pts',(0.151708136070267,0.562275566500915,
-2.55290729817287));
#71705=CARTESIAN_POINT('Ctrl Pts',(-0.390717209409772,0.431867147980593,
-2.52905911611463));
#71706=CARTESIAN_POINT('Ctrl Pts',(-0.574608947300046,-0.0948352725338707,
-2.5052109340564));
#71707=CARTESIAN_POINT('Ctrl Pts',(-0.231222608189202,-0.534514056593488,
-2.48136275199816));
#71708=CARTESIAN_POINT('Ctrl Pts',(0.324340399555256,-0.483707015093002,
-2.45751456993993));
#71709=CARTESIAN_POINT('Ctrl Pts',(0.582279113465016,0.010963815769983,
-2.43366638788169));
#71710=CARTESIAN_POINT('Ctrl Pts',(0.305901380218176,0.495573926689509,
-2.40981820582346));
#71711=CARTESIAN_POINT('Ctrl Pts',(-0.251180460180701,0.525430821000496,
-2.38597002376523));
#71712=CARTESIAN_POINT('Ctrl Pts',(-0.577771719730372,0.0731369339913324,
-2.36212184170699));
#71713=CARTESIAN_POINT('Ctrl Pts',(-0.374182649237275,-0.446269555586775,
-2.33827365964876));
#71714=CARTESIAN_POINT('Ctrl Pts',(0.172767429928028,-0.556165970183279,
-2.31442547759052));
#71715=CARTESIAN_POINT('Ctrl Pts',(0.561181031983256,-0.155708126236403,
-2.29057729553229));
#71716=CARTESIAN_POINT('Ctrl Pts',(0.434638407227192,0.387632075810108,
-2.26672911347405));
#71717=CARTESIAN_POINT('Ctrl Pts',(-0.0907412085475953,0.575269679633096,
-2.24288093141582));
#71718=CARTESIAN_POINT('Ctrl Pts',(-0.5328540214427,0.235022899025148,-2.21903274935759));
#71719=CARTESIAN_POINT('Ctrl Pts',(-0.486004305875971,-0.320887808905013,
-2.19518456729935));
#71720=CARTESIAN_POINT('Ctrl Pts',(0.00681726066985583,-0.582342421768158,
-2.17133638524111));
#71721=CARTESIAN_POINT('Ctrl Pts',(0.493383108237918,-0.30942249391299,
-2.14748820318288));
#71722=CARTESIAN_POINT('Ctrl Pts',(0.527206098669985,0.24743261862377,-2.12364002112464));
#71723=CARTESIAN_POINT('Ctrl Pts',(0.0772492607576471,0.57723627999827,
-2.09979183906641));
#71724=CARTESIAN_POINT('Ctrl Pts',(-0.443593771763116,0.377350946582644,
-2.07594365700817));
#71725=CARTESIAN_POINT('Ctrl Pts',(-0.557382107269562,-0.168802718371432,
-2.05209547494994));
#71726=CARTESIAN_POINT('Ctrl Pts',(-0.159700221059351,-0.560058042195126,
-2.02824729289171));
#71727=CARTESIAN_POINT('Ctrl Pts',(0.384527286921104,-0.437387627679315,
-2.00439911083347));
#71728=CARTESIAN_POINT('Ctrl Pts',(0.575901242316084,0.0866425434335488,
-1.98055092877524));
#71729=CARTESIAN_POINT('Ctrl Pts',(0.238811272779486,0.53116696737211,-1.956702746717));
#71730=CARTESIAN_POINT('Ctrl Pts',(-0.317418947303206,0.488276953302907,
-1.93285456465877));
#71731=CARTESIAN_POINT('Ctrl Pts',(-0.58237620179046,-0.00267035989340219,
-1.90900638260054));
#71732=CARTESIAN_POINT('Ctrl Pts',(-0.312927918017016,-0.491167272280409,
-1.8851582005423));
#71733=CARTESIAN_POINT('Ctrl Pts',(0.243672230737431,-0.528954643803501,
-1.86131001848407));
#71734=CARTESIAN_POINT('Ctrl Pts',(0.576671570897583,-0.0813576705194944,
-1.83746183642583));
#71735=CARTESIAN_POINT('Ctrl Pts',(0.380500109954069,0.440895495053855,
-1.8136136543676));
#71736=CARTESIAN_POINT('Ctrl Pts',(-0.164829447496658,0.558569981713831,
-1.78976547230936));
#71737=CARTESIAN_POINT('Ctrl Pts',(-0.558906654078905,0.163684218115762,
-1.76591729025113));
#71738=CARTESIAN_POINT('Ctrl Pts',(-0.44011466993486,-0.381403000174322,
-1.74206910819289));
#71739=CARTESIAN_POINT('Ctrl Pts',(0.0825394850188265,-0.576503603324966,
-1.71822092613466));
#71740=CARTESIAN_POINT('Ctrl Pts',(0.529452979925558,-0.242587537358763,
-1.69437274407642));
#71741=CARTESIAN_POINT('Ctrl Pts',(0.490524842136848,0.313933990642086,
-1.67052456201819));
#71742=CARTESIAN_POINT('Ctrl Pts',(0.00147667628643591,0.582380451819074,
-1.64667637995995));
#71743=CARTESIAN_POINT('Ctrl Pts',(-0.488926531173269,0.316417474784054,
-1.62282819790172));
#71744=CARTESIAN_POINT('Ctrl Pts',(-0.530676367739226,-0.239899487196084,
-1.59898001584349));
#71745=CARTESIAN_POINT('Ctrl Pts',(-0.0854619549556686,-0.576077621062474,
-1.57513183378525));
#71746=CARTESIAN_POINT('Ctrl Pts',(0.438174862277943,-0.383629979669929,
-1.55128365172701));
#71747=CARTESIAN_POINT('Ctrl Pts',(0.559729533283666,0.160847818772567,
-1.52743546966878));
#71748=CARTESIAN_POINT('Ctrl Pts',(0.167659915392895,0.557726926016926,
-1.50358728761054));
#71749=CARTESIAN_POINT('Ctrl Pts',(-0.378259373989984,0.442819395716301,
-1.47973910555231));
#71750=CARTESIAN_POINT('Ctrl Pts',(-0.5770767321164,-0.0784322413532939,
-1.45589092349408));
#71751=CARTESIAN_POINT('Ctrl Pts',(-0.246351501283537,-0.527712146012568,
-1.43204274143584));
#71752=CARTESIAN_POINT('Ctrl Pts',(0.310433115630021,-0.49274785839624,
-1.40819455937761));
#71753=CARTESIAN_POINT('Ctrl Pts',(0.582355171638496,-0.00562363758986257,
-1.38434637731937));
#71754=CARTESIAN_POINT('Ctrl Pts',(0.319890987272491,0.486660998535609,
-1.36049819526114));
#71755=CARTESIAN_POINT('Ctrl Pts',(-0.23611457930063,0.532371183175357,
-1.3366500132029));
#71756=CARTESIAN_POINT('Ctrl Pts',(-0.575454460609791,0.0895619059541361,
-1.31280183114467));
#71757=CARTESIAN_POINT('Ctrl Pts',(-0.386740397026913,-0.435432011387898,
-1.28895364908643));
#71758=CARTESIAN_POINT('Ctrl Pts',(0.156858034091794,-0.560860703182797,
-1.2651054670282));
#71759=CARTESIAN_POINT('Ctrl Pts',(0.556518917828539,-0.171627111298872,
-1.24125728496997));
#71760=CARTESIAN_POINT('Ctrl Pts',(0.445501667877689,0.375096567768941,
-1.21740910291173));
#71761=CARTESIAN_POINT('Ctrl Pts',(-0.0743210206990269,0.577620599629289,
-1.1935609208535));
#71762=CARTESIAN_POINT('Ctrl Pts',(-0.52594455390394,0.250102973698091,
-1.16971273879526));
#71763=CARTESIAN_POINT('Ctrl Pts',(-0.494945889360727,-0.306916499782533,
-1.14586455673702));
#71764=CARTESIAN_POINT('Ctrl Pts',(-0.00977031374086975,-0.582300362530584,
-1.12201637467879));
#71765=CARTESIAN_POINT('Ctrl Pts',(0.484370789243626,-0.323348279354245,
-1.09816819262055));
#71766=CARTESIAN_POINT('Ctrl Pts',(0.534039004174506,0.232317698968773,
-1.07432001056233));
#71767=CARTESIAN_POINT('Ctrl Pts',(0.0936573156226028,0.574802121137536,
-1.05047182850409));
#71768=CARTESIAN_POINT('Ctrl Pts',(-0.432667081462839,0.389831204308058,
-1.02662364644585));
#71769=CARTESIAN_POINT('Ctrl Pts',(-0.561963434054077,-0.15286029576054,
-1.00277546438762));
#71770=CARTESIAN_POINT('Ctrl Pts',(-0.175585604672873,-0.555282690767055,
-0.978927282329385));
#71771=CARTESIAN_POINT('Ctrl Pts',(0.371914741884562,-0.448161350411617,
-0.955079100271149));
#71772=CARTESIAN_POINT('Ctrl Pts',(0.578135178286308,0.0702060315197663,
-0.931230918212915));
#71773=CARTESIAN_POINT('Ctrl Pts',(0.253841764380009,0.524150293227283,
-0.90738273615468));
#71774=CARTESIAN_POINT('Ctrl Pts',(-0.303384321413146,0.497118823576847,
-0.883534554096446));
#71775=CARTESIAN_POINT('Ctrl Pts',(-0.582216027274799,0.0139164944779112,
-0.859686372038211));
#71776=CARTESIAN_POINT('Ctrl Pts',(-0.326789175723116,-0.48205601942478,
-0.835838189979976));
#71777=CARTESIAN_POINT('Ctrl Pts',(0.228509038724162,-0.535679746168062,
-0.811990007921742));
#71778=CARTESIAN_POINT('Ctrl Pts',(0.574120635725452,-0.0977479762990466,
-0.788141825863507));
#71779=CARTESIAN_POINT('Ctrl Pts',(0.39290224478655,0.429880212701446,-0.764293643805274));
#71780=CARTESIAN_POINT('Ctrl Pts',(-0.148854806480243,0.563037669982351,
-0.740445461747037));
#71781=CARTESIAN_POINT('Ctrl Pts',(-0.554018307532132,0.179535194795418,
-0.716597279688804));
#71782=CARTESIAN_POINT('Ctrl Pts',(-0.450798308426413,-0.368714057674789,
-0.692749097630568));
#71783=CARTESIAN_POINT('Ctrl Pts',(0.0660874824133674,-0.578620441994957,
-0.668900915572334));
#71784=CARTESIAN_POINT('Ctrl Pts',(0.522329455071808,-0.257567683750478,
-0.645052733514099));
#71785=CARTESIAN_POINT('Ctrl Pts',(0.499266550653832,0.299836759625578,
-0.621204551455865));
#71786=CARTESIAN_POINT('Ctrl Pts',(0.0180619699673387,0.582102170145686,
-0.597356369397629));
#71787=CARTESIAN_POINT('Ctrl Pts',(-0.479716807224914,0.330213501908238,
-0.573508187339396));
#71788=CARTESIAN_POINT('Ctrl Pts',(-0.537293324476905,-0.224688791695386,
-0.549660005281161));
#71789=CARTESIAN_POINT('Ctrl Pts',(-0.101833683409545,-0.5734100389165,
-0.525811823222927));
#71790=CARTESIAN_POINT('Ctrl Pts',(0.427071551879351,-0.395953362766007,
-0.501963641164691));
#71791=CARTESIAN_POINT('Ctrl Pts',(0.564083346009815,0.144841769399363,
-0.478115459106457));
#71792=CARTESIAN_POINT('Ctrl Pts',(0.183475701526128,0.552725832147485,
-0.454267277048223));
#71793=CARTESIAN_POINT('Ctrl Pts',(-0.365494716062787,0.453412408381549,
-0.430419094989988));
#71794=CARTESIAN_POINT('Ctrl Pts',(-0.579076292012319,-0.0619655825398327,
-0.406570912931754));
#71795=CARTESIAN_POINT('Ctrl Pts',(-0.261280685166963,-0.520482131141858,
-0.382722730873519));
#71796=CARTESIAN_POINT('Ctrl Pts',(0.296274267374466,-0.501388962884901,
-0.358874548815284));
#71797=CARTESIAN_POINT('Ctrl Pts',(0.581958272836576,-0.0222065277132291,
-0.335026366757049));
#71798=CARTESIAN_POINT('Ctrl Pts',(0.333622090090629,0.477353266851129,
-0.311178184698815));
#71799=CARTESIAN_POINT('Ctrl Pts',(-0.220859081953995,0.538879665737125,
-0.28733000264058));
#71800=CARTESIAN_POINT('Ctrl Pts',(-0.572666661988016,0.105914213558689,
-0.263481820582346));
#71801=CARTESIAN_POINT('Ctrl Pts',(-0.398991513710596,-0.424241210273597,
-0.239633638524111));
#71802=CARTESIAN_POINT('Ctrl Pts',(0.140835033897246,-0.565100468869743,
-0.215785456465876));
#71803=CARTESIAN_POINT('Ctrl Pts',(0.551379140596833,-0.187406810436341,
-0.191937274407642));
#71804=CARTESIAN_POINT('Ctrl Pts',(0.456053783787644,0.36225666087098,-0.168089092349407));
#71805=CARTESIAN_POINT('Ctrl Pts',(-0.0579370393971914,0.57950312116213,
-0.144240910291172));
#71806=CARTESIAN_POINT('Ctrl Pts',(-0.518422960159868,0.264979829502608,
-0.120392728232938));
#71807=CARTESIAN_POINT('Ctrl Pts',(-0.503844216133415,-0.292696019272375,
-0.0965445461747031));
#71808=CARTESIAN_POINT('Ctrl Pts',(-0.0256409405766145,-0.581782268696529,
-0.0726963641164688));
#71809=CARTESIAN_POINT('Ctrl Pts',(0.390234871038739,-0.377845479979599,
-0.0528228790679399));
#71810=CARTESIAN_POINT('Ctrl Pts',(0.509133042526885,-0.0595520553159744,
-0.0369240910291169));
#71811=CARTESIAN_POINT('Ctrl Pts',(0.487584520760919,0.107429610755057,
-0.0289746970097051));
#71812=CARTESIAN_POINT('Ctrl Pts',(0.457029747534529,0.183521279061925,
-0.0249999999999995));
#71813=CARTESIAN_POINT('Ctrl Pts',(0.269291261530791,-0.377880514723371,
-3.49038972033484));
#71814=CARTESIAN_POINT('Ctrl Pts',(0.332205238008411,-0.333045749676066,
-3.48641502332513));
#71815=CARTESIAN_POINT('Ctrl Pts',(0.434170300581829,-0.211529161281045,
-3.47846562930572));
#71816=CARTESIAN_POINT('Ctrl Pts',(0.501622970089507,0.10140876247985,-3.46256684126689));
#71817=CARTESIAN_POINT('Ctrl Pts',(0.275356109787877,0.474568230038501,
-3.44269335621837));
#71818=CARTESIAN_POINT('Ctrl Pts',(-0.250940530447988,0.488284331808477,
-3.41884517416013));
#71819=CARTESIAN_POINT('Ctrl Pts',(-0.545951112318035,0.0532821685155709,
-3.3949969921019));
#71820=CARTESIAN_POINT('Ctrl Pts',(-0.340501276371688,-0.430280696415537,
-3.37114881004366));
#71821=CARTESIAN_POINT('Ctrl Pts',(0.177672735114664,-0.519177724076906,
-3.34730062798543));
#71822=CARTESIAN_POINT('Ctrl Pts',(0.53266834175349,-0.131572270699203,
-3.32345244592719));
#71823=CARTESIAN_POINT('Ctrl Pts',(0.398945092545343,0.376721028864299,
-3.29960426386896));
#71824=CARTESIAN_POINT('Ctrl Pts',(-0.100900097099143,0.539348381000982,
-3.27575608181072));
#71825=CARTESIAN_POINT('Ctrl Pts',(-0.508136492563255,0.207041100214791,
-3.25190789975249));
#71826=CARTESIAN_POINT('Ctrl Pts',(-0.449102258268996,-0.31524657437266,
-3.22805971769425));
#71827=CARTESIAN_POINT('Ctrl Pts',(0.0220468240228047,-0.548258161663471,
-3.20421153563602));
#71828=CARTESIAN_POINT('Ctrl Pts',(0.472962277349624,-0.278170133177261,
-3.18036335357779));
#71829=CARTESIAN_POINT('Ctrl Pts',(0.489875095334758,0.247174058940269,
-3.15651517151955));
#71830=CARTESIAN_POINT('Ctrl Pts',(0.0572633479110232,0.545704549200595,
-3.13266698946132));
#71831=CARTESIAN_POINT('Ctrl Pts',(-0.427894534289014,0.343480234697789,
-3.10881880740308));
#71832=CARTESIAN_POINT('Ctrl Pts',(-0.520404009162348,-0.173931517218637,
-3.08497062534485));
#71833=CARTESIAN_POINT('Ctrl Pts',(-0.135375345069165,-0.531738660214371,
-3.06112244328661));
#71834=CARTESIAN_POINT('Ctrl Pts',(0.373877662541782,-0.401606727108627,
-3.03727426122838));
#71835=CARTESIAN_POINT('Ctrl Pts',(0.540049555593113,0.097051336717778,
-3.01342607917014));
#71836=CARTESIAN_POINT('Ctrl Pts',(0.210656071037705,0.506652248142177,
-2.98957789711191));
#71837=CARTESIAN_POINT('Ctrl Pts',(-0.312041614555778,0.45133414414963,
-2.96572971505367));
#71838=CARTESIAN_POINT('Ctrl Pts',(-0.548400737453845,-0.0181414476596504,
-2.94188153299544));
#71839=CARTESIAN_POINT('Ctrl Pts',(-0.281531205677612,-0.470969914692616,
-2.9180333509372));
#71840=CARTESIAN_POINT('Ctrl Pts',(0.243679642911331,-0.491622529740674,
-2.89418516887897));
#71841=CARTESIAN_POINT('Ctrl Pts',(0.545282881864391,-0.0611478466585844,
-2.87033698682073));
#71842=CARTESIAN_POINT('Ctrl Pts',(0.346518504027128,0.425437899891161,
-2.8464888047625));
#71843=CARTESIAN_POINT('Ctrl Pts',(-0.170221448704391,0.521629311562401,
-2.82264062270426));
#71844=CARTESIAN_POINT('Ctrl Pts',(-0.530761191691188,0.139158318880268,
-2.79879244064603));
#71845=CARTESIAN_POINT('Ctrl Pts',(-0.404258848331051,-0.371008441747237,
-2.77494425858779));
#71846=CARTESIAN_POINT('Ctrl Pts',(0.0932033089117306,-0.540726939877041,
-2.75109607652956));
#71847=CARTESIAN_POINT('Ctrl Pts',(0.505139367549047,-0.21425848794899,
-2.72724789447133));
#71848=CARTESIAN_POINT('Ctrl Pts',(0.453544679591033,0.308819856741773,
-2.70339971241309));
#71849=CARTESIAN_POINT('Ctrl Pts',(-0.0142359511907082,0.54851601434886,
-2.67955153035486));
#71850=CARTESIAN_POINT('Ctrl Pts',(-0.468953254291192,0.284877737975132,
-2.65570334829662));
#71851=CARTESIAN_POINT('Ctrl Pts',(-0.493345253046107,-0.240172732841578,
-2.63185516623839));
#71852=CARTESIAN_POINT('Ctrl Pts',(-0.0650291317033143,-0.544833637300124,
-2.60800698418015));
#71853=CARTESIAN_POINT('Ctrl Pts',(0.422959634269928,-0.349539165304978,
-2.58415880212192));
#71854=CARTESIAN_POINT('Ctrl Pts',(0.522828194919314,0.166502729410674,
-2.56031062006369));
#71855=CARTESIAN_POINT('Ctrl Pts',(0.142934220518859,0.52975682053983,-2.53646243800545));
#71856=CARTESIAN_POINT('Ctrl Pts',(-0.368120400242892,0.406890465885877,
-2.51261425594722));
#71857=CARTESIAN_POINT('Ctrl Pts',(-0.541376910381746,-0.0893505523727755,
-2.48876607388898));
#71858=CARTESIAN_POINT('Ctrl Pts',(-0.217850038395788,-0.503600874775611,
-2.46491789183075));
#71859=CARTESIAN_POINT('Ctrl Pts',(0.305582438714649,-0.455732216825863,
-2.44106970977251));
#71860=CARTESIAN_POINT('Ctrl Pts',(0.548603478781033,0.0103297324823055,
-2.41722152771428));
#71861=CARTESIAN_POINT('Ctrl Pts',(0.288209824929076,0.466912815328684,
-2.39337334565605));
#71862=CARTESIAN_POINT('Ctrl Pts',(-0.236653644395632,0.495042960659046,
-2.36952516359781));
#71863=CARTESIAN_POINT('Ctrl Pts',(-0.54435676646407,0.0689071194332546,
-2.34567698153958));
#71864=CARTESIAN_POINT('Ctrl Pts',(-0.352542102789,-0.420459922067392,-2.32182879948134));
#71865=CARTESIAN_POINT('Ctrl Pts',(0.16277556739852,-0.524000567711426,
-2.29798061742311));
#71866=CARTESIAN_POINT('Ctrl Pts',(0.528725587527778,-0.146702874536301,
-2.27413243536486));
#71867=CARTESIAN_POINT('Ctrl Pts',(0.409501451628164,0.365213692813172,
-2.25028425330664));
#71868=CARTESIAN_POINT('Ctrl Pts',(-0.085493265217381,0.541999429802538,
-2.2264360712484));
#71869=CARTESIAN_POINT('Ctrl Pts',(-0.502036846395473,0.22143054252992,
-2.20258788919017));
#71870=CARTESIAN_POINT('Ctrl Pts',(-0.457896645681655,-0.302329525811319,
-2.17873970713193));
#71871=CARTESIAN_POINT('Ctrl Pts',(0.00642298999355273,-0.548663125700416,
-2.1548915250737));
#71872=CARTESIAN_POINT('Ctrl Pts',(0.464848701064361,-0.291527297902928,
-2.13104334301546));
#71873=CARTESIAN_POINT('Ctrl Pts',(0.49671556660139,0.233122556179506,-2.10719516095723));
#71874=CARTESIAN_POINT('Ctrl Pts',(0.0727816131557911,0.54385229344947,
-2.08334697889899));
#71875=CARTESIAN_POINT('Ctrl Pts',(-0.41793889000531,0.355527164257441,
-2.05949879684076));
#71876=CARTESIAN_POINT('Ctrl Pts',(-0.525146370507339,-0.159040151681187,
-2.03565061478253));
#71877=CARTESIAN_POINT('Ctrl Pts',(-0.150464089831247,-0.52766754493247,
-2.01180243272429));
#71878=CARTESIAN_POINT('Ctrl Pts',(0.36228846684164,-0.412091673171567,
-1.98795425066605));
#71879=CARTESIAN_POINT('Ctrl Pts',(0.542594466576044,0.081631643036665,
-1.96410606860782));
#71880=CARTESIAN_POINT('Ctrl Pts',(0.224999818797078,0.500447361712587,
-1.94025788654959));
#71881=CARTESIAN_POINT('Ctrl Pts',(-0.299061282973556,0.460037856409686,
-1.91640970449135));
#71882=CARTESIAN_POINT('Ctrl Pts',(-0.548694952082849,-0.00251592182037977,
-1.89256152243312));
#71883=CARTESIAN_POINT('Ctrl Pts',(-0.2948299886806,-0.462761016161045,
-1.86871334037488));
#71884=CARTESIAN_POINT('Ctrl Pts',(0.229579647240638,-0.49836298606204,
-1.84486515831665));
#71885=CARTESIAN_POINT('Ctrl Pts',(0.543320243836196,-0.0766524164105996,
-1.82101697625841));
#71886=CARTESIAN_POINT('Ctrl Pts',(0.358494198349619,0.415396665915208,
-1.79716879420018));
#71887=CARTESIAN_POINT('Ctrl Pts',(-0.155296671666819,0.526265545207944,
-1.77332061214194));
#71888=CARTESIAN_POINT('Ctrl Pts',(-0.526582746403072,0.15421767568734,
-1.74947243008371));
#71889=CARTESIAN_POINT('Ctrl Pts',(-0.41466099917619,-0.359344870654934,
-1.72562424802547));
#71890=CARTESIAN_POINT('Ctrl Pts',(0.077765881638212,-0.5431619905303,-1.70177606596724));
#71891=CARTESIAN_POINT('Ctrl Pts',(0.498832501323434,-0.228557686213378,
-1.677927883909));
#71892=CARTESIAN_POINT('Ctrl Pts',(0.46215574043763,0.295777875921027,-1.65407970185077));
#71893=CARTESIAN_POINT('Ctrl Pts',(0.00139127392523328,0.548698956314547,
-1.63023151979253));
#71894=CARTESIAN_POINT('Ctrl Pts',(-0.460649866476988,0.298117729795697,
-1.6063833377343));
#71895=CARTESIAN_POINT('Ctrl Pts',(-0.499985135506862,-0.226025097225929,
-1.58253515567606));
#71896=CARTESIAN_POINT('Ctrl Pts',(-0.08051933292456,-0.54276064460238,
-1.55868697361783));
#71897=CARTESIAN_POINT('Ctrl Pts',(0.412833378703222,-0.361443054618967,
-1.5348387915596));
#71898=CARTESIAN_POINT('Ctrl Pts',(0.527358035064316,0.151545317172489,
-1.51099060950136));
#71899=CARTESIAN_POINT('Ctrl Pts',(0.157963441775079,0.525471246945423,
-1.48714242744312));
#71900=CARTESIAN_POINT('Ctrl Pts',(-0.356383053511173,0.417209299361676,
-1.46329424538489));
#71901=CARTESIAN_POINT('Ctrl Pts',(-0.543701972888415,-0.0738961770394953,
-1.43944606332666));
#71902=CARTESIAN_POINT('Ctrl Pts',(-0.232103964373433,-0.497192347111199,
-1.41559788126843));
#71903=CARTESIAN_POINT('Ctrl Pts',(0.292479471142316,-0.464250190375963,
-1.39174969921019));
#71904=CARTESIAN_POINT('Ctrl Pts',(0.548675138192466,-0.00529839912485062,
-1.36790151715196));
#71905=CARTESIAN_POINT('Ctrl Pts',(0.301390354539878,0.458515359060233,
-1.34405333509372));
#71906=CARTESIAN_POINT('Ctrl Pts',(-0.22245908637255,0.501581932683083,
-1.32020515303549));
#71907=CARTESIAN_POINT('Ctrl Pts',(-0.542173524123086,0.084382166621627,
-1.29635697097725));
#71908=CARTESIAN_POINT('Ctrl Pts',(-0.364373583540652,-0.410249158343502,
-1.27250878891902));
#71909=CARTESIAN_POINT('Ctrl Pts',(0.14778627841454,-0.528423784680618,
-1.24866060686078));
#71910=CARTESIAN_POINT('Ctrl Pts',(0.524333102919268,-0.161701198161485,
-1.22481242480255));
#71911=CARTESIAN_POINT('Ctrl Pts',(0.419736444513797,0.35340316559239,-1.20096424274431));
#71912=CARTESIAN_POINT('Ctrl Pts',(-0.0700227254579231,0.544214386270018,
-1.17711606068608));
#71913=CARTESIAN_POINT('Ctrl Pts',(-0.495526982241611,0.235638473459511,
-1.15326787862784));
#71914=CARTESIAN_POINT('Ctrl Pts',(-0.466321100023418,-0.289166235886481,
-1.12941969656961));
#71915=CARTESIAN_POINT('Ctrl Pts',(-0.00920525566360501,-0.548623498924331,
-1.10557151451137));
#71916=CARTESIAN_POINT('Ctrl Pts',(0.456357602143208,-0.304647696971287,
-1.08172333245314));
#71917=CARTESIAN_POINT('Ctrl Pts',(0.503153296623432,0.218881795498803,
-1.05787515039491));
#71918=CARTESIAN_POINT('Ctrl Pts',(0.088240721632787,0.541558912168871,
-1.03402696833667));
#71919=CARTESIAN_POINT('Ctrl Pts',(-0.407644135871638,0.367285636519142,
-1.01017878627844));
#71920=CARTESIAN_POINT('Ctrl Pts',(-0.529462740016906,-0.144019745998958,
-0.986330604220201));
#71921=CARTESIAN_POINT('Ctrl Pts',(-0.16543075531971,-0.523168372035383,
-0.962482422161966));
#71922=CARTESIAN_POINT('Ctrl Pts',(0.35040535799689,-0.422242306491027,
-0.938634240103732));
#71923=CARTESIAN_POINT('Ctrl Pts',(0.544699204692694,0.0661457233009084,
-0.914786058045497));
#71924=CARTESIAN_POINT('Ctrl Pts',(0.239161034250552,0.49383649115874,-0.890937875987262));
#71925=CARTESIAN_POINT('Ctrl Pts',(-0.28583833815443,0.468368364372352,
-0.867089693929028));
#71926=CARTESIAN_POINT('Ctrl Pts',(-0.548544041128856,0.0131116454402537,
-0.843241511870794));
#71927=CARTESIAN_POINT('Ctrl Pts',(-0.307889591922411,-0.454176705137236,
-0.819393329812559));
#71928=CARTESIAN_POINT('Ctrl Pts',(0.215293405993889,-0.504699147650254,
-0.795545147754323));
#71929=CARTESIAN_POINT('Ctrl Pts',(0.540916839906339,-0.092094802305981,
-0.77169696569609));
#71930=CARTESIAN_POINT('Ctrl Pts',(0.370179065891787,0.405018443378037,
-0.747848783637855));
#71931=CARTESIAN_POINT('Ctrl Pts',(-0.140245910904111,0.530474848391832,
-0.724000601579619));
#71932=CARTESIAN_POINT('Ctrl Pts',(-0.521977113367245,0.169151924138721,
-0.700152419521386));
#71933=CARTESIAN_POINT('Ctrl Pts',(-0.424726758203037,-0.347389782731771,
-0.67630423746315));
#71934=CARTESIAN_POINT('Ctrl Pts',(0.0622653671022191,-0.545156403572981,
-0.652456055404916));
#71935=CARTESIAN_POINT('Ctrl Pts',(0.49212095968373,-0.242671468131879,
-0.628607873346681));
#71936=CARTESIAN_POINT('Ctrl Pts',(0.470391879416357,0.282495946691564,
-0.604759691288447));
#71937=CARTESIAN_POINT('Ctrl Pts',(0.0170173707567055,0.548436768833369,
-0.580911509230212));
#71938=CARTESIAN_POINT('Ctrl Pts',(-0.451972779355291,0.311115875012766,
-0.557063327171978));
#71939=CARTESIAN_POINT('Ctrl Pts',(-0.506219405981777,-0.211694099816963,
-0.533215145113743));
#71940=CARTESIAN_POINT('Ctrl Pts',(-0.0959442158986505,-0.540247339880686,
-0.509366963055509));
#71941=CARTESIAN_POINT('Ctrl Pts',(0.402372219149679,-0.373053724966781,
-0.485518780997274));
#71942=CARTESIAN_POINT('Ctrl Pts',(0.531460048604374,0.136464964529532,
-0.461670598939039));
#71943=CARTESIAN_POINT('Ctrl Pts',(0.17286453489641,0.520759387235809,-0.437822416880805));
#71944=CARTESIAN_POINT('Ctrl Pts',(-0.344356629099969,0.42718967383251,
-0.41397423482257));
#71945=CARTESIAN_POINT('Ctrl Pts',(-0.545585889878679,-0.0583818539252621,
-0.390126052764335));
#71946=CARTESIAN_POINT('Ctrl Pts',(-0.24616973115849,-0.490380474217275,
-0.366277870706102));
#71947=CARTESIAN_POINT('Ctrl Pts',(0.279139488256261,-0.472391543677784,
-0.342429688647865));
#71948=CARTESIAN_POINT('Ctrl Pts',(0.548301193707043,-0.020922231406565,
-0.318581506589632));
#71949=CARTESIAN_POINT('Ctrl Pts',(0.314327330294862,0.449745932399401,
-0.294733324531397));
#71950=CARTESIAN_POINT('Ctrl Pts',(-0.208085878195641,0.507714002497032,
-0.270885142473163));
#71951=CARTESIAN_POINT('Ctrl Pts',(-0.539546955546815,0.0997887519352769,
-0.247036960414928));
#71952=CARTESIAN_POINT('Ctrl Pts',(-0.375916166944726,-0.399705568027995,
-0.223188778356693));
#71953=CARTESIAN_POINT('Ctrl Pts',(0.132689955287081,-0.532418346998393,
-0.199340596298459));
#71954=CARTESIAN_POINT('Ctrl Pts',(0.519490580485835,-0.176568291348837,
-0.175492414240224));
#71955=CARTESIAN_POINT('Ctrl Pts',(0.42967828745962,0.341305844172893,-0.151644232181989));
#71956=CARTESIAN_POINT('Ctrl Pts',(-0.0545862982692795,0.545988033714885,
-0.127796050123755));
#71957=CARTESIAN_POINT('Ctrl Pts',(-0.488440393699185,0.249654938517161,
-0.10394786806552));
#71958=CARTESIAN_POINT('Ctrl Pts',(-0.474704799369555,-0.275768185196691,
-0.0800996860072854));
#71959=CARTESIAN_POINT('Ctrl Pts',(-0.0241580178204238,-0.548135368621999,
-0.056251503949051));
#71960=CARTESIAN_POINT('Ctrl Pts',(0.367665957515721,-0.355993096721218,
-0.036378018900522));
#71961=CARTESIAN_POINT('Ctrl Pts',(0.479687750828799,-0.0561079110677501,
-0.0204792308616991));
#71962=CARTESIAN_POINT('Ctrl Pts',(0.459385470135524,0.101216507378395,
-0.0125298368422873));
#71963=CARTESIAN_POINT('Ctrl Pts',(0.430597807144122,0.172907476492828,
-0.00855513983258168));
#71964=CARTESIAN_POINT('Ctrl Pts',(0.25276100881156,-0.354684587865059,
-3.47394486016742));
#71965=CARTESIAN_POINT('Ctrl Pts',(0.311813055552452,-0.312601973008691,
-3.46997016315771));
#71966=CARTESIAN_POINT('Ctrl Pts',(0.407519065220516,-0.198544594037436,
-3.4620207691383));
#71967=CARTESIAN_POINT('Ctrl Pts',(0.470831200545202,0.0951838576604093,
-3.44612198109948));
#71968=CARTESIAN_POINT('Ctrl Pts',(0.258453570668323,0.445437196485978,
-3.42624849605095));
#71969=CARTESIAN_POINT('Ctrl Pts',(-0.235536724315465,0.458311345096049,
-3.40240031399271));
#71970=CARTESIAN_POINT('Ctrl Pts',(-0.512438291264498,0.0500114804658197,
-3.37855213193448));
#71971=CARTESIAN_POINT('Ctrl Pts',(-0.319599847496316,-0.403868221641854,
-3.35470394987625));
#71972=CARTESIAN_POINT('Ctrl Pts',(0.166766420531462,-0.487308368434241,
-3.33085576781801));
#71973=CARTESIAN_POINT('Ctrl Pts',(0.499970874131756,-0.123495800363189,
-3.30700758575978));
#71974=CARTESIAN_POINT('Ctrl Pts',(0.374456131546814,0.353596276221467,
-3.28315940370154));
#71975=CARTESIAN_POINT('Ctrl Pts',(-0.0947064163426174,0.506240863917161,
-3.25931122164331));
#71976=CARTESIAN_POINT('Ctrl Pts',(-0.476944895070687,0.194332029410326,
-3.23546303958507));
#71977=CARTESIAN_POINT('Ctrl Pts',(-0.421534435296339,-0.295895387432433,
-3.21161485752684));
#71978=CARTESIAN_POINT('Ctrl Pts',(0.0206934953975774,-0.514603724025353,
-3.1877666754686));
#71979=CARTESIAN_POINT('Ctrl Pts',(0.443929824061649,-0.261094857231714,
-3.16391849341037));
#71980=CARTESIAN_POINT('Ctrl Pts',(0.459804460733734,0.232001454984632,
-3.14007031135213));
#71981=CARTESIAN_POINT('Ctrl Pts',(0.0537482779932776,0.512206863248803,
-3.1162221292939));
#71982=CARTESIAN_POINT('Ctrl Pts',(-0.401628532381758,0.322395944582544,
-3.09237394723566));
#71983=CARTESIAN_POINT('Ctrl Pts',(-0.488459378881163,-0.163254854637313,
-3.06852576517743));
#71984=CARTESIAN_POINT('Ctrl Pts',(-0.127065425715578,-0.499098260433244,
-3.04467758311919));
#71985=CARTESIAN_POINT('Ctrl Pts',(0.350927447920041,-0.376954383563904,
-3.02082940106096));
#71986=CARTESIAN_POINT('Ctrl Pts',(0.506898997405238,0.0910939093821704,
-2.99698121900272));
#71987=CARTESIAN_POINT('Ctrl Pts',(0.197725097818228,0.475551759938628,
-2.97313303694449));
#71988=CARTESIAN_POINT('Ctrl Pts',(-0.29288716179633,0.423629318448265,
-2.94928485488626));
#71989=CARTESIAN_POINT('Ctrl Pts',(-0.514737547902153,-0.0170278477871493,
-2.92543667282802));
#71990=CARTESIAN_POINT('Ctrl Pts',(-0.264249612685154,-0.442059761170484,
-2.90158849076979));
#71991=CARTESIAN_POINT('Ctrl Pts',(0.228721541200349,-0.461444630120445,
-2.87774030871155));
#71992=CARTESIAN_POINT('Ctrl Pts',(0.511811079662378,-0.0573943295457097,
-2.85389212665332));
#71993=CARTESIAN_POINT('Ctrl Pts',(0.325247711908225,0.399322696740629,
-2.83004394459509));
#71994=CARTESIAN_POINT('Ctrl Pts',(-0.159772526042282,0.489609466964142,
-2.80619576253684));
#71995=CARTESIAN_POINT('Ctrl Pts',(-0.498180793120726,0.130616184367629,
-2.78234758047862));
#71996=CARTESIAN_POINT('Ctrl Pts',(-0.379443706209799,-0.348234352204978,
-2.75849939842038));
#71997=CARTESIAN_POINT('Ctrl Pts',(0.0874820900284247,-0.507534800936275,
-2.73465121636214));
#71998=CARTESIAN_POINT('Ctrl Pts',(0.474131746445591,-0.201106382927444,
-2.71080303430391));
#71999=CARTESIAN_POINT('Ctrl Pts',(0.425704161742498,0.289863169296219,
-2.68695485224568));
#72000=CARTESIAN_POINT('Ctrl Pts',(-0.0133620874435406,0.51484574860689,
-2.66310667018744));
#72001=CARTESIAN_POINT('Ctrl Pts',(-0.440166892034677,0.267390720475778,
-2.63925848812921));
#72002=CARTESIAN_POINT('Ctrl Pts',(-0.463061605280014,-0.225429900313069,
-2.61541030607097));
#72003=CARTESIAN_POINT('Ctrl Pts',(-0.0610373646661749,-0.511389411656436,
-2.59156212401274));
#72004=CARTESIAN_POINT('Ctrl Pts',(0.396996557693393,-0.328082952040145,
-2.5677139419545));
#72005=CARTESIAN_POINT('Ctrl Pts',(0.490734757718168,0.156282077689729,
-2.54386575989627));
#72006=CARTESIAN_POINT('Ctrl Pts',(0.13416030496745,0.497238074578745,-2.52001757783803));
#72007=CARTESIAN_POINT('Ctrl Pts',(-0.345523591076013,0.381913783791161,
-2.4961693957798));
#72008=CARTESIAN_POINT('Ctrl Pts',(-0.508144873463445,-0.0838658322116802,
-2.47232121372156));
#72009=CARTESIAN_POINT('Ctrl Pts',(-0.204477468602375,-0.472687692957734,
-2.44847303166333));
#72010=CARTESIAN_POINT('Ctrl Pts',(0.286824477874043,-0.427757418558724,
-2.4246248496051));
#72011=CARTESIAN_POINT('Ctrl Pts',(0.514927844097049,0.00969564919462744,
-2.40077666754686));
#72012=CARTESIAN_POINT('Ctrl Pts',(0.270518269639977,0.43825170396786,-2.37692848548863));
#72013=CARTESIAN_POINT('Ctrl Pts',(-0.222126828610562,0.464655100317595,
-2.35308030343039));
#72014=CARTESIAN_POINT('Ctrl Pts',(-0.510941813197769,0.0646773048751767,
-2.32923212137215));
#72015=CARTESIAN_POINT('Ctrl Pts',(-0.330901556340725,-0.394650288548008,
-2.30538393931392));
#72016=CARTESIAN_POINT('Ctrl Pts',(0.15278370486901,-0.491835165239574,
-2.28153575725568));
#72017=CARTESIAN_POINT('Ctrl Pts',(0.4962701430723,-0.137697622836198,-2.25768757519746));
#72018=CARTESIAN_POINT('Ctrl Pts',(0.384364496029135,0.342795309816236,
-2.23383939313921));
#72019=CARTESIAN_POINT('Ctrl Pts',(-0.0802453218871671,0.508729179971981,
-2.20999121108098));
#72020=CARTESIAN_POINT('Ctrl Pts',(-0.471219671348245,0.207838186034692,
-2.18614302902275));
#72021=CARTESIAN_POINT('Ctrl Pts',(-0.429788985487338,-0.283771242717626,
-2.16229484696452));
#72022=CARTESIAN_POINT('Ctrl Pts',(0.0060287193172493,-0.514983829632674,
-2.13844666490628));
#72023=CARTESIAN_POINT('Ctrl Pts',(0.436314293890805,-0.273632101892866,
-2.11459848284804));
#72024=CARTESIAN_POINT('Ctrl Pts',(0.466225034532793,0.218812493735242,
-2.09075030078981));
#72025=CARTESIAN_POINT('Ctrl Pts',(0.0683139655539354,0.510468306900671,
-2.06690211873158));
#72026=CARTESIAN_POINT('Ctrl Pts',(-0.392284008247505,0.333703381932237,
-2.04305393667334));
#72027=CARTESIAN_POINT('Ctrl Pts',(-0.492910633745116,-0.149277584990941,
-2.01920575461511));
#72028=CARTESIAN_POINT('Ctrl Pts',(-0.141227958603144,-0.495277047669815,
-1.99535757255687));
#72029=CARTESIAN_POINT('Ctrl Pts',(0.340049646762177,-0.386795718663819,
-1.97150939049864));
#72030=CARTESIAN_POINT('Ctrl Pts',(0.509287690836003,0.0766207426397812,
-1.9476612084404));
#72031=CARTESIAN_POINT('Ctrl Pts',(0.211188364814669,0.469727756053063,
-1.92381302638217));
#72032=CARTESIAN_POINT('Ctrl Pts',(-0.280703618643906,0.431798759516465,
-1.89996484432393));
#72033=CARTESIAN_POINT('Ctrl Pts',(-0.515013702375239,-0.00236148374735782,
-1.8761166622657));
#72034=CARTESIAN_POINT('Ctrl Pts',(-0.276732059344184,-0.434354760041681,
-1.85226848020746));
#72035=CARTESIAN_POINT('Ctrl Pts',(0.215487063743844,-0.467771328320578,
-1.82842029814923));
#72036=CARTESIAN_POINT('Ctrl Pts',(0.50996891677481,-0.071947162301705,
-1.80457211609099));
#72037=CARTESIAN_POINT('Ctrl Pts',(0.336488286745168,0.389897836776561,
-1.78072393403276));
#72038=CARTESIAN_POINT('Ctrl Pts',(-0.145763895836979,0.493961108702058,
-1.75687575197452));
#72039=CARTESIAN_POINT('Ctrl Pts',(-0.49425883872724,0.144751133258919,
-1.73302756991629));
#72040=CARTESIAN_POINT('Ctrl Pts',(-0.38920732841752,-0.337286741135547,
-1.70917938785805));
#72041=CARTESIAN_POINT('Ctrl Pts',(0.0729922782575974,-0.509820377735635,
-1.68533120579982));
#72042=CARTESIAN_POINT('Ctrl Pts',(0.46821202272131,-0.214527835067992,
-1.66148302374158));
#72043=CARTESIAN_POINT('Ctrl Pts',(0.433786638738412,0.277621761199967,
-1.63763484168335));
#72044=CARTESIAN_POINT('Ctrl Pts',(0.00130587156403045,0.515017460810019,
-1.61378665962512));
#72045=CARTESIAN_POINT('Ctrl Pts',(-0.432373201780706,0.279817984807339,
-1.58993847756689));
#72046=CARTESIAN_POINT('Ctrl Pts',(-0.469293903274499,-0.212150707255774,
-1.56609029550865));
#72047=CARTESIAN_POINT('Ctrl Pts',(-0.0755767108934513,-0.509443668142287,
-1.54224211345042));
#72048=CARTESIAN_POINT('Ctrl Pts',(0.387491895128502,-0.339256129568005,
-1.51839393139218));
#72049=CARTESIAN_POINT('Ctrl Pts',(0.494986536844966,0.142242815572411,
-1.49454574933395));
#72050=CARTESIAN_POINT('Ctrl Pts',(0.148266968157262,0.49321556787392,-1.47069756727571));
#72051=CARTESIAN_POINT('Ctrl Pts',(-0.334506733032362,0.39159920300705,
-1.44684938521747));
#72052=CARTESIAN_POINT('Ctrl Pts',(-0.510327213660431,-0.069360112725696,
-1.42300120315924));
#72053=CARTESIAN_POINT('Ctrl Pts',(-0.217856427463329,-0.466672548209829,
-1.39915302110101));
#72054=CARTESIAN_POINT('Ctrl Pts',(0.274525826654611,-0.435752522355686,
-1.37530483904277));
#72055=CARTESIAN_POINT('Ctrl Pts',(0.514995104746436,-0.004973160659839,
-1.35145665698454));
#72056=CARTESIAN_POINT('Ctrl Pts',(0.282889721807265,0.430369719584858,
-1.3276084749263));
#72057=CARTESIAN_POINT('Ctrl Pts',(-0.208803593444471,0.470792682190809,
-1.30376029286807));
#72058=CARTESIAN_POINT('Ctrl Pts',(-0.508892587636381,0.0792024272891182,
-1.27991211080983));
#72059=CARTESIAN_POINT('Ctrl Pts',(-0.342006770054391,-0.385066305299106,
-1.2560639287516));
#72060=CARTESIAN_POINT('Ctrl Pts',(0.138714522737286,-0.495986866178438,
-1.23221574669336));
#72061=CARTESIAN_POINT('Ctrl Pts',(0.492147288009996,-0.151775285024098,
-1.20836756463513));
#72062=CARTESIAN_POINT('Ctrl Pts',(0.393971221149906,0.331709763415838,
-1.18451938257689));
#72063=CARTESIAN_POINT('Ctrl Pts',(-0.0657244302168194,0.510808172910747,
-1.16067120051866));
#72064=CARTESIAN_POINT('Ctrl Pts',(-0.465109410579282,0.22117397322093,
-1.13682301846043));
#72065=CARTESIAN_POINT('Ctrl Pts',(-0.437696310686108,-0.271415971990429,
-1.11297483640219));
#72066=CARTESIAN_POINT('Ctrl Pts',(-0.00864019758634064,-0.514946635318078,
-1.08912665434395));
#72067=CARTESIAN_POINT('Ctrl Pts',(0.42834441504279,-0.285947114588328,
-1.06527847228572));
#72068=CARTESIAN_POINT('Ctrl Pts',(0.472267589072358,0.205445892028833,
-1.04143029022749));
#72069=CARTESIAN_POINT('Ctrl Pts',(0.0828241276429715,0.508315703200206,
-1.01758210816925));
#72070=CARTESIAN_POINT('Ctrl Pts',(-0.382621190280438,0.344740068730225,
-0.993733926111018));
#72071=CARTESIAN_POINT('Ctrl Pts',(-0.496962045979734,-0.135179196237376,
-0.969885744052783));
#72072=CARTESIAN_POINT('Ctrl Pts',(-0.155275905966547,-0.491054053303712,
-0.946037561994549));
#72073=CARTESIAN_POINT('Ctrl Pts',(0.328895974109219,-0.396323262570435,
-0.922189379936314));
#72074=CARTESIAN_POINT('Ctrl Pts',(0.511263231099079,0.06208541508205,-0.89834119787808));
#72075=CARTESIAN_POINT('Ctrl Pts',(0.224480304121095,0.463522689090198,
-0.874493015819844));
#72076=CARTESIAN_POINT('Ctrl Pts',(-0.268292354895715,0.439617905167857,
-0.850644833761611));
#72077=CARTESIAN_POINT('Ctrl Pts',(-0.514872054982912,0.0123067964025964,
-0.826796651703375));
#72078=CARTESIAN_POINT('Ctrl Pts',(-0.288990008121707,-0.426297390849691,
-0.802948469645141));
#72079=CARTESIAN_POINT('Ctrl Pts',(0.202077773263616,-0.473718549132447,
-0.779100287586905));
#72080=CARTESIAN_POINT('Ctrl Pts',(0.507713044087226,-0.0864416283129147,
-0.755252105528672));
#72081=CARTESIAN_POINT('Ctrl Pts',(0.347455886997024,0.380156674054626,
-0.731403923470436));
#72082=CARTESIAN_POINT('Ctrl Pts',(-0.131637015327978,0.497912026801313,
-0.707555741412202));
#72083=CARTESIAN_POINT('Ctrl Pts',(-0.489935919202359,0.158768653482024,
-0.683707559353968));
#72084=CARTESIAN_POINT('Ctrl Pts',(-0.398655207979661,-0.326065507788752,
-0.659859377295733));
#72085=CARTESIAN_POINT('Ctrl Pts',(0.058443251791071,-0.511692365151006,
-0.636011195237498));
#72086=CARTESIAN_POINT('Ctrl Pts',(0.461912464295652,-0.227775252513281,
-0.612163013179264));
#72087=CARTESIAN_POINT('Ctrl Pts',(0.441517208178881,0.265155133757551,
-0.588314831121029));
#72088=CARTESIAN_POINT('Ctrl Pts',(0.0159727715460726,0.514771367521052,
-0.564466649062794));
#72089=CARTESIAN_POINT('Ctrl Pts',(-0.424228751485667,0.292018248117294,
-0.54061846700456));
#72090=CARTESIAN_POINT('Ctrl Pts',(-0.475145487486649,-0.19869940793854,
-0.516770284946325));
#72091=CARTESIAN_POINT('Ctrl Pts',(-0.0900547483877555,-0.507084640844872,
-0.492922102888091));
#72092=CARTESIAN_POINT('Ctrl Pts',(0.377672886420007,-0.350154087167556,
-0.469073920829856));
#72093=CARTESIAN_POINT('Ctrl Pts',(0.498836751198934,0.128088159659702,
-0.445225738771621));
#72094=CARTESIAN_POINT('Ctrl Pts',(0.162253368266692,0.488792942324132,
-0.421377556713388));
#72095=CARTESIAN_POINT('Ctrl Pts',(-0.323218542137151,0.400966939283472,
-0.397529374655152));
#72096=CARTESIAN_POINT('Ctrl Pts',(-0.512095487745039,-0.0547981253106918,
-0.373681192596918));
#72097=CARTESIAN_POINT('Ctrl Pts',(-0.231058777150018,-0.460278817292692,
-0.349833010538684));
#72098=CARTESIAN_POINT('Ctrl Pts',(0.262004709138057,-0.443394124470668,
-0.325984828480448));
#72099=CARTESIAN_POINT('Ctrl Pts',(0.51464411457751,-0.0196379350999004,
-0.302136646422214));
#72100=CARTESIAN_POINT('Ctrl Pts',(0.295032570499096,0.422138597947673,
-0.278288464363979));
#72101=CARTESIAN_POINT('Ctrl Pts',(-0.195312674437287,0.476548339256938,
-0.254440282305745));
#72102=CARTESIAN_POINT('Ctrl Pts',(-0.506427249105613,0.0936632903118652,
-0.23059210024751));
#72103=CARTESIAN_POINT('Ctrl Pts',(-0.352840820178858,-0.375169925782392,
-0.206743918189276));
#72104=CARTESIAN_POINT('Ctrl Pts',(0.124544876676916,-0.499736225127042,
-0.182895736131041));
#72105=CARTESIAN_POINT('Ctrl Pts',(0.487602020374838,-0.165729772261334,
-0.159047554072806));
#72106=CARTESIAN_POINT('Ctrl Pts',(0.403302791131596,0.320355027474805,
-0.135199372014571));
#72107=CARTESIAN_POINT('Ctrl Pts',(-0.0512355571413682,0.512472946267641,
-0.111351189956337));
#72108=CARTESIAN_POINT('Ctrl Pts',(-0.458457827238502,0.234330047531713,
-0.0875030078981023));
#72109=CARTESIAN_POINT('Ctrl Pts',(-0.445565382605697,-0.258840351121007,
-0.0636548258398675));
#72110=CARTESIAN_POINT('Ctrl Pts',(-0.0226750950642322,-0.514488468547469,
-0.0398066437816332));
#72111=CARTESIAN_POINT('Ctrl Pts',(0.345097043992702,-0.334140713462838,
-0.0199331587331043));
#72112=CARTESIAN_POINT('Ctrl Pts',(0.450242459130713,-0.0526637668195261,
-0.00403437069428129));
#72113=CARTESIAN_POINT('Ctrl Pts',(0.43118641951013,0.0950034040017324,
0.00391502332513044));
#72114=CARTESIAN_POINT('Ctrl Pts',(0.404165866753715,0.162293673923731,
0.00788972033483611));
#72115=CARTESIAN_POINT('Ctrl Pts',(0.236230756092329,-0.331488661006748,
-3.4575));
#72116=CARTESIAN_POINT('Ctrl Pts',(0.291420873096492,-0.292158196341315,
-3.45352530299029));
#72117=CARTESIAN_POINT('Ctrl Pts',(0.380867829859202,-0.185560026793827,
-3.44557590897088));
#72118=CARTESIAN_POINT('Ctrl Pts',(0.440039431000898,0.0889589528409691,
-3.42967712093207));
#72119=CARTESIAN_POINT('Ctrl Pts',(0.241551031548769,0.416306162933455,
-3.40980363588352));
#72120=CARTESIAN_POINT('Ctrl Pts',(-0.22013291818294,0.428338358383622,
-3.3859554538253));
#72121=CARTESIAN_POINT('Ctrl Pts',(-0.478925470210962,0.0467407924160679,
-3.36210727176706));
#72122=CARTESIAN_POINT('Ctrl Pts',(-0.298698418620944,-0.377455746868169,
-3.33825908970883));
#72123=CARTESIAN_POINT('Ctrl Pts',(0.155860105948259,-0.455439012791576,
-3.31441090765059));
#72124=CARTESIAN_POINT('Ctrl Pts',(0.467273406510021,-0.115419330027175,
-3.29056272559236));
#72125=CARTESIAN_POINT('Ctrl Pts',(0.349967170548287,0.330471523578635,
-3.26671454353412));
#72126=CARTESIAN_POINT('Ctrl Pts',(-0.0885127355860925,0.473133346833339,
-3.24286636147589));
#72127=CARTESIAN_POINT('Ctrl Pts',(-0.445753297578119,0.181622958605862,
-3.21901817941765));
#72128=CARTESIAN_POINT('Ctrl Pts',(-0.393966612323683,-0.276544200492206,
-3.19516999735943));
#72129=CARTESIAN_POINT('Ctrl Pts',(0.0193401667723502,-0.480949286387233,
-3.17132181530118));
#72130=CARTESIAN_POINT('Ctrl Pts',(0.414897370773675,-0.244019581286168,
-3.14747363324295));
#72131=CARTESIAN_POINT('Ctrl Pts',(0.429733826132711,0.216828851028994,
-3.12362545118471));
#72132=CARTESIAN_POINT('Ctrl Pts',(0.0502332080755313,0.478709177297012,
-3.09977726912648));
#72133=CARTESIAN_POINT('Ctrl Pts',(-0.375362530474502,0.301311654467299,
-3.07592908706825));
#72134=CARTESIAN_POINT('Ctrl Pts',(-0.456514748599978,-0.15257819205599,
-3.05208090501001));
#72135=CARTESIAN_POINT('Ctrl Pts',(-0.118755506361991,-0.466457860652117,
-3.02823272295178));
#72136=CARTESIAN_POINT('Ctrl Pts',(0.3279772332983,-0.35230204001918,-3.00438454089354));
#72137=CARTESIAN_POINT('Ctrl Pts',(0.473748439217363,0.0851364820465625,
-2.9805363588353));
#72138=CARTESIAN_POINT('Ctrl Pts',(0.184794124598751,0.44445127173508,-2.95668817677707));
#72139=CARTESIAN_POINT('Ctrl Pts',(-0.273732709036882,0.395924492746899,
-2.93283999471884));
#72140=CARTESIAN_POINT('Ctrl Pts',(-0.481074358350462,-0.0159142479146477,
-2.9089918126606));
#72141=CARTESIAN_POINT('Ctrl Pts',(-0.246968019692694,-0.413149607648352,
-2.88514363060237));
#72142=CARTESIAN_POINT('Ctrl Pts',(0.213763439489368,-0.431266730500215,
-2.86129544854413));
#72143=CARTESIAN_POINT('Ctrl Pts',(0.478339277460365,-0.053640812432835,
-2.8374472664859));
#72144=CARTESIAN_POINT('Ctrl Pts',(0.303976919789322,0.373207493590096,
-2.81359908442767));
#72145=CARTESIAN_POINT('Ctrl Pts',(-0.149323603380172,0.457589622365882,
-2.78975090236943));
#72146=CARTESIAN_POINT('Ctrl Pts',(-0.465600394550264,0.122074049854989,
-2.7659027203112));
#72147=CARTESIAN_POINT('Ctrl Pts',(-0.354628564088546,-0.32546026266272,
-2.74205453825296));
#72148=CARTESIAN_POINT('Ctrl Pts',(0.0817608711451184,-0.474342661995509,
-2.71820635619473));
#72149=CARTESIAN_POINT('Ctrl Pts',(0.443124125342135,-0.187954277905899,
-2.69435817413649));
#72150=CARTESIAN_POINT('Ctrl Pts',(0.397863643893962,0.270906481850664,
-2.67050999207826));
#72151=CARTESIAN_POINT('Ctrl Pts',(-0.0124882236963727,0.481175482864919,
-2.64666181002002));
#72152=CARTESIAN_POINT('Ctrl Pts',(-0.411380529778162,0.249903702976424,
-2.62281362796179));
#72153=CARTESIAN_POINT('Ctrl Pts',(-0.432777957513921,-0.210687067784559,
-2.59896544590356));
#72154=CARTESIAN_POINT('Ctrl Pts',(-0.0570455976290363,-0.477945186012748,
-2.57511726384532));
#72155=CARTESIAN_POINT('Ctrl Pts',(0.371033481116859,-0.306626738775311,
-2.55126908178708));
#72156=CARTESIAN_POINT('Ctrl Pts',(0.458641320517021,0.146061425968784,
-2.52742089972885));
#72157=CARTESIAN_POINT('Ctrl Pts',(0.125386389416043,0.46471932861766,-2.50357271767061));
#72158=CARTESIAN_POINT('Ctrl Pts',(-0.322926781909134,0.356937101696446,
-2.47972453561238));
#72159=CARTESIAN_POINT('Ctrl Pts',(-0.474912836545144,-0.078381112050585,
-2.45587635355414));
#72160=CARTESIAN_POINT('Ctrl Pts',(-0.191104898808961,-0.441774511139857,
-2.43202817149591));
#72161=CARTESIAN_POINT('Ctrl Pts',(0.268066517033437,-0.399782620291585,
-2.40817998943768));
#72162=CARTESIAN_POINT('Ctrl Pts',(0.481252209413066,0.00906156590694945,
-2.38433180737944));
#72163=CARTESIAN_POINT('Ctrl Pts',(0.252826714350878,0.409590592607036,
-2.36048362532121));
#72164=CARTESIAN_POINT('Ctrl Pts',(-0.207600012825493,0.434267239976145,
-2.33663544326297));
#72165=CARTESIAN_POINT('Ctrl Pts',(-0.477526859931467,0.0604474903170984,
-2.31278726120474));
#72166=CARTESIAN_POINT('Ctrl Pts',(-0.309261009892451,-0.368840655028625,
-2.2889390791465));
#72167=CARTESIAN_POINT('Ctrl Pts',(0.142791842339502,-0.459669762767722,
-2.26509089708827));
#72168=CARTESIAN_POINT('Ctrl Pts',(0.463814698616821,-0.128692371136095,
-2.24124271503003));
#72169=CARTESIAN_POINT('Ctrl Pts',(0.359227540430107,0.3203769268193,-2.2173945329718));
#72170=CARTESIAN_POINT('Ctrl Pts',(-0.0749973785569536,0.475458930141424,
-2.19354635091357));
#72171=CARTESIAN_POINT('Ctrl Pts',(-0.440402496301018,0.194245829539463,
-2.16969816885533));
#72172=CARTESIAN_POINT('Ctrl Pts',(-0.401681325293022,-0.265212959623932,
-2.1458499867971));
#72173=CARTESIAN_POINT('Ctrl Pts',(0.00563444864094621,-0.481304533564932,
-2.12200180473886));
#72174=CARTESIAN_POINT('Ctrl Pts',(0.407779886717249,-0.255736905882805,
-2.09815362268063));
#72175=CARTESIAN_POINT('Ctrl Pts',(0.435734502464197,0.204502431290978,
-2.07430544062239));
#72176=CARTESIAN_POINT('Ctrl Pts',(0.0638463179520797,0.47708432035187,
-2.05045725856416));
#72177=CARTESIAN_POINT('Ctrl Pts',(-0.366629126489699,0.311879599607034,
-2.02660907650592));
#72178=CARTESIAN_POINT('Ctrl Pts',(-0.460674896982894,-0.139515018300695,
-2.00276089444769));
#72179=CARTESIAN_POINT('Ctrl Pts',(-0.131991827375041,-0.46288655040716,
-1.97891271238946));
#72180=CARTESIAN_POINT('Ctrl Pts',(0.317810826682713,-0.361499764156071,
-1.95506453033122));
#72181=CARTESIAN_POINT('Ctrl Pts',(0.475980915095963,0.0716098422428978,
-1.93121634827299));
#72182=CARTESIAN_POINT('Ctrl Pts',(0.197376910832261,0.439008150393539,
-1.90736816621475));
#72183=CARTESIAN_POINT('Ctrl Pts',(-0.262345954314256,0.403559662623244,
-1.88351998415652));
#72184=CARTESIAN_POINT('Ctrl Pts',(-0.481332452667628,-0.00220704567433563,
-1.85967180209828));
#72185=CARTESIAN_POINT('Ctrl Pts',(-0.258634130007767,-0.405948503922317,
-1.83582362004005));
#72186=CARTESIAN_POINT('Ctrl Pts',(0.20139448024705,-0.437179670579116,
-1.81197543798181));
#72187=CARTESIAN_POINT('Ctrl Pts',(0.476617589713424,-0.0672419081928105,
-1.78812725592358));
#72188=CARTESIAN_POINT('Ctrl Pts',(0.314482375140717,0.364399007637914,
-1.76427907386534));
#72189=CARTESIAN_POINT('Ctrl Pts',(-0.136231120007138,0.461656672196172,
-1.74043089180711));
#72190=CARTESIAN_POINT('Ctrl Pts',(-0.461934931051408,0.135284590830497,
-1.71658270974887));
#72191=CARTESIAN_POINT('Ctrl Pts',(-0.363753657658851,-0.31522861161616,
-1.69273452769064));
#72192=CARTESIAN_POINT('Ctrl Pts',(0.0682186748769831,-0.476478764940969,
-1.6688863456324));
#72193=CARTESIAN_POINT('Ctrl Pts',(0.437591544119186,-0.200497983922606,
-1.64503816357417));
#72194=CARTESIAN_POINT('Ctrl Pts',(0.405417537039194,0.259465646478908,
-1.62118998151593));
#72195=CARTESIAN_POINT('Ctrl Pts',(0.00122046920282805,0.481335965305491,
-1.5973417994577));
#72196=CARTESIAN_POINT('Ctrl Pts',(-0.404096537084426,0.261518239818982,
-1.57349361739947));
#72197=CARTESIAN_POINT('Ctrl Pts',(-0.438602671042135,-0.198276317285618,
-1.54964543534123));
#72198=CARTESIAN_POINT('Ctrl Pts',(-0.0706340888623429,-0.476126691682194,
-1.525797253283));
#72199=CARTESIAN_POINT('Ctrl Pts',(0.362150411553781,-0.317069204517043,
-1.50194907122476));
#72200=CARTESIAN_POINT('Ctrl Pts',(0.462615038625616,0.132940313972334,
-1.47810088916653));
#72201=CARTESIAN_POINT('Ctrl Pts',(0.138570494539446,0.460959888802416,
-1.45425270710829));
#72202=CARTESIAN_POINT('Ctrl Pts',(-0.312630412553551,0.365989106652426,
-1.43040452505006));
#72203=CARTESIAN_POINT('Ctrl Pts',(-0.476952454432448,-0.0648240484118974,
-1.40655634299182));
#72204=CARTESIAN_POINT('Ctrl Pts',(-0.203608890553224,-0.43615274930846,
-1.38270816093359));
#72205=CARTESIAN_POINT('Ctrl Pts',(0.256572182166905,-0.407254854335409,
-1.35885997887535));
#72206=CARTESIAN_POINT('Ctrl Pts',(0.481315071300406,-0.00464792219482722,
-1.33501179681712));
#72207=CARTESIAN_POINT('Ctrl Pts',(0.264389089074653,0.402224080109482,
-1.31116361475888));
#72208=CARTESIAN_POINT('Ctrl Pts',(-0.195148100516391,0.440003431698535,
-1.28731543270065));
#72209=CARTESIAN_POINT('Ctrl Pts',(-0.475611651149676,0.0740226879566094,
-1.26346725064241));
#72210=CARTESIAN_POINT('Ctrl Pts',(-0.31963995656813,-0.35988345225471,
-1.23961906858418));
#72211=CARTESIAN_POINT('Ctrl Pts',(0.129642767060033,-0.463549947676258,
-1.21577088652594));
#72212=CARTESIAN_POINT('Ctrl Pts',(0.459961473100724,-0.141849371886711,
-1.19192270446771));
#72213=CARTESIAN_POINT('Ctrl Pts',(0.368205997786016,0.310016361239286,
-1.16807452240948));
#72214=CARTESIAN_POINT('Ctrl Pts',(-0.0614261349757158,0.477401959551476,
-1.14422634035124));
#72215=CARTESIAN_POINT('Ctrl Pts',(-0.434691838916953,0.206709472982349,
-1.12037815829301));
#72216=CARTESIAN_POINT('Ctrl Pts',(-0.409071521348799,-0.253665708094378,
-1.09652997623477));
#72217=CARTESIAN_POINT('Ctrl Pts',(-0.0080751395090761,-0.481269771711826,
-1.07268179417654));
#72218=CARTESIAN_POINT('Ctrl Pts',(0.400331227942373,-0.26724653220537,
-1.0488336121183));
#72219=CARTESIAN_POINT('Ctrl Pts',(0.441381881521284,0.192009988558863,
-1.02498543006007));
#72220=CARTESIAN_POINT('Ctrl Pts',(0.0774075336531558,0.475072494231541,
-1.00113724800183));
#72221=CARTESIAN_POINT('Ctrl Pts',(-0.357598244689237,0.322194500941308,
-0.9772890659436));
#72222=CARTESIAN_POINT('Ctrl Pts',(-0.464461351942563,-0.126338646475794,
-0.953440883885366));
#72223=CARTESIAN_POINT('Ctrl Pts',(-0.145121056613384,-0.458939734572041,
-0.92959270182713));
#72224=CARTESIAN_POINT('Ctrl Pts',(0.307386590221547,-0.370404218649844,
-0.905744519768897));
#72225=CARTESIAN_POINT('Ctrl Pts',(0.477827257505465,0.0580251068631922,
-0.88189633771066));
#72226=CARTESIAN_POINT('Ctrl Pts',(0.209799573991638,0.433208887021656,
-0.858048155652426));
#72227=CARTESIAN_POINT('Ctrl Pts',(-0.250746371636999,0.410867445963362,
-0.834199973594193));
#72228=CARTESIAN_POINT('Ctrl Pts',(-0.481200068836968,0.0115019473649387,
-0.810351791535957));
#72229=CARTESIAN_POINT('Ctrl Pts',(-0.270090424321002,-0.398418076562146,
-0.786503609477724));
#72230=CARTESIAN_POINT('Ctrl Pts',(0.188862140533343,-0.442737950614639,
-0.762655427419487));
#72231=CARTESIAN_POINT('Ctrl Pts',(0.474509248268113,-0.0807884543198489,
-0.738807245361255));
#72232=CARTESIAN_POINT('Ctrl Pts',(0.324732708102262,0.355294904731216,
-0.714959063303019));
#72233=CARTESIAN_POINT('Ctrl Pts',(-0.123028119751846,0.465349205210794,
-0.691110881244784));
#72234=CARTESIAN_POINT('Ctrl Pts',(-0.457894725037471,0.148385382825327,
-0.66726269918655));
#72235=CARTESIAN_POINT('Ctrl Pts',(-0.372583657756285,-0.304741232845733,
-0.643414517128315));
#72236=CARTESIAN_POINT('Ctrl Pts',(0.0546211364799233,-0.47822832672903,
-0.61956633507008));
#72237=CARTESIAN_POINT('Ctrl Pts',(0.431703968907574,-0.212879036894682,
-0.595718153011845));
#72238=CARTESIAN_POINT('Ctrl Pts',(0.412642536941405,0.247814320823537,
-0.571869970953611));
#72239=CARTESIAN_POINT('Ctrl Pts',(0.0149281723354398,0.481105966208734,
-0.548021788895376));
#72240=CARTESIAN_POINT('Ctrl Pts',(-0.396484723616044,0.272920621221822,
-0.524173606837142));
#72241=CARTESIAN_POINT('Ctrl Pts',(-0.44407156899152,-0.185704716060117,
-0.500325424778908));
#72242=CARTESIAN_POINT('Ctrl Pts',(-0.0841652808768616,-0.473921941809059,
-0.476477242720672));
#72243=CARTESIAN_POINT('Ctrl Pts',(0.352973553690336,-0.327254449368329,
-0.452629060662438));
#72244=CARTESIAN_POINT('Ctrl Pts',(0.466213453793493,0.119711354789871,
-0.428780878604203));
#72245=CARTESIAN_POINT('Ctrl Pts',(0.151642201636973,0.456826497412456,
-0.404932696545969));
#72246=CARTESIAN_POINT('Ctrl Pts',(-0.302080455174332,0.374744204734433,
-0.381084514487734));
#72247=CARTESIAN_POINT('Ctrl Pts',(-0.4786050856114,-0.051214396696121,
-0.3572363324295));
#72248=CARTESIAN_POINT('Ctrl Pts',(-0.215947823141546,-0.43017716036811,
-0.333388150371265));
#72249=CARTESIAN_POINT('Ctrl Pts',(0.244869930019852,-0.41439670526355,
-0.309539968313031));
#72250=CARTESIAN_POINT('Ctrl Pts',(0.480987035447976,-0.0183536387932365,
-0.285691786254796));
#72251=CARTESIAN_POINT('Ctrl Pts',(0.275737810703329,0.394531263495945,
-0.261843604196561));
#72252=CARTESIAN_POINT('Ctrl Pts',(-0.182539470678933,0.445382676016845,
-0.237995422138327));
#72253=CARTESIAN_POINT('Ctrl Pts',(-0.473307542664411,0.0875378286884531,
-0.214147240080092));
#72254=CARTESIAN_POINT('Ctrl Pts',(-0.329765473412989,-0.350634283536789,
-0.190299058021858));
#72255=CARTESIAN_POINT('Ctrl Pts',(0.116399798066751,-0.467054103255692,
-0.166450875963623));
#72256=CARTESIAN_POINT('Ctrl Pts',(0.45571346026384,-0.154891253173831,
-0.142602693905389));
#72257=CARTESIAN_POINT('Ctrl Pts',(0.376927294803572,0.299404210776717,
-0.118754511847154));
#72258=CARTESIAN_POINT('Ctrl Pts',(-0.0478848160134567,0.478957858820396,
-0.094906329788919));
#72259=CARTESIAN_POINT('Ctrl Pts',(-0.428475260777818,0.219005156546266,
-0.0710581477306846));
#72260=CARTESIAN_POINT('Ctrl Pts',(-0.416425965841839,-0.241912517045322,
-0.0472099656724497));
#72261=CARTESIAN_POINT('Ctrl Pts',(-0.0211921723080409,-0.480841568472938,
-0.0233617836142155));
#72262=CARTESIAN_POINT('Ctrl Pts',(0.322528130469684,-0.312288330204457,
-0.00348829856568646));
#72263=CARTESIAN_POINT('Ctrl Pts',(0.420797167432627,-0.0492196225713022,
0.0124104894731365));
#72264=CARTESIAN_POINT('Ctrl Pts',(0.402987368884735,0.08879030062507,0.0203598834925482));
#72265=CARTESIAN_POINT('Ctrl Pts',(0.377733926363309,0.151679871354634,
0.0243345805022539));
#72266=CARTESIAN_POINT('Ctrl Pts',(0.457029747534529,0.183521279061925,
-0.0249999999999995));
#72267=CARTESIAN_POINT('Ctrl Pts',(0.487584520760919,0.107429610755057,
-0.0289746970097051));
#72268=CARTESIAN_POINT('Ctrl Pts',(0.498358781643902,0.0239387777195438,
-0.0329493940194109));
#72269=CARTESIAN_POINT('Ctrl Pts',(0.488883640649376,-0.0575933168811649,
-0.0369240910291166));
#72270=CARTESIAN_POINT('Ctrl Pts',(0.47940849965485,-0.139125411481874,
-0.0408987880388223));
#72271=CARTESIAN_POINT('Ctrl Pts',(0.449683956782815,-0.218698767647778,
-0.0448734850485279));
#72272=CARTESIAN_POINT('Ctrl Pts',(0.402142540760437,-0.285343457672843,
-0.0488481820582336));
#72273=CARTESIAN_POINT('Ctrl Pts',(0.307059708715675,-0.418632837722982,
-0.0567975760776454));
#72274=CARTESIAN_POINT('Ctrl Pts',(0.140709384069528,-0.500207553209759,
-0.0647469700970572));
#72275=CARTESIAN_POINT('Ctrl Pts',(-0.0221663241796822,-0.492813869382451,
-0.072696364116469));
#72276=CARTESIAN_POINT('Ctrl Pts',(-0.185042032428883,-0.485420185555144,
-0.0806457581358803));
#72277=CARTESIAN_POINT('Ctrl Pts',(-0.344443124281146,-0.389058102413761,
-0.0885951521552916));
#72278=CARTESIAN_POINT('Ctrl Pts',(-0.426573460878355,-0.247931086047241,
-0.096544546174703));
#72279=CARTESIAN_POINT('Ctrl Pts',(-0.469867545071818,-0.173537564947853,
-0.100734979919682));
#72280=CARTESIAN_POINT('Ctrl Pts',(-0.491689996710417,-0.0867049756087339,
-0.104925413664661));
#72281=CARTESIAN_POINT('Ctrl Pts',(-0.491761526237315,7.34498668767403E-5,
-0.109115847409639));
#72282=CARTESIAN_POINT('Origin',(0.,0.,-0.0249999999999999));
#72283=CARTESIAN_POINT('',(-0.5175,6.33754718558755E-17,0.));
#72284=CARTESIAN_POINT('Origin',(-0.5175,-6.33754718558755E-17,-0.0249999999999999));
#72285=CARTESIAN_POINT('Origin',(0.,0.,0.));
#72286=CARTESIAN_POINT('Origin',(0.,0.,-0.0249999999999999));
#72287=CARTESIAN_POINT('Origin',(0.,0.,-1.725));
#72288=CARTESIAN_POINT('Origin',(0.77,0.,0.));
#72289=CARTESIAN_POINT('',(-0.77,-9.42978035343462E-17,8.67361737988404E-18));
#72290=CARTESIAN_POINT('Origin',(0.,0.,0.));
#72291=CARTESIAN_POINT('Origin',(0.,0.,0.4));
#72292=CARTESIAN_POINT('',(0.23094010767585,0.4,0.4));
#72293=CARTESIAN_POINT('',(0.461880215351701,0.,0.4));
#72294=CARTESIAN_POINT('',(0.461880215351701,0.,0.4));
#72295=CARTESIAN_POINT('Origin',(0.,0.,0.4));
#72296=CARTESIAN_POINT('Origin',(0.,0.,0.4));
#72297=CARTESIAN_POINT('',(0.23094010767585,-0.4,0.4));
#72298=CARTESIAN_POINT('',(0.23094010767585,-0.4,0.4));
#72299=CARTESIAN_POINT('Origin',(0.,0.,0.4));
#72300=CARTESIAN_POINT('Origin',(0.,0.,0.4));
#72301=CARTESIAN_POINT('',(-0.230940107675851,-0.4,0.4));
#72302=CARTESIAN_POINT('',(-0.230940107675851,-0.4,0.4));
#72303=CARTESIAN_POINT('Origin',(0.,0.,0.4));
#72304=CARTESIAN_POINT('Origin',(0.,0.,0.4));
#72305=CARTESIAN_POINT('',(-0.461880215351701,5.55111512312578E-17,0.4));
#72306=CARTESIAN_POINT('',(-0.461880215351701,5.6564012731995E-17,0.4));
#72307=CARTESIAN_POINT('Origin',(0.,0.,0.4));
#72308=CARTESIAN_POINT('Origin',(0.,0.,0.4));
#72309=CARTESIAN_POINT('',(-0.23094010767585,0.4,0.4));
#72310=CARTESIAN_POINT('',(-0.23094010767585,0.4,0.4));
#72311=CARTESIAN_POINT('Origin',(0.,0.,0.4));
#72312=CARTESIAN_POINT('Origin',(0.,0.,0.4));
#72313=CARTESIAN_POINT('',(0.23094010767585,0.4,0.4));
#72314=CARTESIAN_POINT('Origin',(0.,0.,0.4));
#72315=CARTESIAN_POINT('Origin',(0.,0.,0.26143593539449));
#72316=CARTESIAN_POINT('',(0.,0.,0.12287187078898));
#72317=CARTESIAN_POINT('',(-0.23094010767585,-2.82820063659975E-17,0.26143593539449));
#72318=CARTESIAN_POINT('Origin',(0.23094010767585,0.4,1.));
#72319=CARTESIAN_POINT('',(0.23094010767585,0.4,1.));
#72320=CARTESIAN_POINT('',(0.461880215351701,0.,1.));
#72321=CARTESIAN_POINT('',(0.288675134594813,0.3,1.));
#72322=CARTESIAN_POINT('',(0.23094010767585,0.4,1.));
#72323=CARTESIAN_POINT('',(0.461880215351701,0.,1.));
#72324=CARTESIAN_POINT('Origin',(-0.23094010767585,0.4,1.));
#72325=CARTESIAN_POINT('',(-0.23094010767585,0.4,1.));
#72326=CARTESIAN_POINT('',(-0.115470053837925,0.4,1.));
#72327=CARTESIAN_POINT('',(-0.23094010767585,0.4,1.));
#72328=CARTESIAN_POINT('Origin',(-0.461880215351701,5.55111512312578E-17,
1.));
#72329=CARTESIAN_POINT('',(-0.461880215351701,5.6564012731995E-17,1.));
#72330=CARTESIAN_POINT('',(-0.404145188432738,0.1,1.));
#72331=CARTESIAN_POINT('',(-0.461880215351701,5.6564012731995E-17,1.));
#72332=CARTESIAN_POINT('Origin',(-0.230940107675851,-0.4,1.));
#72333=CARTESIAN_POINT('',(-0.230940107675851,-0.4,1.));
#72334=CARTESIAN_POINT('',(-0.288675134594813,-0.3,1.));
#72335=CARTESIAN_POINT('',(-0.230940107675851,-0.4,1.));
#72336=CARTESIAN_POINT('Origin',(0.23094010767585,-0.4,1.));
#72337=CARTESIAN_POINT('',(0.23094010767585,-0.4,1.));
#72338=CARTESIAN_POINT('',(0.115470053837925,-0.4,1.));
#72339=CARTESIAN_POINT('',(0.23094010767585,-0.4,1.));
#72340=CARTESIAN_POINT('Origin',(0.461880215351701,0.,1.));
#72341=CARTESIAN_POINT('',(0.404145188432738,-0.1,1.));
#72342=CARTESIAN_POINT('Origin',(0.77322407690005,-0.32821414793099,0.95));
#72343=CARTESIAN_POINT('',(0.746549912099409,-0.28751213669055,0.0499999999999999));
#72344=CARTESIAN_POINT('',(0.746549912099409,-0.28751213669055,0.95));
#72345=CARTESIAN_POINT('',(0.746549912099409,-0.28751213669055,0.49));
#72346=CARTESIAN_POINT('',(0.732960244213009,-0.266775711794021,0.0499999999999999));
#72347=CARTESIAN_POINT('',(0.77322407690005,-0.32821414793099,0.0499999999999999));
#72348=CARTESIAN_POINT('',(0.732960244213009,-0.266775711794021,0.95));
#72349=CARTESIAN_POINT('',(0.732960244213009,-0.266775711794021,0.95));
#72350=CARTESIAN_POINT('',(0.77322407690005,-0.32821414793099,0.95));
#72351=CARTESIAN_POINT('Origin',(0.768128119610979,-0.286903189949045,0.95));
#72352=CARTESIAN_POINT('',(0.756699650773902,-0.259625958869015,0.95));
#72353=CARTESIAN_POINT('Origin',(0.,0.,0.95));
#72354=CARTESIAN_POINT('',(0.732960244213009,-0.266775711794021,0.95));
#72355=CARTESIAN_POINT('Origin',(0.732960244213009,-0.266775711794021,0.95));
#72356=CARTESIAN_POINT('',(0.756699650773902,-0.259625958869015,0.0499999999999999));
#72357=CARTESIAN_POINT('',(0.756699650773902,-0.259625958869015,0.49));
#72358=CARTESIAN_POINT('',(0.732960244213009,-0.266775711794021,0.0499999999999999));
#72359=CARTESIAN_POINT('Origin',(0.768128119610979,-0.286903189949045,0.0499999999999999));
#72360=CARTESIAN_POINT('Origin',(0.,0.,0.0499999999999999));
#72361=CARTESIAN_POINT('Origin',(0.614337109360103,-0.572878622452499,0.95));
#72362=CARTESIAN_POINT('',(0.603192501249412,-0.525508141170504,0.0499999999999999));
#72363=CARTESIAN_POINT('',(0.603192501249412,-0.525508141170504,0.95));
#72364=CARTESIAN_POINT('',(0.603192501249412,-0.525508141170504,0.49));
#72365=CARTESIAN_POINT('',(0.597514665632803,-0.501374335555501,0.0499999999999999));
#72366=CARTESIAN_POINT('',(0.614337109360103,-0.572878622452499,0.0499999999999999));
#72367=CARTESIAN_POINT('',(0.597514665632803,-0.501374335555501,0.95));
#72368=CARTESIAN_POINT('',(0.597514665632803,-0.501374335555501,0.95));
#72369=CARTESIAN_POINT('',(0.614337109360103,-0.572878622452499,0.95));
#72370=CARTESIAN_POINT('Origin',(0.634184247036264,-0.537126479004,0.95));
#72371=CARTESIAN_POINT('',(0.622267770320064,-0.502775120725853,0.95));
#72372=CARTESIAN_POINT('Origin',(0.,0.,0.95));
#72373=CARTESIAN_POINT('',(0.597514665632803,-0.501374335555501,0.95));
#72374=CARTESIAN_POINT('Origin',(0.597514665632803,-0.501374335555501,0.95));
#72375=CARTESIAN_POINT('',(0.622267770320064,-0.502775120725853,0.0499999999999999));
#72376=CARTESIAN_POINT('',(0.622267770320064,-0.502775120725853,0.49));
#72377=CARTESIAN_POINT('',(0.597514665632803,-0.501374335555501,0.0499999999999999));
#72378=CARTESIAN_POINT('Origin',(0.634184247036264,-0.537126479004,0.0499999999999999));
#72379=CARTESIAN_POINT('Origin',(0.,0.,0.0499999999999999));
#72380=CARTESIAN_POINT('Origin',(0.381352019781219,-0.748445480318229,0.95));
#72381=CARTESIAN_POINT('',(0.387081172575526,-0.700120108151134,0.0499999999999999));
#72382=CARTESIAN_POINT('',(0.387081172575526,-0.700120108151134,0.95));
#72383=CARTESIAN_POINT('',(0.387081172575525,-0.700120108151135,0.49));
#72384=CARTESIAN_POINT('',(0.39,-0.675499814951862,0.0499999999999999));
#72385=CARTESIAN_POINT('',(0.381352019781219,-0.748445480318229,0.0499999999999999));
#72386=CARTESIAN_POINT('',(0.39,-0.675499814951862,0.95));
#72387=CARTESIAN_POINT('',(0.39,-0.675499814951862,0.95));
#72388=CARTESIAN_POINT('',(0.381352019781219,-0.748445480318229,0.95));
#72389=CARTESIAN_POINT('Origin',(0.419424404596921,-0.711972647635046,0.95));
#72390=CARTESIAN_POINT('',(0.412781213071428,-0.685282182852641,0.95));
#72391=CARTESIAN_POINT('Origin',(0.,0.,0.95));
#72392=CARTESIAN_POINT('',(0.39,-0.675499814951862,0.95));
#72393=CARTESIAN_POINT('Origin',(0.39,-0.675499814951862,0.95));
#72394=CARTESIAN_POINT('',(0.412781213071428,-0.685282182852641,0.0499999999999999));
#72395=CARTESIAN_POINT('',(0.412781213071428,-0.685282182852641,0.49));
#72396=CARTESIAN_POINT('',(0.39,-0.675499814951862,0.0499999999999999));
#72397=CARTESIAN_POINT('Origin',(0.419424404596921,-0.711972647635046,0.0499999999999999));
#72398=CARTESIAN_POINT('Origin',(0.,0.,0.0499999999999999));
#72399=CARTESIAN_POINT('Origin',(0.102370248460324,-0.833738767378711,0.95));
#72400=CARTESIAN_POINT('',(0.124282141779344,-0.790287257416402,0.0499999999999999));
#72401=CARTESIAN_POINT('',(0.124282141779344,-0.790287257416402,0.95));
#72402=CARTESIAN_POINT('',(0.124282141779344,-0.790287257416402,0.49));
#72403=CARTESIAN_POINT('',(0.135445578580205,-0.768150047349522,0.0499999999999999));
#72404=CARTESIAN_POINT('',(0.102370248460324,-0.833738767378711,0.0499999999999999));
#72405=CARTESIAN_POINT('',(0.135445578580205,-0.768150047349522,0.95));
#72406=CARTESIAN_POINT('',(0.135445578580205,-0.768150047349522,0.95));
#72407=CARTESIAN_POINT('',(0.102370248460324,-0.833738767378711,0.95));
#72408=CARTESIAN_POINT('Origin',(0.145664567054585,-0.800944407364116,0.95));
#72409=CARTESIAN_POINT('',(0.15350714952449,-0.785134100039519,0.95));
#72410=CARTESIAN_POINT('Origin',(0.,0.,0.95));
#72411=CARTESIAN_POINT('',(0.135445578580205,-0.768150047349522,0.95));
#72412=CARTESIAN_POINT('Origin',(0.135445578580205,-0.768150047349522,0.95));
#72413=CARTESIAN_POINT('',(0.15350714952449,-0.785134100039519,0.0499999999999999));
#72414=CARTESIAN_POINT('',(0.15350714952449,-0.785134100039519,0.49));
#72415=CARTESIAN_POINT('',(0.135445578580205,-0.768150047349522,0.0499999999999999));
#72416=CARTESIAN_POINT('Origin',(0.145664567054585,-0.800944407364116,0.0499999999999999));
#72417=CARTESIAN_POINT('Origin',(0.,0.,0.0499999999999999));
#72418=CARTESIAN_POINT('Origin',(-0.188958885648847,-0.818470854419598,
0.95));
#72419=CARTESIAN_POINT('',(-0.15350714952449,-0.785134100039519,0.0499999999999999));
#72420=CARTESIAN_POINT('',(-0.15350714952449,-0.785134100039519,0.95));
#72421=CARTESIAN_POINT('',(-0.15350714952449,-0.785134100039519,0.49));
#72422=CARTESIAN_POINT('',(-0.135445578580206,-0.768150047349522,0.0499999999999999));
#72423=CARTESIAN_POINT('',(-0.188958885648847,-0.818470854419598,0.0499999999999999));
#72424=CARTESIAN_POINT('',(-0.135445578580206,-0.768150047349522,0.95));
#72425=CARTESIAN_POINT('',(-0.135445578580206,-0.768150047349522,0.95));
#72426=CARTESIAN_POINT('',(-0.188958885648847,-0.818470854419598,0.95));
#72427=CARTESIAN_POINT('Origin',(-0.145664567054585,-0.800944407364116,
0.95));
#72428=CARTESIAN_POINT('',(-0.124282141779344,-0.790287257416402,0.95));
#72429=CARTESIAN_POINT('Origin',(0.,0.,0.95));
#72430=CARTESIAN_POINT('',(-0.135445578580206,-0.768150047349522,0.95));
#72431=CARTESIAN_POINT('Origin',(-0.135445578580206,-0.768150047349522,
0.95));
#72432=CARTESIAN_POINT('',(-0.124282141779344,-0.790287257416402,0.0499999999999999));
#72433=CARTESIAN_POINT('',(-0.124282141779344,-0.790287257416402,0.49));
#72434=CARTESIAN_POINT('',(-0.135445578580206,-0.768150047349522,0.0499999999999999));
#72435=CARTESIAN_POINT('Origin',(-0.145664567054585,-0.800944407364116,
0.0499999999999999));
#72436=CARTESIAN_POINT('Origin',(0.,0.,0.0499999999999999));
#72437=CARTESIAN_POINT('Origin',(-0.457496789412623,-0.704483277074156,
0.95));
#72438=CARTESIAN_POINT('',(-0.412781213071429,-0.685282182852641,0.0499999999999999));
#72439=CARTESIAN_POINT('',(-0.412781213071429,-0.685282182852641,0.95));
#72440=CARTESIAN_POINT('',(-0.412781213071429,-0.685282182852641,0.49));
#72441=CARTESIAN_POINT('',(-0.39,-0.675499814951862,0.0499999999999999));
#72442=CARTESIAN_POINT('',(-0.457496789412623,-0.704483277074156,0.0499999999999999));
#72443=CARTESIAN_POINT('',(-0.39,-0.675499814951862,0.95));
#72444=CARTESIAN_POINT('',(-0.39,-0.675499814951862,0.95));
#72445=CARTESIAN_POINT('',(-0.457496789412623,-0.704483277074156,0.95));
#72446=CARTESIAN_POINT('Origin',(-0.419424404596921,-0.711972647635045,
0.95));
#72447=CARTESIAN_POINT('',(-0.387081172575526,-0.700120108151134,0.95));
#72448=CARTESIAN_POINT('Origin',(0.,0.,0.95));
#72449=CARTESIAN_POINT('',(-0.39,-0.675499814951862,0.95));
#72450=CARTESIAN_POINT('Origin',(-0.39,-0.675499814951862,0.95));
#72451=CARTESIAN_POINT('',(-0.387081172575526,-0.700120108151134,0.0499999999999999));
#72452=CARTESIAN_POINT('',(-0.387081172575526,-0.700120108151134,0.49));
#72453=CARTESIAN_POINT('',(-0.39,-0.675499814951862,0.0499999999999999));
#72454=CARTESIAN_POINT('Origin',(-0.419424404596921,-0.711972647635045,
0.0499999999999999));
#72455=CARTESIAN_POINT('Origin',(0.,0.,0.0499999999999999));
#72456=CARTESIAN_POINT('Origin',(-0.670853828439726,-0.505524619447721,
0.95));
#72457=CARTESIAN_POINT('',(-0.622267770320064,-0.502775120725853,0.0499999999999999));
#72458=CARTESIAN_POINT('',(-0.622267770320064,-0.502775120725853,0.95));
#72459=CARTESIAN_POINT('',(-0.622267770320064,-0.502775120725853,0.49));
#72460=CARTESIAN_POINT('',(-0.597514665632803,-0.501374335555501,0.0499999999999999));
#72461=CARTESIAN_POINT('',(-0.670853828439726,-0.505524619447721,0.0499999999999999));
#72462=CARTESIAN_POINT('',(-0.597514665632803,-0.501374335555501,0.95));
#72463=CARTESIAN_POINT('',(-0.597514665632803,-0.501374335555501,0.95));
#72464=CARTESIAN_POINT('',(-0.670853828439726,-0.505524619447721,0.95));
#72465=CARTESIAN_POINT('Origin',(-0.634184247036264,-0.537126479004,0.95));
#72466=CARTESIAN_POINT('',(-0.603192501249412,-0.525508141170504,0.95));
#72467=CARTESIAN_POINT('Origin',(0.,0.,0.95));
#72468=CARTESIAN_POINT('',(-0.597514665632803,-0.501374335555501,0.95));
#72469=CARTESIAN_POINT('Origin',(-0.597514665632803,-0.501374335555501,
0.95));
#72470=CARTESIAN_POINT('',(-0.603192501249412,-0.525508141170504,0.0499999999999999));
#72471=CARTESIAN_POINT('',(-0.603192501249412,-0.525508141170504,0.49));
#72472=CARTESIAN_POINT('',(-0.597514665632803,-0.501374335555501,0.0499999999999999));
#72473=CARTESIAN_POINT('Origin',(-0.634184247036264,-0.537126479004,0.0499999999999999));
#72474=CARTESIAN_POINT('Origin',(0.,0.,0.0499999999999999));
#72475=CARTESIAN_POINT('Origin',(-0.80329599500895,-0.245592231967099,0.95));
#72476=CARTESIAN_POINT('',(-0.756699650773902,-0.259625958869015,0.0499999999999999));
#72477=CARTESIAN_POINT('',(-0.756699650773902,-0.259625958869015,0.95));
#72478=CARTESIAN_POINT('',(-0.756699650773902,-0.259625958869015,0.49));
#72479=CARTESIAN_POINT('',(-0.732960244213009,-0.266775711794022,0.0499999999999999));
#72480=CARTESIAN_POINT('',(-0.80329599500895,-0.245592231967099,0.0499999999999999));
#72481=CARTESIAN_POINT('',(-0.732960244213009,-0.266775711794022,0.95));
#72482=CARTESIAN_POINT('',(-0.732960244213009,-0.266775711794022,0.95));
#72483=CARTESIAN_POINT('',(-0.80329599500895,-0.245592231967099,0.95));
#72484=CARTESIAN_POINT('Origin',(-0.768128119610979,-0.286903189949044,
0.95));
#72485=CARTESIAN_POINT('',(-0.746549912099409,-0.287512136690549,0.95));
#72486=CARTESIAN_POINT('Origin',(0.,0.,0.95));
#72487=CARTESIAN_POINT('',(-0.732960244213009,-0.266775711794022,0.95));
#72488=CARTESIAN_POINT('Origin',(-0.732960244213009,-0.266775711794022,
0.95));
#72489=CARTESIAN_POINT('',(-0.746549912099409,-0.287512136690549,0.0499999999999999));
#72490=CARTESIAN_POINT('',(-0.746549912099409,-0.287512136690549,0.49));
#72491=CARTESIAN_POINT('',(-0.732960244213009,-0.266775711794022,0.0499999999999999));
#72492=CARTESIAN_POINT('Origin',(-0.768128119610979,-0.286903189949044,
0.0499999999999999));
#72493=CARTESIAN_POINT('Origin',(0.,0.,0.0499999999999999));
#72494=CARTESIAN_POINT('Origin',(-0.838848809193842,0.0439622032440728,
0.95));
#72495=CARTESIAN_POINT('',(-0.799862385646954,0.0148379252984938,0.0499999999999999));
#72496=CARTESIAN_POINT('',(-0.799862385646954,0.0148379252984938,0.95));
#72497=CARTESIAN_POINT('',(-0.799862385646954,0.0148379252984938,0.49));
#72498=CARTESIAN_POINT('',(-0.78,9.55224503334935E-17,0.0499999999999999));
#72499=CARTESIAN_POINT('',(-0.838848809193842,0.0439622032440728,0.0499999999999999));
#72500=CARTESIAN_POINT('',(-0.78,9.55224503334935E-17,0.95));
#72501=CARTESIAN_POINT('',(-0.78,9.55224503334935E-17,0.95));
#72502=CARTESIAN_POINT('',(-0.838848809193842,0.0439622032440728,0.95));
#72503=CARTESIAN_POINT('Origin',(-0.809424404596921,1.04083408558608E-16,
0.95));
#72504=CARTESIAN_POINT('',(-0.8,-9.79717439317883E-17,0.95));
#72505=CARTESIAN_POINT('Origin',(0.,0.,0.95));
#72506=CARTESIAN_POINT('',(-0.799862385646954,-0.0148379252984938,0.95));
#72507=CARTESIAN_POINT('',(-0.78,9.55224503334935E-17,0.95));
#72508=CARTESIAN_POINT('Origin',(0.,0.,0.95));
#72509=CARTESIAN_POINT('Origin',(-0.78,9.55224503334935E-17,0.95));
#72510=CARTESIAN_POINT('',(-0.799862385646954,-0.0148379252984938,0.0499999999999999));
#72511=CARTESIAN_POINT('',(-0.799862385646954,-0.0148379252984938,0.49));
#72512=CARTESIAN_POINT('',(-0.78,9.55224503334935E-17,0.0499999999999999));
#72513=CARTESIAN_POINT('Origin',(-0.809424404596921,1.04083408558608E-16,
0.0499999999999999));
#72514=CARTESIAN_POINT('',(-0.8,-9.79717439317883E-17,0.0499999999999999));
#72515=CARTESIAN_POINT('Origin',(0.,0.,0.0499999999999999));
#72516=CARTESIAN_POINT('Origin',(0.,0.,0.0499999999999999));
#72517=CARTESIAN_POINT('Origin',(-0.818470854419598,0.188958885648847,0.95));
#72518=CARTESIAN_POINT('',(-0.785134100039519,0.15350714952449,0.0499999999999999));
#72519=CARTESIAN_POINT('',(-0.785134100039519,0.15350714952449,0.95));
#72520=CARTESIAN_POINT('',(-0.785134100039519,0.15350714952449,0.49));
#72521=CARTESIAN_POINT('',(-0.768150047349522,0.135445578580206,0.0499999999999999));
#72522=CARTESIAN_POINT('',(-0.818470854419598,0.188958885648847,0.0499999999999999));
#72523=CARTESIAN_POINT('',(-0.768150047349522,0.135445578580206,0.95));
#72524=CARTESIAN_POINT('',(-0.768150047349522,0.135445578580206,0.95));
#72525=CARTESIAN_POINT('',(-0.818470854419598,0.188958885648847,0.95));
#72526=CARTESIAN_POINT('Origin',(-0.800944407364116,0.145664567054585,0.95));
#72527=CARTESIAN_POINT('',(-0.790287257416402,0.124282141779344,0.95));
#72528=CARTESIAN_POINT('Origin',(0.,0.,0.95));
#72529=CARTESIAN_POINT('',(-0.768150047349522,0.135445578580206,0.95));
#72530=CARTESIAN_POINT('Origin',(-0.768150047349522,0.135445578580206,0.95));
#72531=CARTESIAN_POINT('',(-0.790287257416402,0.124282141779344,0.0499999999999999));
#72532=CARTESIAN_POINT('',(-0.790287257416402,0.124282141779344,0.49));
#72533=CARTESIAN_POINT('',(-0.768150047349522,0.135445578580206,0.0499999999999999));
#72534=CARTESIAN_POINT('Origin',(-0.800944407364116,0.145664567054585,0.0499999999999999));
#72535=CARTESIAN_POINT('Origin',(0.,0.,0.0499999999999999));
#72536=CARTESIAN_POINT('Origin',(-0.704483277074156,0.457496789412623,0.95));
#72537=CARTESIAN_POINT('',(-0.685282182852641,0.412781213071428,0.0499999999999999));
#72538=CARTESIAN_POINT('',(-0.685282182852641,0.412781213071428,0.95));
#72539=CARTESIAN_POINT('',(-0.685282182852641,0.412781213071428,0.49));
#72540=CARTESIAN_POINT('',(-0.675499814951862,0.39,0.0499999999999999));
#72541=CARTESIAN_POINT('',(-0.704483277074156,0.457496789412623,0.0499999999999999));
#72542=CARTESIAN_POINT('',(-0.675499814951862,0.39,0.95));
#72543=CARTESIAN_POINT('',(-0.675499814951862,0.39,0.95));
#72544=CARTESIAN_POINT('',(-0.704483277074156,0.457496789412623,0.95));
#72545=CARTESIAN_POINT('Origin',(-0.711972647635046,0.419424404596921,0.95));
#72546=CARTESIAN_POINT('',(-0.700120108151135,0.387081172575525,0.95));
#72547=CARTESIAN_POINT('Origin',(0.,0.,0.95));
#72548=CARTESIAN_POINT('',(-0.675499814951862,0.39,0.95));
#72549=CARTESIAN_POINT('Origin',(-0.675499814951862,0.39,0.95));
#72550=CARTESIAN_POINT('',(-0.700120108151135,0.387081172575525,0.0499999999999999));
#72551=CARTESIAN_POINT('',(-0.700120108151135,0.387081172575525,0.49));
#72552=CARTESIAN_POINT('',(-0.675499814951862,0.39,0.0499999999999999));
#72553=CARTESIAN_POINT('Origin',(-0.711972647635046,0.419424404596921,0.0499999999999999));
#72554=CARTESIAN_POINT('Origin',(0.,0.,0.0499999999999999));
#72555=CARTESIAN_POINT('Origin',(-0.505524619447721,0.670853828439726,0.95));
#72556=CARTESIAN_POINT('',(-0.502775120725853,0.622267770320064,0.0499999999999999));
#72557=CARTESIAN_POINT('',(-0.502775120725853,0.622267770320064,0.95));
#72558=CARTESIAN_POINT('',(-0.502775120725853,0.622267770320064,0.49));
#72559=CARTESIAN_POINT('',(-0.501374335555501,0.597514665632803,0.0499999999999999));
#72560=CARTESIAN_POINT('',(-0.505524619447721,0.670853828439726,0.0499999999999999));
#72561=CARTESIAN_POINT('',(-0.501374335555501,0.597514665632803,0.95));
#72562=CARTESIAN_POINT('',(-0.501374335555501,0.597514665632803,0.95));
#72563=CARTESIAN_POINT('',(-0.505524619447721,0.670853828439726,0.95));
#72564=CARTESIAN_POINT('Origin',(-0.537126479004,0.634184247036264,0.95));
#72565=CARTESIAN_POINT('',(-0.525508141170504,0.603192501249412,0.95));
#72566=CARTESIAN_POINT('Origin',(0.,0.,0.95));
#72567=CARTESIAN_POINT('',(-0.501374335555501,0.597514665632803,0.95));
#72568=CARTESIAN_POINT('Origin',(-0.501374335555501,0.597514665632803,0.95));
#72569=CARTESIAN_POINT('',(-0.525508141170504,0.603192501249412,0.0499999999999999));
#72570=CARTESIAN_POINT('',(-0.525508141170504,0.603192501249412,0.49));
#72571=CARTESIAN_POINT('',(-0.501374335555501,0.597514665632803,0.0499999999999999));
#72572=CARTESIAN_POINT('Origin',(-0.537126479004,0.634184247036264,0.0499999999999999));
#72573=CARTESIAN_POINT('Origin',(0.,0.,0.0499999999999999));
#72574=CARTESIAN_POINT('Origin',(-0.245592231967099,0.80329599500895,0.95));
#72575=CARTESIAN_POINT('',(-0.259625958869015,0.756699650773901,0.0499999999999999));
#72576=CARTESIAN_POINT('',(-0.259625958869015,0.756699650773901,0.95));
#72577=CARTESIAN_POINT('',(-0.259625958869015,0.756699650773901,0.49));
#72578=CARTESIAN_POINT('',(-0.266775711794022,0.732960244213009,0.0499999999999999));
#72579=CARTESIAN_POINT('',(-0.245592231967099,0.80329599500895,0.0499999999999999));
#72580=CARTESIAN_POINT('',(-0.266775711794022,0.732960244213009,0.95));
#72581=CARTESIAN_POINT('',(-0.266775711794022,0.732960244213009,0.95));
#72582=CARTESIAN_POINT('',(-0.245592231967099,0.80329599500895,0.95));
#72583=CARTESIAN_POINT('Origin',(-0.286903189949044,0.768128119610979,0.95));
#72584=CARTESIAN_POINT('',(-0.28751213669055,0.746549912099409,0.95));
#72585=CARTESIAN_POINT('Origin',(0.,0.,0.95));
#72586=CARTESIAN_POINT('',(-0.266775711794022,0.732960244213009,0.95));
#72587=CARTESIAN_POINT('Origin',(-0.266775711794022,0.732960244213009,0.95));
#72588=CARTESIAN_POINT('',(-0.28751213669055,0.746549912099409,0.0499999999999999));
#72589=CARTESIAN_POINT('',(-0.28751213669055,0.746549912099409,0.49));
#72590=CARTESIAN_POINT('',(-0.266775711794022,0.732960244213009,0.0499999999999999));
#72591=CARTESIAN_POINT('Origin',(-0.286903189949044,0.768128119610979,0.0499999999999999));
#72592=CARTESIAN_POINT('Origin',(0.,0.,0.0499999999999999));
#72593=CARTESIAN_POINT('Origin',(0.0439622032440729,0.838848809193842,0.95));
#72594=CARTESIAN_POINT('',(0.0148379252984938,0.799862385646954,0.0499999999999999));
#72595=CARTESIAN_POINT('',(0.0148379252984938,0.799862385646954,0.95));
#72596=CARTESIAN_POINT('',(0.0148379252984938,0.799862385646954,0.49));
#72597=CARTESIAN_POINT('',(4.77612251667468E-17,0.78,0.0499999999999999));
#72598=CARTESIAN_POINT('',(0.0439622032440729,0.838848809193842,0.0499999999999999));
#72599=CARTESIAN_POINT('',(4.77612251667468E-17,0.78,0.95));
#72600=CARTESIAN_POINT('',(4.77612251667468E-17,0.78,0.95));
#72601=CARTESIAN_POINT('',(0.0439622032440729,0.838848809193842,0.95));
#72602=CARTESIAN_POINT('Origin',(4.85722573273506E-17,0.809424404596921,
0.95));
#72603=CARTESIAN_POINT('',(-0.0148379252984937,0.799862385646954,0.95));
#72604=CARTESIAN_POINT('Origin',(0.,0.,0.95));
#72605=CARTESIAN_POINT('',(4.77612251667468E-17,0.78,0.95));
#72606=CARTESIAN_POINT('Origin',(4.77612251667468E-17,0.78,0.95));
#72607=CARTESIAN_POINT('',(-0.0148379252984937,0.799862385646954,0.0499999999999999));
#72608=CARTESIAN_POINT('',(-0.0148379252984937,0.799862385646954,0.49));
#72609=CARTESIAN_POINT('',(4.77612251667468E-17,0.78,0.0499999999999999));
#72610=CARTESIAN_POINT('Origin',(4.85722573273506E-17,0.809424404596921,
0.0499999999999999));
#72611=CARTESIAN_POINT('Origin',(0.,0.,0.0499999999999999));
#72612=CARTESIAN_POINT('Origin',(0.32821414793099,0.77322407690005,0.95));
#72613=CARTESIAN_POINT('',(0.28751213669055,0.746549912099409,0.0499999999999999));
#72614=CARTESIAN_POINT('',(0.28751213669055,0.746549912099409,0.95));
#72615=CARTESIAN_POINT('',(0.28751213669055,0.746549912099409,0.49));
#72616=CARTESIAN_POINT('',(0.266775711794022,0.732960244213009,0.0499999999999999));
#72617=CARTESIAN_POINT('',(0.32821414793099,0.77322407690005,0.0499999999999999));
#72618=CARTESIAN_POINT('',(0.266775711794022,0.732960244213009,0.95));
#72619=CARTESIAN_POINT('',(0.266775711794022,0.732960244213009,0.95));
#72620=CARTESIAN_POINT('',(0.32821414793099,0.77322407690005,0.95));
#72621=CARTESIAN_POINT('Origin',(0.286903189949044,0.768128119610979,0.95));
#72622=CARTESIAN_POINT('',(0.259625958869015,0.756699650773901,0.95));
#72623=CARTESIAN_POINT('Origin',(0.,0.,0.95));
#72624=CARTESIAN_POINT('',(0.266775711794022,0.732960244213009,0.95));
#72625=CARTESIAN_POINT('Origin',(0.266775711794022,0.732960244213009,0.95));
#72626=CARTESIAN_POINT('',(0.259625958869015,0.756699650773901,0.0499999999999999));
#72627=CARTESIAN_POINT('',(0.259625958869015,0.756699650773901,0.49));
#72628=CARTESIAN_POINT('',(0.266775711794022,0.732960244213009,0.0499999999999999));
#72629=CARTESIAN_POINT('Origin',(0.286903189949044,0.768128119610979,0.0499999999999999));
#72630=CARTESIAN_POINT('Origin',(0.,0.,0.0499999999999999));
#72631=CARTESIAN_POINT('Origin',(0.572878622452499,0.614337109360103,0.95));
#72632=CARTESIAN_POINT('',(0.525508141170504,0.603192501249412,0.0499999999999999));
#72633=CARTESIAN_POINT('',(0.525508141170504,0.603192501249412,0.95));
#72634=CARTESIAN_POINT('',(0.525508141170504,0.603192501249412,0.49));
#72635=CARTESIAN_POINT('',(0.501374335555501,0.597514665632803,0.0499999999999999));
#72636=CARTESIAN_POINT('',(0.572878622452499,0.614337109360103,0.0499999999999999));
#72637=CARTESIAN_POINT('',(0.501374335555501,0.597514665632803,0.95));
#72638=CARTESIAN_POINT('',(0.501374335555501,0.597514665632803,0.95));
#72639=CARTESIAN_POINT('',(0.572878622452499,0.614337109360103,0.95));
#72640=CARTESIAN_POINT('Origin',(0.537126479004,0.634184247036264,0.95));
#72641=CARTESIAN_POINT('',(0.502775120725853,0.622267770320064,0.95));
#72642=CARTESIAN_POINT('Origin',(0.,0.,0.95));
#72643=CARTESIAN_POINT('',(0.501374335555501,0.597514665632803,0.95));
#72644=CARTESIAN_POINT('Origin',(0.501374335555501,0.597514665632803,0.95));
#72645=CARTESIAN_POINT('',(0.502775120725853,0.622267770320064,0.0499999999999999));
#72646=CARTESIAN_POINT('',(0.502775120725853,0.622267770320064,0.49));
#72647=CARTESIAN_POINT('',(0.501374335555501,0.597514665632803,0.0499999999999999));
#72648=CARTESIAN_POINT('Origin',(0.537126479004,0.634184247036264,0.0499999999999999));
#72649=CARTESIAN_POINT('Origin',(0.,0.,0.0499999999999999));
#72650=CARTESIAN_POINT('Origin',(0.748445480318229,0.381352019781219,0.95));
#72651=CARTESIAN_POINT('',(0.700120108151135,0.387081172575526,0.0499999999999999));
#72652=CARTESIAN_POINT('',(0.700120108151135,0.387081172575526,0.95));
#72653=CARTESIAN_POINT('',(0.700120108151135,0.387081172575526,0.49));
#72654=CARTESIAN_POINT('',(0.675499814951862,0.39,0.0499999999999999));
#72655=CARTESIAN_POINT('',(0.748445480318229,0.381352019781219,0.0499999999999999));
#72656=CARTESIAN_POINT('',(0.675499814951862,0.39,0.95));
#72657=CARTESIAN_POINT('',(0.675499814951862,0.39,0.95));
#72658=CARTESIAN_POINT('',(0.748445480318229,0.381352019781219,0.95));
#72659=CARTESIAN_POINT('Origin',(0.711972647635046,0.419424404596921,0.95));
#72660=CARTESIAN_POINT('',(0.685282182852641,0.412781213071428,0.95));
#72661=CARTESIAN_POINT('Origin',(0.,0.,0.95));
#72662=CARTESIAN_POINT('',(0.675499814951862,0.39,0.95));
#72663=CARTESIAN_POINT('Origin',(0.675499814951862,0.39,0.95));
#72664=CARTESIAN_POINT('',(0.685282182852641,0.412781213071428,0.0499999999999999));
#72665=CARTESIAN_POINT('',(0.685282182852641,0.412781213071428,0.49));
#72666=CARTESIAN_POINT('',(0.675499814951862,0.39,0.0499999999999999));
#72667=CARTESIAN_POINT('Origin',(0.711972647635046,0.419424404596921,0.0499999999999999));
#72668=CARTESIAN_POINT('Origin',(0.,0.,0.0499999999999999));
#72669=CARTESIAN_POINT('Origin',(0.833738767378711,0.102370248460324,0.95));
#72670=CARTESIAN_POINT('',(0.790287257416402,0.124282141779344,0.0499999999999999));
#72671=CARTESIAN_POINT('',(0.790287257416402,0.124282141779344,0.95));
#72672=CARTESIAN_POINT('',(0.790287257416402,0.124282141779344,0.49));
#72673=CARTESIAN_POINT('',(0.768150047349522,0.135445578580206,0.0499999999999999));
#72674=CARTESIAN_POINT('',(0.833738767378711,0.102370248460324,0.0499999999999999));
#72675=CARTESIAN_POINT('',(0.768150047349522,0.135445578580206,0.95));
#72676=CARTESIAN_POINT('',(0.768150047349522,0.135445578580206,0.95));
#72677=CARTESIAN_POINT('',(0.833738767378711,0.102370248460324,0.95));
#72678=CARTESIAN_POINT('Origin',(0.800944407364116,0.145664567054585,0.95));
#72679=CARTESIAN_POINT('',(0.785134100039519,0.15350714952449,0.95));
#72680=CARTESIAN_POINT('Origin',(0.,0.,0.95));
#72681=CARTESIAN_POINT('',(0.768150047349522,0.135445578580206,0.95));
#72682=CARTESIAN_POINT('Origin',(0.768150047349522,0.135445578580206,0.95));
#72683=CARTESIAN_POINT('',(0.785134100039519,0.15350714952449,0.0499999999999999));
#72684=CARTESIAN_POINT('',(0.785134100039519,0.15350714952449,0.49));
#72685=CARTESIAN_POINT('',(0.768150047349522,0.135445578580206,0.0499999999999999));
#72686=CARTESIAN_POINT('Origin',(0.800944407364116,0.145664567054585,0.0499999999999999));
#72687=CARTESIAN_POINT('Origin',(0.,0.,0.0499999999999999));
#72688=CARTESIAN_POINT('Origin',(0.80329599500895,0.245592231967099,0.95));
#72689=CARTESIAN_POINT('',(0.756699650773901,0.259625958869015,0.0499999999999999));
#72690=CARTESIAN_POINT('',(0.756699650773901,0.259625958869015,0.95));
#72691=CARTESIAN_POINT('',(0.756699650773902,0.259625958869015,0.49));
#72692=CARTESIAN_POINT('',(0.732960244213009,0.266775711794022,0.0499999999999999));
#72693=CARTESIAN_POINT('',(0.80329599500895,0.245592231967099,0.0499999999999999));
#72694=CARTESIAN_POINT('',(0.732960244213009,0.266775711794022,0.95));
#72695=CARTESIAN_POINT('',(0.732960244213009,0.266775711794022,0.95));
#72696=CARTESIAN_POINT('',(0.80329599500895,0.245592231967099,0.95));
#72697=CARTESIAN_POINT('Origin',(0.768128119610979,0.286903189949044,0.95));
#72698=CARTESIAN_POINT('',(0.746549912099409,0.28751213669055,0.95));
#72699=CARTESIAN_POINT('Origin',(0.,0.,0.95));
#72700=CARTESIAN_POINT('',(0.732960244213009,0.266775711794022,0.95));
#72701=CARTESIAN_POINT('Origin',(0.732960244213009,0.266775711794022,0.95));
#72702=CARTESIAN_POINT('',(0.746549912099409,0.28751213669055,0.0499999999999999));
#72703=CARTESIAN_POINT('',(0.746549912099409,0.28751213669055,0.49));
#72704=CARTESIAN_POINT('',(0.732960244213009,0.266775711794022,0.0499999999999999));
#72705=CARTESIAN_POINT('Origin',(0.768128119610979,0.286903189949044,0.0499999999999999));
#72706=CARTESIAN_POINT('Origin',(0.,0.,0.0499999999999999));
#72707=CARTESIAN_POINT('Origin',(0.670853828439726,0.505524619447721,0.95));
#72708=CARTESIAN_POINT('',(0.622267770320064,0.502775120725853,0.0499999999999999));
#72709=CARTESIAN_POINT('',(0.622267770320064,0.502775120725853,0.95));
#72710=CARTESIAN_POINT('',(0.622267770320064,0.502775120725853,0.49));
#72711=CARTESIAN_POINT('',(0.597514665632803,0.501374335555501,0.0499999999999999));
#72712=CARTESIAN_POINT('',(0.670853828439726,0.505524619447721,0.0499999999999999));
#72713=CARTESIAN_POINT('',(0.597514665632803,0.501374335555501,0.95));
#72714=CARTESIAN_POINT('',(0.597514665632803,0.501374335555501,0.95));
#72715=CARTESIAN_POINT('',(0.670853828439726,0.505524619447721,0.95));
#72716=CARTESIAN_POINT('Origin',(0.634184247036264,0.537126479004,0.95));
#72717=CARTESIAN_POINT('',(0.603192501249412,0.525508141170504,0.95));
#72718=CARTESIAN_POINT('Origin',(0.,0.,0.95));
#72719=CARTESIAN_POINT('',(0.597514665632803,0.501374335555501,0.95));
#72720=CARTESIAN_POINT('Origin',(0.597514665632803,0.501374335555501,0.95));
#72721=CARTESIAN_POINT('',(0.603192501249412,0.525508141170504,0.0499999999999999));
#72722=CARTESIAN_POINT('',(0.603192501249412,0.525508141170504,0.49));
#72723=CARTESIAN_POINT('',(0.597514665632803,0.501374335555501,0.0499999999999999));
#72724=CARTESIAN_POINT('Origin',(0.634184247036264,0.537126479004,0.0499999999999999));
#72725=CARTESIAN_POINT('Origin',(0.,0.,0.0499999999999999));
#72726=CARTESIAN_POINT('Origin',(0.457496789412623,0.704483277074156,0.95));
#72727=CARTESIAN_POINT('',(0.412781213071428,0.685282182852641,0.0499999999999999));
#72728=CARTESIAN_POINT('',(0.412781213071428,0.685282182852641,0.95));
#72729=CARTESIAN_POINT('',(0.412781213071428,0.685282182852641,0.49));
#72730=CARTESIAN_POINT('',(0.39,0.675499814951862,0.0499999999999999));
#72731=CARTESIAN_POINT('',(0.457496789412623,0.704483277074156,0.0499999999999999));
#72732=CARTESIAN_POINT('',(0.39,0.675499814951862,0.95));
#72733=CARTESIAN_POINT('',(0.39,0.675499814951862,0.95));
#72734=CARTESIAN_POINT('',(0.457496789412623,0.704483277074156,0.95));
#72735=CARTESIAN_POINT('Origin',(0.419424404596921,0.711972647635046,0.95));
#72736=CARTESIAN_POINT('',(0.387081172575526,0.700120108151134,0.95));
#72737=CARTESIAN_POINT('Origin',(0.,0.,0.95));
#72738=CARTESIAN_POINT('',(0.39,0.675499814951862,0.95));
#72739=CARTESIAN_POINT('Origin',(0.39,0.675499814951862,0.95));
#72740=CARTESIAN_POINT('',(0.387081172575526,0.700120108151134,0.0499999999999999));
#72741=CARTESIAN_POINT('',(0.387081172575526,0.700120108151134,0.49));
#72742=CARTESIAN_POINT('',(0.39,0.675499814951862,0.0499999999999999));
#72743=CARTESIAN_POINT('Origin',(0.419424404596921,0.711972647635046,0.0499999999999999));
#72744=CARTESIAN_POINT('Origin',(0.,0.,0.0499999999999999));
#72745=CARTESIAN_POINT('Origin',(0.188958885648847,0.818470854419598,0.95));
#72746=CARTESIAN_POINT('',(0.15350714952449,0.785134100039519,0.0499999999999999));
#72747=CARTESIAN_POINT('',(0.15350714952449,0.785134100039519,0.95));
#72748=CARTESIAN_POINT('',(0.15350714952449,0.785134100039519,0.49));
#72749=CARTESIAN_POINT('',(0.135445578580206,0.768150047349522,0.0499999999999999));
#72750=CARTESIAN_POINT('',(0.188958885648847,0.818470854419598,0.0499999999999999));
#72751=CARTESIAN_POINT('',(0.135445578580206,0.768150047349522,0.95));
#72752=CARTESIAN_POINT('',(0.135445578580206,0.768150047349522,0.95));
#72753=CARTESIAN_POINT('',(0.188958885648847,0.818470854419598,0.95));
#72754=CARTESIAN_POINT('Origin',(0.145664567054585,0.800944407364116,0.95));
#72755=CARTESIAN_POINT('',(0.124282141779344,0.790287257416402,0.95));
#72756=CARTESIAN_POINT('Origin',(0.,0.,0.95));
#72757=CARTESIAN_POINT('',(0.135445578580206,0.768150047349522,0.95));
#72758=CARTESIAN_POINT('Origin',(0.135445578580206,0.768150047349522,0.95));
#72759=CARTESIAN_POINT('',(0.124282141779344,0.790287257416402,0.0499999999999999));
#72760=CARTESIAN_POINT('',(0.124282141779344,0.790287257416402,0.49));
#72761=CARTESIAN_POINT('',(0.135445578580206,0.768150047349522,0.0499999999999999));
#72762=CARTESIAN_POINT('Origin',(0.145664567054585,0.800944407364116,0.0499999999999999));
#72763=CARTESIAN_POINT('Origin',(0.,0.,0.0499999999999999));
#72764=CARTESIAN_POINT('Origin',(-0.102370248460324,0.833738767378711,0.95));
#72765=CARTESIAN_POINT('',(-0.124282141779344,0.790287257416403,0.0499999999999999));
#72766=CARTESIAN_POINT('',(-0.124282141779344,0.790287257416403,0.95));
#72767=CARTESIAN_POINT('',(-0.124282141779344,0.790287257416403,0.49));
#72768=CARTESIAN_POINT('',(-0.135445578580206,0.768150047349522,0.0499999999999999));
#72769=CARTESIAN_POINT('',(-0.102370248460324,0.833738767378711,0.0499999999999999));
#72770=CARTESIAN_POINT('',(-0.135445578580206,0.768150047349522,0.95));
#72771=CARTESIAN_POINT('',(-0.135445578580206,0.768150047349522,0.95));
#72772=CARTESIAN_POINT('',(-0.102370248460324,0.833738767378711,0.95));
#72773=CARTESIAN_POINT('Origin',(-0.145664567054585,0.800944407364116,0.95));
#72774=CARTESIAN_POINT('',(-0.15350714952449,0.785134100039519,0.95));
#72775=CARTESIAN_POINT('Origin',(0.,0.,0.95));
#72776=CARTESIAN_POINT('',(-0.135445578580206,0.768150047349522,0.95));
#72777=CARTESIAN_POINT('Origin',(-0.135445578580206,0.768150047349522,0.95));
#72778=CARTESIAN_POINT('',(-0.15350714952449,0.785134100039519,0.0499999999999999));
#72779=CARTESIAN_POINT('',(-0.15350714952449,0.785134100039519,0.49));
#72780=CARTESIAN_POINT('',(-0.135445578580206,0.768150047349522,0.0499999999999999));
#72781=CARTESIAN_POINT('Origin',(-0.145664567054585,0.800944407364116,0.0499999999999999));
#72782=CARTESIAN_POINT('Origin',(0.,0.,0.0499999999999999));
#72783=CARTESIAN_POINT('Origin',(-0.381352019781219,0.748445480318229,0.95));
#72784=CARTESIAN_POINT('',(-0.387081172575525,0.700120108151135,0.0499999999999999));
#72785=CARTESIAN_POINT('',(-0.387081172575525,0.700120108151135,0.95));
#72786=CARTESIAN_POINT('',(-0.387081172575525,0.700120108151135,0.49));
#72787=CARTESIAN_POINT('',(-0.39,0.675499814951862,0.0499999999999999));
#72788=CARTESIAN_POINT('',(-0.381352019781219,0.748445480318229,0.0499999999999999));
#72789=CARTESIAN_POINT('',(-0.39,0.675499814951862,0.95));
#72790=CARTESIAN_POINT('',(-0.39,0.675499814951862,0.95));
#72791=CARTESIAN_POINT('',(-0.381352019781219,0.748445480318229,0.95));
#72792=CARTESIAN_POINT('Origin',(-0.419424404596921,0.711972647635046,0.95));
#72793=CARTESIAN_POINT('',(-0.412781213071428,0.685282182852641,0.95));
#72794=CARTESIAN_POINT('Origin',(0.,0.,0.95));
#72795=CARTESIAN_POINT('',(-0.39,0.675499814951862,0.95));
#72796=CARTESIAN_POINT('Origin',(-0.39,0.675499814951862,0.95));
#72797=CARTESIAN_POINT('',(-0.412781213071428,0.685282182852641,0.0499999999999999));
#72798=CARTESIAN_POINT('',(-0.412781213071428,0.685282182852641,0.49));
#72799=CARTESIAN_POINT('',(-0.39,0.675499814951862,0.0499999999999999));
#72800=CARTESIAN_POINT('Origin',(-0.419424404596921,0.711972647635046,0.0499999999999999));
#72801=CARTESIAN_POINT('Origin',(0.,0.,0.0499999999999999));
#72802=CARTESIAN_POINT('Origin',(-0.614337109360103,0.572878622452499,0.95));
#72803=CARTESIAN_POINT('',(-0.603192501249412,0.525508141170504,0.0499999999999999));
#72804=CARTESIAN_POINT('',(-0.603192501249412,0.525508141170504,0.95));
#72805=CARTESIAN_POINT('',(-0.603192501249412,0.525508141170504,0.49));
#72806=CARTESIAN_POINT('',(-0.597514665632803,0.501374335555501,0.0499999999999999));
#72807=CARTESIAN_POINT('',(-0.614337109360103,0.572878622452499,0.0499999999999999));
#72808=CARTESIAN_POINT('',(-0.597514665632803,0.501374335555501,0.95));
#72809=CARTESIAN_POINT('',(-0.597514665632803,0.501374335555501,0.95));
#72810=CARTESIAN_POINT('',(-0.614337109360103,0.572878622452499,0.95));
#72811=CARTESIAN_POINT('Origin',(-0.634184247036264,0.537126479004,0.95));
#72812=CARTESIAN_POINT('',(-0.622267770320064,0.502775120725853,0.95));
#72813=CARTESIAN_POINT('Origin',(0.,0.,0.95));
#72814=CARTESIAN_POINT('',(-0.597514665632803,0.501374335555501,0.95));
#72815=CARTESIAN_POINT('Origin',(-0.597514665632803,0.501374335555501,0.95));
#72816=CARTESIAN_POINT('',(-0.622267770320064,0.502775120725853,0.0499999999999999));
#72817=CARTESIAN_POINT('',(-0.622267770320064,0.502775120725853,0.49));
#72818=CARTESIAN_POINT('',(-0.597514665632803,0.501374335555501,0.0499999999999999));
#72819=CARTESIAN_POINT('Origin',(-0.634184247036264,0.537126479004,0.0499999999999999));
#72820=CARTESIAN_POINT('Origin',(0.,0.,0.0499999999999999));
#72821=CARTESIAN_POINT('Origin',(-0.77322407690005,0.32821414793099,0.95));
#72822=CARTESIAN_POINT('',(-0.746549912099409,0.28751213669055,0.0499999999999999));
#72823=CARTESIAN_POINT('',(-0.746549912099409,0.28751213669055,0.95));
#72824=CARTESIAN_POINT('',(-0.746549912099409,0.28751213669055,0.49));
#72825=CARTESIAN_POINT('',(-0.732960244213009,0.266775711794022,0.0499999999999999));
#72826=CARTESIAN_POINT('',(-0.77322407690005,0.32821414793099,0.0499999999999999));
#72827=CARTESIAN_POINT('',(-0.732960244213009,0.266775711794022,0.95));
#72828=CARTESIAN_POINT('',(-0.732960244213009,0.266775711794022,0.95));
#72829=CARTESIAN_POINT('',(-0.77322407690005,0.32821414793099,0.95));
#72830=CARTESIAN_POINT('Origin',(-0.768128119610979,0.286903189949044,0.95));
#72831=CARTESIAN_POINT('',(-0.756699650773901,0.259625958869015,0.95));
#72832=CARTESIAN_POINT('Origin',(0.,0.,0.95));
#72833=CARTESIAN_POINT('',(-0.732960244213009,0.266775711794022,0.95));
#72834=CARTESIAN_POINT('Origin',(-0.732960244213009,0.266775711794022,0.95));
#72835=CARTESIAN_POINT('',(-0.756699650773901,0.259625958869015,0.0499999999999999));
#72836=CARTESIAN_POINT('',(-0.756699650773901,0.259625958869015,0.49));
#72837=CARTESIAN_POINT('',(-0.732960244213009,0.266775711794022,0.0499999999999999));
#72838=CARTESIAN_POINT('Origin',(-0.768128119610979,0.286903189949044,0.0499999999999999));
#72839=CARTESIAN_POINT('Origin',(0.,0.,0.0499999999999999));
#72840=CARTESIAN_POINT('Origin',(0.809424404596921,0.,0.95));
#72841=CARTESIAN_POINT('',(0.799862385646954,-0.0148379252984939,0.95));
#72842=CARTESIAN_POINT('',(0.799862385646954,0.0148379252984938,0.95));
#72843=CARTESIAN_POINT('Origin',(0.,0.,0.95));
#72844=CARTESIAN_POINT('',(0.78,0.,0.95));
#72845=CARTESIAN_POINT('',(0.838848809193842,-0.0439622032440728,0.95));
#72846=CARTESIAN_POINT('',(0.78,0.,0.95));
#72847=CARTESIAN_POINT('Origin',(0.838848809193842,-0.0439622032440728,
0.95));
#72848=CARTESIAN_POINT('',(0.799862385646954,-0.0148379252984939,0.0499999999999999));
#72849=CARTESIAN_POINT('',(0.799862385646954,-0.0148379252984938,0.49));
#72850=CARTESIAN_POINT('',(0.78,0.,0.0499999999999999));
#72851=CARTESIAN_POINT('',(0.838848809193842,-0.0439622032440728,0.0499999999999999));
#72852=CARTESIAN_POINT('',(0.78,0.,0.95));
#72853=CARTESIAN_POINT('Origin',(0.78,0.,0.95));
#72854=CARTESIAN_POINT('',(0.799862385646954,0.0148379252984938,0.0499999999999999));
#72855=CARTESIAN_POINT('',(0.799862385646954,0.0148379252984938,0.49));
#72856=CARTESIAN_POINT('',(0.78,0.,0.0499999999999999));
#72857=CARTESIAN_POINT('Origin',(0.809424404596921,0.,0.0499999999999999));
#72858=CARTESIAN_POINT('Origin',(0.,0.,0.0499999999999999));
#72859=CARTESIAN_POINT('Origin',(-0.833738767378711,-0.102370248460324,
0.95));
#72860=CARTESIAN_POINT('',(-0.790287257416402,-0.124282141779344,0.0499999999999999));
#72861=CARTESIAN_POINT('',(-0.790287257416402,-0.124282141779344,0.95));
#72862=CARTESIAN_POINT('',(-0.790287257416402,-0.124282141779344,0.49));
#72863=CARTESIAN_POINT('',(-0.768150047349522,-0.135445578580206,0.0499999999999999));
#72864=CARTESIAN_POINT('',(-0.833738767378711,-0.102370248460324,0.0499999999999999));
#72865=CARTESIAN_POINT('',(-0.768150047349522,-0.135445578580206,0.95));
#72866=CARTESIAN_POINT('',(-0.768150047349522,-0.135445578580206,0.95));
#72867=CARTESIAN_POINT('',(-0.833738767378711,-0.102370248460324,0.95));
#72868=CARTESIAN_POINT('Origin',(-0.800944407364116,-0.145664567054585,
0.95));
#72869=CARTESIAN_POINT('',(-0.785134100039519,-0.15350714952449,0.95));
#72870=CARTESIAN_POINT('Origin',(0.,0.,0.95));
#72871=CARTESIAN_POINT('',(-0.768150047349522,-0.135445578580206,0.95));
#72872=CARTESIAN_POINT('Origin',(-0.768150047349522,-0.135445578580206,
0.95));
#72873=CARTESIAN_POINT('',(-0.785134100039519,-0.15350714952449,0.0499999999999999));
#72874=CARTESIAN_POINT('',(-0.785134100039519,-0.15350714952449,0.49));
#72875=CARTESIAN_POINT('',(-0.768150047349522,-0.135445578580206,0.0499999999999999));
#72876=CARTESIAN_POINT('Origin',(-0.800944407364116,-0.145664567054585,
0.0499999999999999));
#72877=CARTESIAN_POINT('Origin',(0.,0.,0.0499999999999999));
#72878=CARTESIAN_POINT('Origin',(-0.748445480318229,-0.381352019781219,
0.95));
#72879=CARTESIAN_POINT('',(-0.700120108151134,-0.387081172575526,0.0499999999999999));
#72880=CARTESIAN_POINT('',(-0.700120108151134,-0.387081172575526,0.95));
#72881=CARTESIAN_POINT('',(-0.700120108151134,-0.387081172575526,0.49));
#72882=CARTESIAN_POINT('',(-0.675499814951862,-0.39,0.0499999999999999));
#72883=CARTESIAN_POINT('',(-0.748445480318229,-0.381352019781219,0.0499999999999999));
#72884=CARTESIAN_POINT('',(-0.675499814951862,-0.39,0.95));
#72885=CARTESIAN_POINT('',(-0.675499814951862,-0.39,0.95));
#72886=CARTESIAN_POINT('',(-0.748445480318229,-0.381352019781219,0.95));
#72887=CARTESIAN_POINT('Origin',(-0.711972647635046,-0.419424404596921,
0.95));
#72888=CARTESIAN_POINT('',(-0.685282182852641,-0.412781213071428,0.95));
#72889=CARTESIAN_POINT('Origin',(0.,0.,0.95));
#72890=CARTESIAN_POINT('',(-0.675499814951862,-0.39,0.95));
#72891=CARTESIAN_POINT('Origin',(-0.675499814951862,-0.39,0.95));
#72892=CARTESIAN_POINT('',(-0.685282182852641,-0.412781213071428,0.0499999999999999));
#72893=CARTESIAN_POINT('',(-0.685282182852641,-0.412781213071428,0.49));
#72894=CARTESIAN_POINT('',(-0.675499814951862,-0.39,0.0499999999999999));
#72895=CARTESIAN_POINT('Origin',(-0.711972647635046,-0.419424404596921,
0.0499999999999999));
#72896=CARTESIAN_POINT('Origin',(0.,0.,0.0499999999999999));
#72897=CARTESIAN_POINT('Origin',(-0.572878622452499,-0.614337109360103,
0.95));
#72898=CARTESIAN_POINT('',(-0.525508141170504,-0.603192501249412,0.0499999999999999));
#72899=CARTESIAN_POINT('',(-0.525508141170504,-0.603192501249412,0.95));
#72900=CARTESIAN_POINT('',(-0.525508141170504,-0.603192501249412,0.49));
#72901=CARTESIAN_POINT('',(-0.501374335555501,-0.597514665632803,0.0499999999999999));
#72902=CARTESIAN_POINT('',(-0.572878622452499,-0.614337109360103,0.0499999999999999));
#72903=CARTESIAN_POINT('',(-0.501374335555501,-0.597514665632803,0.95));
#72904=CARTESIAN_POINT('',(-0.501374335555501,-0.597514665632803,0.95));
#72905=CARTESIAN_POINT('',(-0.572878622452499,-0.614337109360103,0.95));
#72906=CARTESIAN_POINT('Origin',(-0.537126479004,-0.634184247036264,0.95));
#72907=CARTESIAN_POINT('',(-0.502775120725853,-0.622267770320064,0.95));
#72908=CARTESIAN_POINT('Origin',(0.,0.,0.95));
#72909=CARTESIAN_POINT('',(-0.501374335555501,-0.597514665632803,0.95));
#72910=CARTESIAN_POINT('Origin',(-0.501374335555501,-0.597514665632803,
0.95));
#72911=CARTESIAN_POINT('',(-0.502775120725853,-0.622267770320064,0.0499999999999999));
#72912=CARTESIAN_POINT('',(-0.502775120725853,-0.622267770320064,0.49));
#72913=CARTESIAN_POINT('',(-0.501374335555501,-0.597514665632803,0.0499999999999999));
#72914=CARTESIAN_POINT('Origin',(-0.537126479004,-0.634184247036264,0.0499999999999999));
#72915=CARTESIAN_POINT('Origin',(0.,0.,0.0499999999999999));
#72916=CARTESIAN_POINT('Origin',(-0.32821414793099,-0.77322407690005,0.95));
#72917=CARTESIAN_POINT('',(-0.28751213669055,-0.746549912099409,0.0499999999999999));
#72918=CARTESIAN_POINT('',(-0.28751213669055,-0.746549912099409,0.95));
#72919=CARTESIAN_POINT('',(-0.28751213669055,-0.746549912099409,0.49));
#72920=CARTESIAN_POINT('',(-0.266775711794021,-0.732960244213009,0.0499999999999999));
#72921=CARTESIAN_POINT('',(-0.32821414793099,-0.77322407690005,0.0499999999999999));
#72922=CARTESIAN_POINT('',(-0.266775711794021,-0.732960244213009,0.95));
#72923=CARTESIAN_POINT('',(-0.266775711794021,-0.732960244213009,0.95));
#72924=CARTESIAN_POINT('',(-0.32821414793099,-0.77322407690005,0.95));
#72925=CARTESIAN_POINT('Origin',(-0.286903189949045,-0.768128119610979,
0.95));
#72926=CARTESIAN_POINT('',(-0.259625958869015,-0.756699650773902,0.95));
#72927=CARTESIAN_POINT('Origin',(0.,0.,0.95));
#72928=CARTESIAN_POINT('',(-0.266775711794021,-0.732960244213009,0.95));
#72929=CARTESIAN_POINT('Origin',(-0.266775711794021,-0.732960244213009,
0.95));
#72930=CARTESIAN_POINT('',(-0.259625958869015,-0.756699650773902,0.0499999999999999));
#72931=CARTESIAN_POINT('',(-0.259625958869015,-0.756699650773902,0.49));
#72932=CARTESIAN_POINT('',(-0.266775711794021,-0.732960244213009,0.0499999999999999));
#72933=CARTESIAN_POINT('Origin',(-0.286903189949045,-0.768128119610979,
0.0499999999999999));
#72934=CARTESIAN_POINT('Origin',(0.,0.,0.0499999999999999));
#72935=CARTESIAN_POINT('Origin',(-0.0439622032440732,-0.838848809193842,
0.95));
#72936=CARTESIAN_POINT('',(-0.014837925298494,-0.799862385646954,0.0499999999999999));
#72937=CARTESIAN_POINT('',(-0.014837925298494,-0.799862385646954,0.95));
#72938=CARTESIAN_POINT('',(-0.0148379252984941,-0.799862385646954,0.49));
#72939=CARTESIAN_POINT('',(-1.4328367550024E-16,-0.78,0.0499999999999999));
#72940=CARTESIAN_POINT('',(-0.0439622032440732,-0.838848809193842,0.0499999999999999));
#72941=CARTESIAN_POINT('',(-1.4328367550024E-16,-0.78,0.95));
#72942=CARTESIAN_POINT('',(-1.4328367550024E-16,-0.78,0.95));
#72943=CARTESIAN_POINT('',(-0.0439622032440732,-0.838848809193842,0.95));
#72944=CARTESIAN_POINT('Origin',(-1.52655665885959E-16,-0.809424404596921,
0.95));
#72945=CARTESIAN_POINT('',(0.0148379252984936,-0.799862385646954,0.95));
#72946=CARTESIAN_POINT('Origin',(0.,0.,0.95));
#72947=CARTESIAN_POINT('',(-1.4328367550024E-16,-0.78,0.95));
#72948=CARTESIAN_POINT('Origin',(-1.4328367550024E-16,-0.78,0.95));
#72949=CARTESIAN_POINT('',(0.0148379252984936,-0.799862385646954,0.0499999999999999));
#72950=CARTESIAN_POINT('',(0.0148379252984936,-0.799862385646954,0.49));
#72951=CARTESIAN_POINT('',(-1.4328367550024E-16,-0.78,0.0499999999999999));
#72952=CARTESIAN_POINT('Origin',(-1.52655665885959E-16,-0.809424404596921,
0.0499999999999999));
#72953=CARTESIAN_POINT('Origin',(0.,0.,0.0499999999999999));
#72954=CARTESIAN_POINT('Origin',(0.245592231967099,-0.80329599500895,0.95));
#72955=CARTESIAN_POINT('',(0.259625958869016,-0.756699650773901,0.0499999999999999));
#72956=CARTESIAN_POINT('',(0.259625958869016,-0.756699650773901,0.95));
#72957=CARTESIAN_POINT('',(0.259625958869016,-0.756699650773901,0.49));
#72958=CARTESIAN_POINT('',(0.266775711794022,-0.732960244213009,0.0499999999999999));
#72959=CARTESIAN_POINT('',(0.245592231967099,-0.80329599500895,0.0499999999999999));
#72960=CARTESIAN_POINT('',(0.266775711794022,-0.732960244213009,0.95));
#72961=CARTESIAN_POINT('',(0.266775711794022,-0.732960244213009,0.95));
#72962=CARTESIAN_POINT('',(0.245592231967099,-0.80329599500895,0.95));
#72963=CARTESIAN_POINT('Origin',(0.286903189949044,-0.768128119610979,0.95));
#72964=CARTESIAN_POINT('',(0.28751213669055,-0.746549912099409,0.95));
#72965=CARTESIAN_POINT('Origin',(0.,0.,0.95));
#72966=CARTESIAN_POINT('',(0.266775711794022,-0.732960244213009,0.95));
#72967=CARTESIAN_POINT('Origin',(0.266775711794022,-0.732960244213009,0.95));
#72968=CARTESIAN_POINT('',(0.28751213669055,-0.746549912099409,0.0499999999999999));
#72969=CARTESIAN_POINT('',(0.28751213669055,-0.746549912099409,0.49));
#72970=CARTESIAN_POINT('',(0.266775711794022,-0.732960244213009,0.0499999999999999));
#72971=CARTESIAN_POINT('Origin',(0.286903189949044,-0.768128119610979,0.0499999999999999));
#72972=CARTESIAN_POINT('Origin',(0.,0.,0.0499999999999999));
#72973=CARTESIAN_POINT('Origin',(0.50552461944772,-0.670853828439726,0.95));
#72974=CARTESIAN_POINT('',(0.502775120725853,-0.622267770320064,0.0499999999999999));
#72975=CARTESIAN_POINT('',(0.502775120725853,-0.622267770320064,0.95));
#72976=CARTESIAN_POINT('',(0.502775120725853,-0.622267770320064,0.49));
#72977=CARTESIAN_POINT('',(0.501374335555501,-0.597514665632803,0.0499999999999999));
#72978=CARTESIAN_POINT('',(0.50552461944772,-0.670853828439726,0.0499999999999999));
#72979=CARTESIAN_POINT('',(0.501374335555501,-0.597514665632803,0.95));
#72980=CARTESIAN_POINT('',(0.501374335555501,-0.597514665632803,0.95));
#72981=CARTESIAN_POINT('',(0.50552461944772,-0.670853828439726,0.95));
#72982=CARTESIAN_POINT('Origin',(0.537126479004,-0.634184247036265,0.95));
#72983=CARTESIAN_POINT('',(0.525508141170504,-0.603192501249412,0.95));
#72984=CARTESIAN_POINT('Origin',(0.,0.,0.95));
#72985=CARTESIAN_POINT('',(0.501374335555501,-0.597514665632803,0.95));
#72986=CARTESIAN_POINT('Origin',(0.501374335555501,-0.597514665632803,0.95));
#72987=CARTESIAN_POINT('',(0.525508141170504,-0.603192501249412,0.0499999999999999));
#72988=CARTESIAN_POINT('',(0.525508141170504,-0.603192501249412,0.49));
#72989=CARTESIAN_POINT('',(0.501374335555501,-0.597514665632803,0.0499999999999999));
#72990=CARTESIAN_POINT('Origin',(0.537126479004,-0.634184247036265,0.0499999999999999));
#72991=CARTESIAN_POINT('Origin',(0.,0.,0.0499999999999999));
#72992=CARTESIAN_POINT('Origin',(0.704483277074156,-0.457496789412623,0.95));
#72993=CARTESIAN_POINT('',(0.685282182852641,-0.412781213071429,0.0499999999999999));
#72994=CARTESIAN_POINT('',(0.685282182852641,-0.412781213071429,0.95));
#72995=CARTESIAN_POINT('',(0.685282182852641,-0.412781213071429,0.49));
#72996=CARTESIAN_POINT('',(0.675499814951862,-0.39,0.0499999999999999));
#72997=CARTESIAN_POINT('',(0.704483277074156,-0.457496789412623,0.0499999999999999));
#72998=CARTESIAN_POINT('',(0.675499814951862,-0.39,0.95));
#72999=CARTESIAN_POINT('',(0.675499814951862,-0.39,0.95));
#73000=CARTESIAN_POINT('',(0.704483277074156,-0.457496789412623,0.95));
#73001=CARTESIAN_POINT('Origin',(0.711972647635045,-0.419424404596921,0.95));
#73002=CARTESIAN_POINT('',(0.700120108151134,-0.387081172575526,0.95));
#73003=CARTESIAN_POINT('Origin',(0.,0.,0.95));
#73004=CARTESIAN_POINT('',(0.675499814951862,-0.39,0.95));
#73005=CARTESIAN_POINT('Origin',(0.675499814951862,-0.39,0.95));
#73006=CARTESIAN_POINT('',(0.700120108151134,-0.387081172575526,0.0499999999999999));
#73007=CARTESIAN_POINT('',(0.700120108151134,-0.387081172575526,0.49));
#73008=CARTESIAN_POINT('',(0.675499814951862,-0.39,0.0499999999999999));
#73009=CARTESIAN_POINT('Origin',(0.711972647635045,-0.419424404596921,0.0499999999999999));
#73010=CARTESIAN_POINT('Origin',(0.,0.,0.0499999999999999));
#73011=CARTESIAN_POINT('Origin',(0.818470854419598,-0.188958885648847,0.95));
#73012=CARTESIAN_POINT('',(0.785134100039519,-0.15350714952449,0.0499999999999999));
#73013=CARTESIAN_POINT('',(0.785134100039519,-0.15350714952449,0.95));
#73014=CARTESIAN_POINT('',(0.785134100039519,-0.15350714952449,0.49));
#73015=CARTESIAN_POINT('',(0.768150047349522,-0.135445578580206,0.0499999999999999));
#73016=CARTESIAN_POINT('',(0.818470854419598,-0.188958885648847,0.0499999999999999));
#73017=CARTESIAN_POINT('',(0.768150047349522,-0.135445578580206,0.95));
#73018=CARTESIAN_POINT('',(0.768150047349522,-0.135445578580206,0.95));
#73019=CARTESIAN_POINT('',(0.818470854419598,-0.188958885648847,0.95));
#73020=CARTESIAN_POINT('Origin',(0.800944407364116,-0.145664567054585,0.95));
#73021=CARTESIAN_POINT('',(0.790287257416402,-0.124282141779344,0.95));
#73022=CARTESIAN_POINT('Origin',(0.,0.,0.95));
#73023=CARTESIAN_POINT('',(0.768150047349522,-0.135445578580206,0.95));
#73024=CARTESIAN_POINT('Origin',(0.768150047349522,-0.135445578580206,0.95));
#73025=CARTESIAN_POINT('',(0.790287257416402,-0.124282141779344,0.0499999999999999));
#73026=CARTESIAN_POINT('',(0.790287257416402,-0.124282141779344,0.49));
#73027=CARTESIAN_POINT('',(0.768150047349522,-0.135445578580206,0.0499999999999999));
#73028=CARTESIAN_POINT('Origin',(0.800944407364116,-0.145664567054585,0.0499999999999999));
#73029=CARTESIAN_POINT('Origin',(0.,0.,0.0499999999999999));
#73030=CARTESIAN_POINT('Origin',(0.45,0.,-3.5));
#73031=CARTESIAN_POINT('',(-0.45,-5.51091059616309E-17,-3.5));
#73032=CARTESIAN_POINT('Origin',(0.,0.,-3.5));
#73033=CARTESIAN_POINT('Origin',(0.,0.,-3.475));
#73034=CARTESIAN_POINT('',(-0.475,-5.81707229594993E-17,-3.475));
#73035=CARTESIAN_POINT('Origin',(0.,0.,0.015));
#73036=CARTESIAN_POINT('',(-0.8,-9.79717439317883E-17,0.03));
#73037=CARTESIAN_POINT('Origin',(0.,0.,0.03));
#73038=CARTESIAN_POINT('',(-0.785,-9.61347737330672E-17,0.015));
#73039=CARTESIAN_POINT('Origin',(0.,0.,0.49));
#73040=CARTESIAN_POINT('Origin',(0.,0.,0.95));
#73041=CARTESIAN_POINT('Origin',(0.,0.,0.95));
#73042=CARTESIAN_POINT('Origin',(0.,0.,0.95));
#73043=CARTESIAN_POINT('Origin',(0.,0.,0.95));
#73044=CARTESIAN_POINT('Origin',(0.,0.,0.95));
#73045=CARTESIAN_POINT('Origin',(0.,0.,0.95));
#73046=CARTESIAN_POINT('Origin',(0.,0.,0.95));
#73047=CARTESIAN_POINT('Origin',(0.,0.,0.95));
#73048=CARTESIAN_POINT('Origin',(0.,0.,0.95));
#73049=CARTESIAN_POINT('Origin',(0.,0.,0.95));
#73050=CARTESIAN_POINT('Origin',(0.,0.,0.95));
#73051=CARTESIAN_POINT('Origin',(0.,0.,0.95));
#73052=CARTESIAN_POINT('Origin',(0.,0.,0.95));
#73053=CARTESIAN_POINT('Origin',(0.,0.,0.95));
#73054=CARTESIAN_POINT('Origin',(0.,0.,0.95));
#73055=CARTESIAN_POINT('Origin',(0.,0.,0.95));
#73056=CARTESIAN_POINT('',(-0.8,-9.79717439317883E-17,0.49));
#73057=CARTESIAN_POINT('Origin',(0.,0.,0.95));
#73058=CARTESIAN_POINT('Origin',(0.,0.,0.95));
#73059=CARTESIAN_POINT('Origin',(0.,0.,0.95));
#73060=CARTESIAN_POINT('Origin',(0.,0.,0.95));
#73061=CARTESIAN_POINT('Origin',(0.,0.,0.95));
#73062=CARTESIAN_POINT('Origin',(0.,0.,0.95));
#73063=CARTESIAN_POINT('Origin',(0.,0.,0.95));
#73064=CARTESIAN_POINT('Origin',(0.,0.,0.95));
#73065=CARTESIAN_POINT('Origin',(0.,0.,0.95));
#73066=CARTESIAN_POINT('Origin',(0.,0.,0.95));
#73067=CARTESIAN_POINT('Origin',(0.,0.,0.95));
#73068=CARTESIAN_POINT('Origin',(0.,0.,0.95));
#73069=CARTESIAN_POINT('Origin',(0.,0.,0.95));
#73070=CARTESIAN_POINT('Origin',(0.,0.,0.95));
#73071=CARTESIAN_POINT('Origin',(0.,0.,0.95));
#73072=CARTESIAN_POINT('Origin',(0.,0.,0.95));
#73073=CARTESIAN_POINT('Origin',(0.,0.,0.95));
#73074=CARTESIAN_POINT('Origin',(0.,0.,0.95));
#73075=CARTESIAN_POINT('Origin',(0.,0.,0.95));
#73076=CARTESIAN_POINT('Origin',(0.,0.,0.95));
#73077=CARTESIAN_POINT('Origin',(0.,0.,0.975));
#73078=CARTESIAN_POINT('',(-0.75,-9.18485099360515E-17,1.));
#73079=CARTESIAN_POINT('Origin',(0.,0.,1.));
#73080=CARTESIAN_POINT('',(-0.775,-9.49101269339199E-17,0.975));
#73081=CARTESIAN_POINT('Origin',(0.,0.,1.));
#76636=UNCERTAINTY_MEASURE_WITH_UNIT(LENGTH_MEASURE(0.001),#76661,
'DISTANCE_ACCURACY_VALUE',
'Maximum model space distance between geometric entities at asserted c
onnectivities');
#76638=UNCERTAINTY_MEASURE_WITH_UNIT(LENGTH_MEASURE(0.001),#76661,
'DISTANCE_ACCURACY_VALUE',
'Maximum model space distance between geometric entities at asserted c
onnectivities');
#76658=(
GEOMETRIC_REPRESENTATION_CONTEXT(3)
GLOBAL_UNCERTAINTY_ASSIGNED_CONTEXT((#76636))
GLOBAL_UNIT_ASSIGNED_CONTEXT((#76661,#76663,#76664))
REPRESENTATION_CONTEXT('','3D')
);
#76660=(
GEOMETRIC_REPRESENTATION_CONTEXT(3)
GLOBAL_UNCERTAINTY_ASSIGNED_CONTEXT((#76638))
GLOBAL_UNIT_ASSIGNED_CONTEXT((#76661,#76663,#76664))
REPRESENTATION_CONTEXT('','3D')
);
#76661=(
LENGTH_UNIT()
NAMED_UNIT(*)
SI_UNIT(.CENTI.,.METRE.)
);
#76663=(
NAMED_UNIT(*)
PLANE_ANGLE_UNIT()
SI_UNIT($,.RADIAN.)
);
#76664=(
NAMED_UNIT(*)
SI_UNIT($,.STERADIAN.)
SOLID_ANGLE_UNIT()
);
#76684=SHAPE_DEFINITION_REPRESENTATION(#76705,#76754);
#76705=PRODUCT_DEFINITION_SHAPE('',$,#76776);
#76754=SHAPE_REPRESENTATION('',(#28632),#76658);
#76756=PRODUCT_DEFINITION_CONTEXT('part definition',#76821,'design');
#76776=PRODUCT_DEFINITION('2026-10-26-11-13-40-862',
'19_Casing_Screw_ISO_4762_M10x35',#76797,#76756);
#76797=PRODUCT_DEFINITION_FORMATION('',$,#76842);
#76821=APPLICATION_CONTEXT(
'Core Data for Automotive Mechanical Design Process');
#76822=PRODUCT_CONTEXT('part definition',#76821,'mechanical');
#76842=PRODUCT('2026-10-26-11-13-40-862',
'19_Casing_Screw_ISO_4762_M10x35',$,(#76822));
#76907=COLOUR_RGB('Black',0.12,0.14,0.17);
#76908=FILL_AREA_STYLE_COLOUR('',#76907);
#76909=FILL_AREA_STYLE('',(#76908));
#76910=SURFACE_STYLE_FILL_AREA(#76909);
#76911=SURFACE_SIDE_STYLE('',(#76910));
#76912=SURFACE_STYLE_USAGE(.BOTH.,#76911);
#76913=PRESENTATION_STYLE_ASSIGNMENT((#76912));
ENDSEC;
END-ISO-10303-21;
